ISO-10303-21;
HEADER;
/* Generated by software containing ST-Developer
 * from STEP Tools, Inc. (www.steptools.com) 
 */

FILE_DESCRIPTION(
/* description */ (''),
/* implementation_level */ '2;1');

FILE_NAME(
/* name */ 'Socket head cap screw M3x16.step',
/* time_stamp */ '2026-11-10T09:09:39-08:00',
/* author */ (''),
/* organization */ (''),
/* preprocessor_version */ 'ST-DEVELOPER v20.2',
/* originating_system */ 'Autodesk Translation Framework v15.17.0.0',
/* authorisation */ '');

FILE_SCHEMA (('AUTOMOTIVE_DESIGN { 1 0 10303 214 3 1 1 }'));
ENDSEC;

DATA;
#10=MECHANICAL_DESIGN_GEOMETRIC_PRESENTATION_REPRESENTATION('',(#561),#18353);
#167=B_SPLINE_SURFACE_WITH_KNOTS('',3,3,((#15603,#15604,#15605,#15606,#15607,
#15608,#15609,#15610,#15611,#15612,#15613,#15614,#15615,#15616,#15617,#15618,
#15619,#15620,#15621,#15622,#15623,#15624,#15625,#15626,#15627,#15628,#15629,
#15630,#15631,#15632,#15633,#15634,#15635,#15636,#15637,#15638,#15639,#15640,
#15641,#15642,#15643,#15644,#15645,#15646,#15647,#15648,#15649,#15650,#15651,
#15652,#15653,#15654,#15655,#15656,#15657,#15658,#15659,#15660,#15661,#15662,
#15663,#15664,#15665,#15666,#15667,#15668,#15669,#15670,#15671,#15672,#15673,
#15674,#15675,#15676,#15677,#15678,#15679,#15680,#15681,#15682,#15683,#15684,
#15685,#15686,#15687,#15688,#15689,#15690,#15691,#15692,#15693,#15694,#15695,
#15696,#15697,#15698,#15699,#15700,#15701,#15702,#15703,#15704,#15705,#15706,
#15707,#15708,#15709,#15710,#15711,#15712,#15713,#15714,#15715,#15716,#15717,
#15718,#15719,#15720,#15721,#15722,#15723,#15724,#15725,#15726,#15727,#15728,
#15729,#15730,#15731,#15732,#15733,#15734,#15735,#15736,#15737,#15738,#15739,
#15740,#15741,#15742,#15743,#15744,#15745,#15746,#15747,#15748,#15749,#15750,
#15751,#15752,#15753,#15754,#15755,#15756,#15757,#15758,#15759,#15760,#15761,
#15762,#15763,#15764,#15765,#15766,#15767,#15768,#15769,#15770,#15771,#15772,
#15773,#15774,#15775,#15776,#15777,#15778,#15779,#15780,#15781,#15782,#15783,
#15784,#15785,#15786,#15787,#15788,#15789,#15790,#15791,#15792,#15793,#15794,
#15795,#15796,#15797,#15798),(#15799,#15800,#15801,#15802,#15803,#15804,
#15805,#15806,#15807,#15808,#15809,#15810,#15811,#15812,#15813,#15814,#15815,
#15816,#15817,#15818,#15819,#15820,#15821,#15822,#15823,#15824,#15825,#15826,
#15827,#15828,#15829,#15830,#15831,#15832,#15833,#15834,#15835,#15836,#15837,
#15838,#15839,#15840,#15841,#15842,#15843,#15844,#15845,#15846,#15847,#15848,
#15849,#15850,#15851,#15852,#15853,#15854,#15855,#15856,#15857,#15858,#15859,
#15860,#15861,#15862,#15863,#15864,#15865,#15866,#15867,#15868,#15869,#15870,
#15871,#15872,#15873,#15874,#15875,#15876,#15877,#15878,#15879,#15880,#15881,
#15882,#15883,#15884,#15885,#15886,#15887,#15888,#15889,#15890,#15891,#15892,
#15893,#15894,#15895,#15896,#15897,#15898,#15899,#15900,#15901,#15902,#15903,
#15904,#15905,#15906,#15907,#15908,#15909,#15910,#15911,#15912,#15913,#15914,
#15915,#15916,#15917,#15918,#15919,#15920,#15921,#15922,#15923,#15924,#15925,
#15926,#15927,#15928,#15929,#15930,#15931,#15932,#15933,#15934,#15935,#15936,
#15937,#15938,#15939,#15940,#15941,#15942,#15943,#15944,#15945,#15946,#15947,
#15948,#15949,#15950,#15951,#15952,#15953,#15954,#15955,#15956,#15957,#15958,
#15959,#15960,#15961,#15962,#15963,#15964,#15965,#15966,#15967,#15968,#15969,
#15970,#15971,#15972,#15973,#15974,#15975,#15976,#15977,#15978,#15979,#15980,
#15981,#15982,#15983,#15984,#15985,#15986,#15987,#15988,#15989,#15990,#15991,
#15992,#15993,#15994),(#15995,#15996,#15997,#15998,#15999,#16000,#16001,
#16002,#16003,#16004,#16005,#16006,#16007,#16008,#16009,#16010,#16011,#16012,
#16013,#16014,#16015,#16016,#16017,#16018,#16019,#16020,#16021,#16022,#16023,
#16024,#16025,#16026,#16027,#16028,#16029,#16030,#16031,#16032,#16033,#16034,
#16035,#16036,#16037,#16038,#16039,#16040,#16041,#16042,#16043,#16044,#16045,
#16046,#16047,#16048,#16049,#16050,#16051,#16052,#16053,#16054,#16055,#16056,
#16057,#16058,#16059,#16060,#16061,#16062,#16063,#16064,#16065,#16066,#16067,
#16068,#16069,#16070,#16071,#16072,#16073,#16074,#16075,#16076,#16077,#16078,
#16079,#16080,#16081,#16082,#16083,#16084,#16085,#16086,#16087,#16088,#16089,
#16090,#16091,#16092,#16093,#16094,#16095,#16096,#16097,#16098,#16099,#16100,
#16101,#16102,#16103,#16104,#16105,#16106,#16107,#16108,#16109,#16110,#16111,
#16112,#16113,#16114,#16115,#16116,#16117,#16118,#16119,#16120,#16121,#16122,
#16123,#16124,#16125,#16126,#16127,#16128,#16129,#16130,#16131,#16132,#16133,
#16134,#16135,#16136,#16137,#16138,#16139,#16140,#16141,#16142,#16143,#16144,
#16145,#16146,#16147,#16148,#16149,#16150,#16151,#16152,#16153,#16154,#16155,
#16156,#16157,#16158,#16159,#16160,#16161,#16162,#16163,#16164,#16165,#16166,
#16167,#16168,#16169,#16170,#16171,#16172,#16173,#16174,#16175,#16176,#16177,
#16178,#16179,#16180,#16181,#16182,#16183,#16184,#16185,#16186,#16187,#16188,
#16189,#16190),(#16191,#16192,#16193,#16194,#16195,#16196,#16197,#16198,
#16199,#16200,#16201,#16202,#16203,#16204,#16205,#16206,#16207,#16208,#16209,
#16210,#16211,#16212,#16213,#16214,#16215,#16216,#16217,#16218,#16219,#16220,
#16221,#16222,#16223,#16224,#16225,#16226,#16227,#16228,#16229,#16230,#16231,
#16232,#16233,#16234,#16235,#16236,#16237,#16238,#16239,#16240,#16241,#16242,
#16243,#16244,#16245,#16246,#16247,#16248,#16249,#16250,#16251,#16252,#16253,
#16254,#16255,#16256,#16257,#16258,#16259,#16260,#16261,#16262,#16263,#16264,
#16265,#16266,#16267,#16268,#16269,#16270,#16271,#16272,#16273,#16274,#16275,
#16276,#16277,#16278,#16279,#16280,#16281,#16282,#16283,#16284,#16285,#16286,
#16287,#16288,#16289,#16290,#16291,#16292,#16293,#16294,#16295,#16296,#16297,
#16298,#16299,#16300,#16301,#16302,#16303,#16304,#16305,#16306,#16307,#16308,
#16309,#16310,#16311,#16312,#16313,#16314,#16315,#16316,#16317,#16318,#16319,
#16320,#16321,#16322,#16323,#16324,#16325,#16326,#16327,#16328,#16329,#16330,
#16331,#16332,#16333,#16334,#16335,#16336,#16337,#16338,#16339,#16340,#16341,
#16342,#16343,#16344,#16345,#16346,#16347,#16348,#16349,#16350,#16351,#16352,
#16353,#16354,#16355,#16356,#16357,#16358,#16359,#16360,#16361,#16362,#16363,
#16364,#16365,#16366,#16367,#16368,#16369,#16370,#16371,#16372,#16373,#16374,
#16375,#16376,#16377,#16378,#16379,#16380,#16381,#16382,#16383,#16384,#16385,
#16386)),.UNSPECIFIED.,.F.,.F.,.F.,(4,4),(4,1,1,1,1,1,1,1,1,1,1,1,1,1,1,
1,1,1,1,1,1,1,1,1,1,1,1,1,1,1,1,1,1,1,1,1,1,1,1,1,1,1,1,1,1,1,1,1,1,1,1,
1,1,1,1,1,1,1,1,1,1,1,1,1,1,1,1,1,1,1,1,1,1,1,1,1,1,1,1,1,1,1,1,1,1,1,1,
1,1,1,1,1,1,1,1,1,1,1,1,1,1,1,1,1,1,1,1,1,1,1,1,1,1,1,1,1,1,1,1,1,1,1,1,
1,1,1,1,1,1,1,1,1,1,1,1,1,1,1,1,1,1,1,1,1,1,1,1,1,1,1,1,1,1,1,1,1,1,1,1,
1,1,1,1,1,1,1,1,1,1,1,1,1,1,1,1,1,1,1,1,1,1,1,1,1,1,1,1,1,1,1,1,1,1,4),
(0.,0.0329955678841871),(11.6159397475006,12.61358260836,13.6112254692194,
14.6088683300789,15.6065111909383,16.6041540517977,17.6017969126571,18.5994397735165,
19.5970826343759,20.5947254952353,21.5923683560947,22.5900112169541,23.5876540778135,
24.5852969386729,25.5829397995323,26.5805826603917,27.5782255212511,28.5758683821105,
29.5735112429699,30.5711541038294,31.5687969646888,32.5664398255482,33.5640826864076,
34.561725547267,35.5593684081264,36.5570112689858,37.5546541298452,38.5522969907046,
39.549939851564,40.5475827124234,41.5452255732828,42.5428684341422,43.5405112950016,
44.538154155861,45.5357970167204,46.5334398775799,47.5310827384393,48.5287255992987,
49.5263684601581,50.5240113210175,51.5216541818769,52.5192970427363,53.5169399035957,
54.5145827644551,55.5122256253145,56.5098684861739,57.5075113470333,58.5051542078927,
59.5027970687521,60.5004399296115,61.4980827904709,62.4957256513303,63.4933685121897,
64.4910113730492,65.4886542339086,66.486297094768,67.4839399556274,68.4815828164868,
69.4792256773462,70.4768685382056,71.474511399065,72.4721542599244,73.4697971207838,
74.4674399816432,75.4650828425026,76.462725703362,77.4603685642214,78.4580114250808,
79.4556542859402,80.4532971467996,81.4509400076591,82.4485828685185,83.4462257293779,
84.4438685902373,85.4415114510967,86.4391543119561,87.4367971728155,88.4344400336749,
89.4320828945343,90.4297257553937,91.4273686162531,92.4250114771125,93.4226543379719,
94.4202971988313,95.4179400596907,96.4155829205502,97.4132257814096,98.410868642269,
99.4085115031284,100.406154363988,101.403797224847,102.401440085707,103.399082946566,
104.396725807425,105.394368668285,106.392011529144,107.389654390004,108.387297250863,
109.384940111722,110.382582972582,111.380225833441,112.377868694301,113.37551155516,
114.373154416019,115.370797276879,116.368440137738,117.366082998598,118.363725859457,
119.361368720316,120.359011581176,121.356654442035,122.354297302895,123.351940163754,
124.349583024614,125.347225885473,126.344868746332,127.342511607192,128.340154468051,
129.337797328911,130.33544018977,131.333083050629,132.330725911489,133.328368772348,
134.326011633208,135.323654494067,136.321297354926,137.318940215786,138.316583076645,
139.314225937505,140.311868798364,141.309511659223,142.307154520083,143.304797380942,
144.302440241802,145.300083102661,146.29772596352,147.29536882438,148.293011685239,
149.290654546099,150.288297406958,151.285940267817,152.283583128677,153.281225989536,
154.278868850396,155.276511711255,156.274154572115,157.271797432974,158.269440293833,
159.267083154693,160.264726015552,161.262368876412,162.260011737271,163.25765459813,
164.25529745899,165.252940319849,166.250583180709,167.248226041568,168.245868902427,
169.243511763287,170.241154624146,171.238797485006,172.236440345865,173.234083206724,
174.231726067584,175.229368928443,176.227011789303,177.224654650162,178.222297511021,
179.219940371881,180.21758323274,181.2152260936,182.212868954459,183.210511815318,
184.208154676178,185.205797537037,186.203440397897,187.201083258756,188.198726119616,
189.196368980475,190.194011841334,191.191654702194,192.189297563053,193.186940423913,
194.184583284772,195.182226145631,196.179869006491,197.17751186735,198.17515472821,
199.172797589069,200.170440449928,201.168083310788,202.165726171647,203.163369032507,
204.161011893366),.UNSPECIFIED.);
#168=B_SPLINE_SURFACE_WITH_KNOTS('',3,3,((#16476,#16477,#16478,#16479,#16480,
#16481,#16482,#16483,#16484,#16485,#16486,#16487,#16488,#16489,#16490,#16491,
#16492,#16493,#16494,#16495,#16496,#16497,#16498,#16499,#16500,#16501,#16502,
#16503,#16504,#16505,#16506,#16507,#16508,#16509,#16510,#16511,#16512,#16513,
#16514,#16515,#16516,#16517,#16518,#16519,#16520,#16521,#16522,#16523,#16524,
#16525,#16526,#16527,#16528,#16529,#16530,#16531,#16532,#16533,#16534,#16535,
#16536,#16537,#16538,#16539,#16540,#16541,#16542,#16543,#16544,#16545,#16546,
#16547,#16548,#16549,#16550,#16551,#16552,#16553,#16554,#16555,#16556,#16557,
#16558,#16559,#16560,#16561,#16562,#16563,#16564,#16565,#16566,#16567,#16568,
#16569,#16570,#16571,#16572,#16573,#16574,#16575,#16576,#16577,#16578,#16579,
#16580,#16581,#16582,#16583,#16584,#16585,#16586,#16587,#16588,#16589,#16590,
#16591,#16592,#16593,#16594,#16595,#16596,#16597,#16598,#16599,#16600,#16601,
#16602,#16603,#16604,#16605,#16606,#16607,#16608,#16609,#16610,#16611,#16612,
#16613,#16614,#16615,#16616,#16617,#16618,#16619,#16620,#16621,#16622,#16623,
#16624,#16625,#16626,#16627,#16628,#16629,#16630,#16631,#16632,#16633,#16634,
#16635,#16636,#16637,#16638,#16639,#16640,#16641,#16642,#16643,#16644,#16645,
#16646,#16647,#16648,#16649,#16650,#16651,#16652,#16653,#16654,#16655,#16656,
#16657,#16658,#16659,#16660,#16661,#16662,#16663,#16664,#16665,#16666,#16667,
#16668,#16669,#16670,#16671,#16672,#16673),(#16674,#16675,#16676,#16677,
#16678,#16679,#16680,#16681,#16682,#16683,#16684,#16685,#16686,#16687,#16688,
#16689,#16690,#16691,#16692,#16693,#16694,#16695,#16696,#16697,#16698,#16699,
#16700,#16701,#16702,#16703,#16704,#16705,#16706,#16707,#16708,#16709,#16710,
#16711,#16712,#16713,#16714,#16715,#16716,#16717,#16718,#16719,#16720,#16721,
#16722,#16723,#16724,#16725,#16726,#16727,#16728,#16729,#16730,#16731,#16732,
#16733,#16734,#16735,#16736,#16737,#16738,#16739,#16740,#16741,#16742,#16743,
#16744,#16745,#16746,#16747,#16748,#16749,#16750,#16751,#16752,#16753,#16754,
#16755,#16756,#16757,#16758,#16759,#16760,#16761,#16762,#16763,#16764,#16765,
#16766,#16767,#16768,#16769,#16770,#16771,#16772,#16773,#16774,#16775,#16776,
#16777,#16778,#16779,#16780,#16781,#16782,#16783,#16784,#16785,#16786,#16787,
#16788,#16789,#16790,#16791,#16792,#16793,#16794,#16795,#16796,#16797,#16798,
#16799,#16800,#16801,#16802,#16803,#16804,#16805,#16806,#16807,#16808,#16809,
#16810,#16811,#16812,#16813,#16814,#16815,#16816,#16817,#16818,#16819,#16820,
#16821,#16822,#16823,#16824,#16825,#16826,#16827,#16828,#16829,#16830,#16831,
#16832,#16833,#16834,#16835,#16836,#16837,#16838,#16839,#16840,#16841,#16842,
#16843,#16844,#16845,#16846,#16847,#16848,#16849,#16850,#16851,#16852,#16853,
#16854,#16855,#16856,#16857,#16858,#16859,#16860,#16861,#16862,#16863,#16864,
#16865,#16866,#16867,#16868,#16869,#16870,#16871),(#16872,#16873,#16874,
#16875,#16876,#16877,#16878,#16879,#16880,#16881,#16882,#16883,#16884,#16885,
#16886,#16887,#16888,#16889,#16890,#16891,#16892,#16893,#16894,#16895,#16896,
#16897,#16898,#16899,#16900,#16901,#16902,#16903,#16904,#16905,#16906,#16907,
#16908,#16909,#16910,#16911,#16912,#16913,#16914,#16915,#16916,#16917,#16918,
#16919,#16920,#16921,#16922,#16923,#16924,#16925,#16926,#16927,#16928,#16929,
#16930,#16931,#16932,#16933,#16934,#16935,#16936,#16937,#16938,#16939,#16940,
#16941,#16942,#16943,#16944,#16945,#16946,#16947,#16948,#16949,#16950,#16951,
#16952,#16953,#16954,#16955,#16956,#16957,#16958,#16959,#16960,#16961,#16962,
#16963,#16964,#16965,#16966,#16967,#16968,#16969,#16970,#16971,#16972,#16973,
#16974,#16975,#16976,#16977,#16978,#16979,#16980,#16981,#16982,#16983,#16984,
#16985,#16986,#16987,#16988,#16989,#16990,#16991,#16992,#16993,#16994,#16995,
#16996,#16997,#16998,#16999,#17000,#17001,#17002,#17003,#17004,#17005,#17006,
#17007,#17008,#17009,#17010,#17011,#17012,#17013,#17014,#17015,#17016,#17017,
#17018,#17019,#17020,#17021,#17022,#17023,#17024,#17025,#17026,#17027,#17028,
#17029,#17030,#17031,#17032,#17033,#17034,#17035,#17036,#17037,#17038,#17039,
#17040,#17041,#17042,#17043,#17044,#17045,#17046,#17047,#17048,#17049,#17050,
#17051,#17052,#17053,#17054,#17055,#17056,#17057,#17058,#17059,#17060,#17061,
#17062,#17063,#17064,#17065,#17066,#17067,#17068,#17069),(#17070,#17071,
#17072,#17073,#17074,#17075,#17076,#17077,#17078,#17079,#17080,#17081,#17082,
#17083,#17084,#17085,#17086,#17087,#17088,#17089,#17090,#17091,#17092,#17093,
#17094,#17095,#17096,#17097,#17098,#17099,#17100,#17101,#17102,#17103,#17104,
#17105,#17106,#17107,#17108,#17109,#17110,#17111,#17112,#17113,#17114,#17115,
#17116,#17117,#17118,#17119,#17120,#17121,#17122,#17123,#17124,#17125,#17126,
#17127,#17128,#17129,#17130,#17131,#17132,#17133,#17134,#17135,#17136,#17137,
#17138,#17139,#17140,#17141,#17142,#17143,#17144,#17145,#17146,#17147,#17148,
#17149,#17150,#17151,#17152,#17153,#17154,#17155,#17156,#17157,#17158,#17159,
#17160,#17161,#17162,#17163,#17164,#17165,#17166,#17167,#17168,#17169,#17170,
#17171,#17172,#17173,#17174,#17175,#17176,#17177,#17178,#17179,#17180,#17181,
#17182,#17183,#17184,#17185,#17186,#17187,#17188,#17189,#17190,#17191,#17192,
#17193,#17194,#17195,#17196,#17197,#17198,#17199,#17200,#17201,#17202,#17203,
#17204,#17205,#17206,#17207,#17208,#17209,#17210,#17211,#17212,#17213,#17214,
#17215,#17216,#17217,#17218,#17219,#17220,#17221,#17222,#17223,#17224,#17225,
#17226,#17227,#17228,#17229,#17230,#17231,#17232,#17233,#17234,#17235,#17236,
#17237,#17238,#17239,#17240,#17241,#17242,#17243,#17244,#17245,#17246,#17247,
#17248,#17249,#17250,#17251,#17252,#17253,#17254,#17255,#17256,#17257,#17258,
#17259,#17260,#17261,#17262,#17263,#17264,#17265,#17266,#17267)),
 .UNSPECIFIED.,.F.,.F.,.F.,(4,4),(4,1,1,1,1,1,1,1,1,1,1,1,1,1,1,1,1,1,1,
1,1,1,1,1,1,1,1,1,1,1,1,1,1,1,1,1,1,1,1,1,1,1,1,1,1,1,1,1,1,1,1,1,1,1,1,
1,1,1,1,1,1,1,1,1,1,1,1,1,1,1,1,1,1,1,1,1,1,1,1,1,1,1,1,1,1,1,1,1,1,1,1,
1,1,1,1,1,1,1,1,1,1,1,1,1,1,1,1,1,1,1,1,1,1,1,1,1,1,1,1,1,1,1,1,1,1,1,1,
1,1,1,1,1,1,1,1,1,1,1,1,1,1,1,1,1,1,1,1,1,1,1,1,1,1,1,1,1,1,1,1,1,1,1,1,
1,1,1,1,1,1,1,1,1,1,1,1,1,1,1,1,1,1,1,1,1,1,1,1,1,1,1,1,1,1,1,1,4),(0.,
0.0329955678841871),(8.30203615430855,9.30007843543257,10.2981207165566,
11.2961629976806,12.2942052788047,13.2922475599287,14.2902898410527,15.2883321221767,
16.2863744033008,17.2844166844248,18.2824589655488,19.2805012466728,20.2785435277969,
21.2765858089209,22.2746280900449,23.272670371169,24.270712652293,25.268754933417,
26.266797214541,27.2648394956651,28.2628817767891,29.2609240579131,30.2589663390371,
31.2570086201612,32.2550509012852,33.2530931824092,34.2511354635333,35.2491777446573,
36.2472200257813,37.2452623069053,38.2433045880294,39.2413468691534,40.2393891502774,
41.2374314314014,42.2354737125255,43.2335159936495,44.2315582747735,45.2296005558975,
46.2276428370216,47.2256851181456,48.2237273992696,49.2217696803937,50.2198119615177,
51.2178542426417,52.2158965237657,53.2139388048898,54.2119810860138,55.2100233671378,
56.2080656482619,57.2061079293859,58.2041502105099,59.2021924916339,60.200234772758,
61.198277053882,62.196319335006,63.19436161613,64.1924038972541,65.1904461783781,
66.1884884595021,67.1865307406262,68.1845730217502,69.1826153028742,70.1806575839982,
71.1786998651223,72.1767421462463,73.1747844273703,74.1728267084943,75.1708689896184,
76.1689112707424,77.1669535518664,78.1649958329905,79.1630381141145,80.1610803952385,
81.1591226763625,82.1571649574865,83.1552072386106,84.1532495197346,85.1512918008586,
86.1493340819827,87.1473763631067,88.1454186442307,89.1434609253548,90.1415032064788,
91.1395454876028,92.1375877687268,93.1356300498508,94.1336723309749,95.1317146120989,
96.1297568932229,97.127799174347,98.125841455471,99.123883736595,100.121926017719,
101.119968298843,102.118010579967,103.116052861091,104.114095142215,105.112137423339,
106.110179704463,107.108221985587,108.106264266711,109.104306547835,110.102348828959,
111.100391110083,112.098433391207,113.096475672331,114.094517953455,115.092560234579,
116.090602515703,117.088644796828,118.086687077952,119.084729359076,120.0827716402,
121.080813921324,122.078856202448,123.076898483572,124.074940764696,125.07298304582,
126.071025326944,127.069067608068,128.067109889192,129.065152170316,130.06319445144,
131.061236732564,132.059279013688,133.057321294812,134.055363575936,135.05340585706,
136.051448138184,137.049490419308,138.047532700432,139.045574981556,140.04361726268,
141.041659543804,142.039701824928,143.037744106052,144.035786387176,145.0338286683,
146.031870949424,147.029913230548,148.027955511672,149.025997792796,150.02404007392,
151.022082355044,152.020124636168,153.018166917292,154.016209198417,155.014251479541,
156.012293760665,157.010336041789,158.008378322913,159.006420604037,160.004462885161,
161.002505166285,162.000547447409,162.998589728533,163.996632009657,164.994674290781,
165.992716571905,166.990758853029,167.988801134153,168.986843415277,169.984885696401,
170.982927977525,171.980970258649,172.979012539773,173.977054820897,174.975097102021,
175.973139383145,176.971181664269,177.969223945393,178.967266226517,179.965308507641,
180.963350788765,181.961393069889,182.959435351013,183.957477632137,184.955519913261,
185.953562194385,186.951604475509,187.949646756633,188.947689037757,189.945731318881,
190.943773600006,191.94181588113,192.939858162254,193.937900443378,194.935942724502,
195.933985005626,196.93202728675,197.930069567874,198.928111848998,199.926154130122,
200.924196411246,201.92223869237,202.920280973494),.UNSPECIFIED.);
#381=B_SPLINE_CURVE_WITH_KNOTS('',3,(#13227,#13228,#13229,#13230,#13231,
#13232,#13233,#13234,#13235,#13236),.UNSPECIFIED.,.F.,.F.,(4,3,3,4),(-4.09202352044852,
-3.99057144343763,-2.99292858257822,-2.07317267331971),.UNSPECIFIED.);
#382=B_SPLINE_CURVE_WITH_KNOTS('',3,(#13239,#13240,#13241,#13242,#13243,
#13244,#13245),.UNSPECIFIED.,.F.,.F.,(4,3,4),(0.,0.998042281124014,1.12274180646116),
 .UNSPECIFIED.);
#383=B_SPLINE_CURVE_WITH_KNOTS('',3,(#13250,#13251,#13252,#13253,#13254,
#13255,#13256,#13257,#13258,#13259,#13260,#13261,#13262,#13263,#13264,#13265,
#13266,#13267,#13268,#13269,#13270,#13271),.UNSPECIFIED.,.F.,.F.,(4,3,3,
3,3,3,3,4),(-10.3752088276281,-9.97642860859406,-8.97878574773466,-7.98114288687525,
-6.98350002601584,-5.98585716515644,-4.98821430429703,-4.09202352044852),
 .UNSPECIFIED.);
#384=B_SPLINE_CURVE_WITH_KNOTS('',3,(#13272,#13273,#13274,#13275,#13276,
#13277,#13278,#13279,#13280,#13281,#13282,#13283,#13284,#13285,#13286,#13287,
#13288,#13289,#13290,#13291,#13292,#13293),.UNSPECIFIED.,.F.,.F.,(4,3,3,
3,3,3,3,4),(1.12274180646116,1.99608456224804,2.99412684337208,3.99216912449611,
4.99021140562014,5.98825368674417,6.98629596786821,7.40592711364074),
 .UNSPECIFIED.);
#385=B_SPLINE_CURVE_WITH_KNOTS('',3,(#13298,#13299,#13300,#13301,#13302,
#13303,#13304,#13305,#13306,#13307,#13308,#13309,#13310,#13311,#13312,#13313,
#13314,#13315,#13316,#13317,#13318,#13319),.UNSPECIFIED.,.F.,.F.,(4,3,3,
3,3,3,3,4),(-16.6583941348077,-15.9622857737505,-14.9646429128911,-13.9670000520317,
-12.9693571911723,-11.9717143303129,-10.9740714694535,-10.3752088276281),
 .UNSPECIFIED.);
#386=B_SPLINE_CURVE_WITH_KNOTS('',3,(#13320,#13321,#13322,#13323,#13324,
#13325,#13326,#13327,#13328,#13329,#13330,#13331,#13332,#13333,#13334,#13335,
#13336,#13337,#13338,#13339,#13340,#13341),.UNSPECIFIED.,.F.,.F.,(4,3,3,
3,3,3,3,4),(7.40592711364074,7.98433824899223,8.98238053011626,9.98042281124028,
10.9784650923643,11.9765073734883,12.9745496546124,13.6891124208203),
 .UNSPECIFIED.);
#387=B_SPLINE_CURVE_WITH_KNOTS('',3,(#13346,#13347,#13348,#13349,#13350,
#13351,#13352,#13353,#13354,#13355,#13356,#13357,#13358,#13359,#13360,#13361,
#13362,#13363,#13364,#13365,#13366,#13367),.UNSPECIFIED.,.F.,.F.,(4,3,3,
3,3,3,3,4),(-22.9415794419873,-21.9481429389069,-20.9505000780475,-19.9528572171881,
-18.9552143563287,-17.9575714954693,-16.9599286346099,-16.6583941348077),
 .UNSPECIFIED.);
#388=B_SPLINE_CURVE_WITH_KNOTS('',3,(#13368,#13369,#13370,#13371,#13372,
#13373,#13374,#13375,#13376,#13377,#13378,#13379,#13380,#13381,#13382,#13383,
#13384,#13385,#13386,#13387,#13388,#13389,#13390,#13391,#13392),
 .UNSPECIFIED.,.F.,.F.,(4,3,3,3,3,3,3,3,4),(13.6891124208203,13.9725919357364,
14.9706342168604,15.9686764979844,16.9667187791085,17.9647610602325,18.9628033413565,
19.9608456224805,19.9722977279999),.UNSPECIFIED.);
#389=B_SPLINE_CURVE_WITH_KNOTS('',3,(#13397,#13398,#13399,#13400,#13401,
#13402,#13403,#13404,#13405,#13406,#13407,#13408,#13409,#13410,#13411,#13412,
#13413,#13414,#13415,#13416,#13417,#13418),.UNSPECIFIED.,.F.,.F.,(4,3,3,
3,3,3,3,4),(-29.2247647491669,-28.9316429649228,-27.9340001040634,-26.936357243204,
-25.9387143823446,-24.9410715214852,-23.9434286606257,-22.9415794419873),
 .UNSPECIFIED.);
#390=B_SPLINE_CURVE_WITH_KNOTS('',3,(#13419,#13420,#13421,#13422,#13423,
#13424,#13425,#13426,#13427,#13428,#13429,#13430,#13431,#13432,#13433,#13434,
#13435,#13436,#13437,#13438,#13439,#13440),.UNSPECIFIED.,.F.,.F.,(4,3,3,
3,3,3,3,4),(19.9722977279999,20.9588879036046,21.9569301847286,22.9549724658526,
23.9530147469767,24.9510570281007,25.9490993092247,26.2554830351795),
 .UNSPECIFIED.);
#391=B_SPLINE_CURVE_WITH_KNOTS('',3,(#13445,#13446,#13447,#13448,#13449,
#13450,#13451,#13452,#13453,#13454,#13455,#13456,#13457,#13458,#13459,#13460,
#13461,#13462,#13463,#13464,#13465,#13466),.UNSPECIFIED.,.F.,.F.,(4,3,3,
3,3,3,3,4),(-35.5079500563465,-34.9175001300792,-33.9198572692198,-32.9222144083604,
-31.924571547501,-30.9269286866416,-29.9292858257822,-29.2247647491669),
 .UNSPECIFIED.);
#392=B_SPLINE_CURVE_WITH_KNOTS('',3,(#13467,#13468,#13469,#13470,#13471,
#13472,#13473,#13474,#13475,#13476,#13477,#13478,#13479,#13480,#13481,#13482,
#13483,#13484,#13485,#13486,#13487,#13488),.UNSPECIFIED.,.F.,.F.,(4,3,3,
3,3,3,3,4),(26.2554830351795,26.9471415903487,27.9451838714728,28.9432261525968,
29.9412684337208,30.9393107148448,31.9373529959689,32.5386683423591),
 .UNSPECIFIED.);
#393=B_SPLINE_CURVE_WITH_KNOTS('',3,(#13493,#13494,#13495,#13496,#13497,
#13498,#13499,#13500,#13501,#13502,#13503,#13504,#13505,#13506,#13507,#13508,
#13509,#13510,#13511,#13512,#13513,#13514),.UNSPECIFIED.,.F.,.F.,(4,3,3,
3,3,3,3,4),(-41.791135363526,-40.9033572952357,-39.9057144343762,-38.9080715735168,
-37.9104287126574,-36.912785851798,-35.9151429909386,-35.5079500563465),
 .UNSPECIFIED.);
#394=B_SPLINE_CURVE_WITH_KNOTS('',3,(#13515,#13516,#13517,#13518,#13519,
#13520,#13521,#13522,#13523,#13524,#13525,#13526,#13527,#13528,#13529,#13530,
#13531,#13532,#13533,#13534,#13535,#13536),.UNSPECIFIED.,.F.,.F.,(4,3,3,
3,3,3,3,4),(32.5386683423591,32.9353952770929,33.9334375582169,34.931479839341,
35.929522120465,36.927564401589,37.9256066827131,38.8218536495387),
 .UNSPECIFIED.);
#395=B_SPLINE_CURVE_WITH_KNOTS('',3,(#13541,#13542,#13543,#13544,#13545,
#13546,#13547,#13548,#13549,#13550,#13551,#13552,#13553,#13554,#13555,#13556,
#13557,#13558,#13559,#13560,#13561,#13562,#13563,#13564,#13565),
 .UNSPECIFIED.,.F.,.F.,(4,3,3,3,3,3,3,3,4),(-48.0743206707056,-47.8868573212515,
-46.8892144603921,-45.8915715995327,-44.8939287386733,-43.8962858778139,
-42.8986430169545,-41.9010001560951,-41.791135363526),.UNSPECIFIED.);
#396=B_SPLINE_CURVE_WITH_KNOTS('',3,(#13566,#13567,#13568,#13569,#13570,
#13571,#13572,#13573,#13574,#13575,#13576,#13577,#13578,#13579,#13580,#13581,
#13582,#13583,#13584,#13585,#13586,#13587,#13588,#13589,#13590),
 .UNSPECIFIED.,.F.,.F.,(4,3,3,3,3,3,3,3,4),(38.8218536495387,38.9236489638371,
39.9216912449611,40.9197335260851,41.9177758072091,42.9158180883332,43.9138603694572,
44.9119026505812,45.1050389567183),.UNSPECIFIED.);
#397=B_SPLINE_CURVE_WITH_KNOTS('',3,(#13595,#13596,#13597,#13598,#13599,
#13600,#13601,#13602,#13603,#13604,#13605,#13606,#13607,#13608,#13609,#13610,
#13611,#13612,#13613,#13614,#13615,#13616),.UNSPECIFIED.,.F.,.F.,(4,3,3,
3,3,3,3,4),(-54.3575059778852,-53.8727144864079,-52.8750716255485,-51.8774287646891,
-50.8797859038297,-49.8821430429703,-48.8845001821109,-48.0743206707056),
 .UNSPECIFIED.);
#398=B_SPLINE_CURVE_WITH_KNOTS('',3,(#13617,#13618,#13619,#13620,#13621,
#13622,#13623,#13624,#13625,#13626,#13627,#13628,#13629,#13630,#13631,#13632,
#13633,#13634,#13635,#13636,#13637,#13638),.UNSPECIFIED.,.F.,.F.,(4,3,3,
3,3,3,3,4),(45.1050389567183,45.9099449317052,46.9079872128293,47.9060294939533,
48.9040717750773,49.9021140562014,50.9001563373254,51.3882242638979),
 .UNSPECIFIED.);
#399=B_SPLINE_CURVE_WITH_KNOTS('',3,(#13643,#13644,#13645,#13646,#13647,
#13648,#13649,#13650,#13651,#13652,#13653,#13654,#13655,#13656,#13657,#13658,
#13659,#13660,#13661,#13662,#13663,#13664),.UNSPECIFIED.,.F.,.F.,(4,3,3,
3,3,3,3,4),(-60.6406912850648,-59.8585716515644,-58.860928790705,-57.8632859298455,
-56.8656430689861,-55.8680002081267,-54.8703573472673,-54.3575059778852),
 .UNSPECIFIED.);
#400=B_SPLINE_CURVE_WITH_KNOTS('',3,(#13665,#13666,#13667,#13668,#13669,
#13670,#13671,#13672,#13673,#13674,#13675,#13676,#13677,#13678,#13679,#13680,
#13681,#13682,#13683,#13684,#13685,#13686),.UNSPECIFIED.,.F.,.F.,(4,3,3,
3,3,3,3,4),(51.3882242638979,51.8981986184494,52.8962408995734,53.8942831806975,
54.8923254618215,55.8903677429455,56.8884100240695,57.6714095710775),
 .UNSPECIFIED.);
#401=B_SPLINE_CURVE_WITH_KNOTS('',3,(#13691,#13692,#13693,#13694,#13695,
#13696,#13697,#13698,#13699,#13700,#13701,#13702,#13703,#13704,#13705,#13706,
#13707,#13708,#13709,#13710,#13711,#13712,#13713,#13714,#13715),
 .UNSPECIFIED.,.F.,.F.,(4,3,3,3,3,3,3,3,4),(-66.9238765922444,-66.8420716775802,
-65.8444288167208,-64.8467859558614,-63.849143095002,-62.8515002341426,
-61.8538573732832,-60.8562145124238,-60.6406912850648),.UNSPECIFIED.);
#402=B_SPLINE_CURVE_WITH_KNOTS('',3,(#13716,#13717,#13718,#13719,#13720,
#13721,#13722,#13723,#13724,#13725,#13726,#13727,#13728,#13729,#13730,#13731,
#13732,#13733,#13734,#13735,#13736,#13737,#13738,#13739,#13740),
 .UNSPECIFIED.,.F.,.F.,(4,3,3,3,3,3,3,3,4),(57.6714095710775,57.8864523051936,
58.8844945863176,59.8825368674416,60.8805791485657,61.8786214296897,62.8766637108137,
63.8747059919378,63.9545948782571),.UNSPECIFIED.);
#403=B_SPLINE_CURVE_WITH_KNOTS('',3,(#13745,#13746,#13747,#13748,#13749,
#13750,#13751,#13752,#13753,#13754,#13755,#13756,#13757,#13758,#13759,#13760,
#13761,#13762,#13763,#13764,#13765,#13766),.UNSPECIFIED.,.F.,.F.,(4,3,3,
3,3,3,3,4),(-73.207061899424,-72.8279288427366,-71.8302859818773,-70.8326431210178,
-69.8350002601584,-68.837357399299,-67.8397145384396,-66.9238765922444),
 .UNSPECIFIED.);
#404=B_SPLINE_CURVE_WITH_KNOTS('',3,(#13767,#13768,#13769,#13770,#13771,
#13772,#13773,#13774,#13775,#13776,#13777,#13778,#13779,#13780,#13781,#13782,
#13783,#13784,#13785,#13786,#13787,#13788),.UNSPECIFIED.,.F.,.F.,(4,3,3,
3,3,3,3,4),(63.9545948782571,64.8727482730618,65.8707905541858,66.8688328353098,
67.8668751164338,68.8649173975579,69.8629596786819,70.2377801854366),
 .UNSPECIFIED.);
#405=B_SPLINE_CURVE_WITH_KNOTS('',3,(#13793,#13794,#13795,#13796,#13797,
#13798,#13799,#13800,#13801,#13802,#13803,#13804,#13805,#13806,#13807,#13808,
#13809,#13810,#13811,#13812,#13813,#13814),.UNSPECIFIED.,.F.,.F.,(4,3,3,
3,3,3,3,4),(-79.4902472066036,-78.8137860078931,-77.8161431470337,-76.8185002861743,
-75.8208574253149,-74.8232145644555,-73.825571703596,-73.207061899424),
 .UNSPECIFIED.);
#406=B_SPLINE_CURVE_WITH_KNOTS('',3,(#13815,#13816,#13817,#13818,#13819,
#13820,#13821,#13822,#13823,#13824,#13825,#13826,#13827,#13828,#13829,#13830,
#13831,#13832,#13833,#13834,#13835,#13836),.UNSPECIFIED.,.F.,.F.,(4,3,3,
3,3,3,3,4),(70.2377801854366,70.8610019598059,71.85904424093,72.857086522054,
73.855128803178,74.853171084302,75.8512133654261,76.5209654926162),
 .UNSPECIFIED.);
#407=B_SPLINE_CURVE_WITH_KNOTS('',3,(#13841,#13842,#13843,#13844,#13845,
#13846,#13847,#13848,#13849,#13850,#13851,#13852,#13853,#13854,#13855,#13856,
#13857,#13858,#13859,#13860,#13861,#13862),.UNSPECIFIED.,.F.,.F.,(4,3,3,
3,3,3,3,4),(-85.7734325137832,-84.7996431730495,-83.8020003121901,-82.8043574513307,
-81.8067145904713,-80.8090717296119,-79.8114288687525,-79.4902472066036),
 .UNSPECIFIED.);
#408=B_SPLINE_CURVE_WITH_KNOTS('',3,(#13863,#13864,#13865,#13866,#13867,
#13868,#13869,#13870,#13871,#13872,#13873,#13874,#13875,#13876,#13877,#13878,
#13879,#13880,#13881,#13882,#13883,#13884),.UNSPECIFIED.,.F.,.F.,(4,3,3,
3,3,3,3,4),(76.5209654926162,76.8492556465501,77.8472979276741,78.8453402087982,
79.8433824899222,80.8414247710462,81.8394670521702,82.8041507997958),
 .UNSPECIFIED.);
#409=B_SPLINE_CURVE_WITH_KNOTS('',3,(#13889,#13890,#13891,#13892,#13893,
#13894,#13895,#13896,#13897,#13898,#13899,#13900,#13901,#13902,#13903,#13904,
#13905,#13906,#13907,#13908,#13909,#13910,#13911,#13912,#13913),
 .UNSPECIFIED.,.F.,.F.,(4,3,3,3,3,3,3,3,4),(-92.0566178209628,-91.7831431990654,
-90.7855003382059,-89.7878574773465,-88.7902146164871,-87.7925717556277,
-86.7949288947683,-85.7972860339089,-85.7734325137832),.UNSPECIFIED.);
#410=B_SPLINE_CURVE_WITH_KNOTS('',3,(#13914,#13915,#13916,#13917,#13918,
#13919,#13920,#13921,#13922,#13923,#13924,#13925,#13926,#13927,#13928,#13929,
#13930,#13931,#13932,#13933,#13934,#13935,#13936,#13937,#13938),
 .UNSPECIFIED.,.F.,.F.,(4,3,3,3,3,3,3,3,4),(82.8041507997958,82.8375093332942,
83.8355516144183,84.8335938955423,85.8316361766664,86.8296784577904,87.8277207389144,
88.8257630200384,89.0873361069754),.UNSPECIFIED.);
#411=B_SPLINE_CURVE_WITH_KNOTS('',3,(#13943,#13944,#13945,#13946,#13947,
#13948,#13949,#13950,#13951,#13952,#13953,#13954,#13955,#13956,#13957,#13958,
#13959,#13960,#13961,#13962,#13963,#13964),.UNSPECIFIED.,.F.,.F.,(4,3,3,
3,3,3,3,4),(-98.3398031281424,-97.7690003642218,-96.7713575033624,-95.773714642503,
-94.7760717816436,-93.7784289207842,-92.7807860599248,-92.0566178209628),
 .UNSPECIFIED.);
#412=B_SPLINE_CURVE_WITH_KNOTS('',3,(#13965,#13966,#13967,#13968,#13969,
#13970,#13971,#13972,#13973,#13974,#13975,#13976,#13977,#13978,#13979,#13980,
#13981,#13982,#13983,#13984,#13985,#13986),.UNSPECIFIED.,.F.,.F.,(4,3,3,
3,3,3,3,4),(89.0873361069754,89.8238053011624,90.8218475822865,91.8198898634105,
92.8179321445345,93.8159744256585,94.8140167067826,95.370521414155),
 .UNSPECIFIED.);
#413=B_SPLINE_CURVE_WITH_KNOTS('',3,(#13991,#13992,#13993,#13994,#13995,
#13996,#13997,#13998,#13999,#14000,#14001,#14002,#14003,#14004,#14005,#14006,
#14007,#14008,#14009,#14010,#14011,#14012),.UNSPECIFIED.,.F.,.F.,(4,3,3,
3,3,3,3,4),(-104.622988435322,-103.754857529378,-102.757214668519,-101.759571807659,
-100.7619289468,-99.7642860859406,-98.7666432250812,-98.3398031281424),
 .UNSPECIFIED.);
#414=B_SPLINE_CURVE_WITH_KNOTS('',3,(#14013,#14014,#14015,#14016,#14017,
#14018,#14019,#14020,#14021,#14022,#14023,#14024,#14025,#14026,#14027,#14028,
#14029,#14030,#14031,#14032,#14033,#14034),.UNSPECIFIED.,.F.,.F.,(4,3,3,
3,3,3,3,4),(95.370521414155,95.8120589879066,96.8101012690306,97.8081435501546,
98.8061858312787,99.8042281124027,100.802270393527,101.653706721335),
 .UNSPECIFIED.);
#415=B_SPLINE_CURVE_WITH_KNOTS('',3,(#14039,#14040,#14041,#14042,#14043,
#14044,#14045,#14046,#14047,#14048,#14049,#14050,#14051,#14052,#14053,#14054,
#14055,#14056,#14057,#14058,#14059,#14060,#14061,#14062,#14063),
 .UNSPECIFIED.,.F.,.F.,(4,3,3,3,3,3,3,3,4),(-110.906173742502,-110.738357555394,
-109.740714694535,-108.743071833675,-107.745428972816,-106.747786111956,
-105.750143251097,-104.752500390238,-104.622988435322),.UNSPECIFIED.);
#416=B_SPLINE_CURVE_WITH_KNOTS('',3,(#14064,#14065,#14066,#14067,#14068,
#14069,#14070,#14071,#14072,#14073,#14074,#14075,#14076,#14077,#14078,#14079,
#14080,#14081,#14082,#14083,#14084,#14085,#14086,#14087,#14088),
 .UNSPECIFIED.,.F.,.F.,(4,3,3,3,3,3,3,3,4),(101.653706721335,101.800312674651,
102.798354955775,103.796397236899,104.794439518023,105.792481799147,106.790524080271,
107.788566361395,107.936892028514),.UNSPECIFIED.);
#417=B_SPLINE_CURVE_WITH_KNOTS('',3,(#14093,#14094,#14095,#14096,#14097,
#14098,#14099,#14100,#14101,#14102,#14103,#14104,#14105,#14106,#14107,#14108,
#14109,#14110,#14111,#14112,#14113,#14114),.UNSPECIFIED.,.F.,.F.,(4,3,3,
3,3,3,3,4),(-117.189359049681,-116.724214720551,-115.726571859691,-114.728928998832,
-113.731286137972,-112.733643277113,-111.736000416253,-110.906173742502),
 .UNSPECIFIED.);
#418=B_SPLINE_CURVE_WITH_KNOTS('',3,(#14115,#14116,#14117,#14118,#14119,
#14120,#14121,#14122,#14123,#14124,#14125,#14126,#14127,#14128,#14129,#14130,
#14131,#14132,#14133,#14134,#14135,#14136),.UNSPECIFIED.,.F.,.F.,(4,3,3,
3,3,3,3,4),(107.936892028514,108.786608642519,109.784650923643,110.782693204767,
111.780735485891,112.778777767015,113.776820048139,114.220077335694),
 .UNSPECIFIED.);
#419=B_SPLINE_CURVE_WITH_KNOTS('',3,(#14141,#14142,#14143,#14144,#14145,
#14146,#14147,#14148,#14149,#14150,#14151,#14152,#14153,#14154,#14155,#14156,
#14157,#14158,#14159,#14160,#14161,#14162),.UNSPECIFIED.,.F.,.F.,(4,3,3,
3,3,3,3,4),(-123.472544356861,-122.710071885707,-121.712429024848,-120.714786163988,
-119.717143303129,-118.719500442269,-117.72185758141,-117.189359049681),
 .UNSPECIFIED.);
#420=B_SPLINE_CURVE_WITH_KNOTS('',3,(#14163,#14164,#14165,#14166,#14167,
#14168,#14169,#14170,#14171,#14172,#14173,#14174,#14175,#14176,#14177,#14178,
#14179,#14180,#14181,#14182,#14183,#14184),.UNSPECIFIED.,.F.,.F.,(4,3,3,
3,3,3,3,4),(114.220077335694,114.774862329263,115.772904610387,116.770946891511,
117.768989172635,118.767031453759,119.765073734883,120.503262642873),
 .UNSPECIFIED.);
#421=B_SPLINE_CURVE_WITH_KNOTS('',3,(#14189,#14190,#14191,#14192,#14193,
#14194,#14195,#14196,#14197,#14198,#14199,#14200,#14201,#14202,#14203,#14204,
#14205,#14206,#14207,#14208,#14209,#14210,#14211,#14212,#14213),
 .UNSPECIFIED.,.F.,.F.,(4,3,3,3,3,3,3,3,4),(-129.75572966404,-129.693571911723,
-128.695929050863,-127.698286190004,-126.700643329145,-125.703000468285,
-124.705357607426,-123.707714746566,-123.472544356861),.UNSPECIFIED.);
#422=B_SPLINE_CURVE_WITH_KNOTS('',3,(#14214,#14215,#14216,#14217,#14218,
#14219,#14220,#14221,#14222,#14223,#14224,#14225,#14226,#14227,#14228,#14229,
#14230,#14231,#14232,#14233,#14234,#14235,#14236,#14237,#14238),
 .UNSPECIFIED.,.F.,.F.,(4,3,3,3,3,3,3,3,4),(120.503262642873,120.763116016007,
121.761158297131,122.759200578255,123.757242859379,124.755285140503,125.753327421627,
126.751369702751,126.786447950053),.UNSPECIFIED.);
#423=B_SPLINE_CURVE_WITH_KNOTS('',3,(#14243,#14244,#14245,#14246,#14247,
#14248,#14249,#14250,#14251,#14252,#14253,#14254,#14255,#14256,#14257,#14258,
#14259,#14260,#14261,#14262,#14263,#14264),.UNSPECIFIED.,.F.,.F.,(4,3,3,
3,3,3,3,4),(-136.03891497122,-135.679429076879,-134.68178621602,-133.68414335516,
-132.686500494301,-131.688857633442,-130.691214772582,-129.75572966404),
 .UNSPECIFIED.);
#424=B_SPLINE_CURVE_WITH_KNOTS('',3,(#14265,#14266,#14267,#14268,#14269,
#14270,#14271,#14272,#14273,#14274,#14275,#14276,#14277,#14278,#14279,#14280,
#14281,#14282,#14283,#14284,#14285,#14286),.UNSPECIFIED.,.F.,.F.,(4,3,3,
3,3,3,3,4),(126.786447950053,127.749411983875,128.747454265,129.745496546124,
130.743538827248,131.741581108372,132.739623389496,133.069633257233),
 .UNSPECIFIED.);
#425=B_SPLINE_CURVE_WITH_KNOTS('',3,(#14291,#14292,#14293,#14294,#14295,
#14296,#14297,#14298,#14299,#14300,#14301,#14302,#14303,#14304,#14305,#14306,
#14307,#14308,#14309,#14310,#14311,#14312),.UNSPECIFIED.,.F.,.F.,(4,3,3,
3,3,3,3,4),(-142.322100278399,-141.665286242036,-140.667643381176,-139.670000520317,
-138.672357659457,-137.674714798598,-136.677071937739,-136.03891497122),
 .UNSPECIFIED.);
#426=B_SPLINE_CURVE_WITH_KNOTS('',3,(#14313,#14314,#14315,#14316,#14317,
#14318,#14319,#14320,#14321,#14322,#14323,#14324,#14325,#14326,#14327,#14328,
#14329,#14330,#14331,#14332,#14333,#14334),.UNSPECIFIED.,.F.,.F.,(4,3,3,
3,3,3,3,4),(133.069633257233,133.73766567062,134.735707951744,135.733750232868,
136.731792513992,137.729834795116,138.72787707624,139.352818564412),
 .UNSPECIFIED.);
#427=B_SPLINE_CURVE_WITH_KNOTS('',3,(#14339,#14340,#14341,#14342,#14343,
#14344,#14345,#14346,#14347,#14348,#14349,#14350,#14351,#14352,#14353,#14354,
#14355,#14356,#14357,#14358,#14359,#14360),.UNSPECIFIED.,.F.,.F.,(4,3,3,
3,3,3,3,4),(-148.605285585579,-147.651143407192,-146.653500546333,-145.655857685473,
-144.658214824614,-143.660571963754,-142.662929102895,-142.322100278399),
 .UNSPECIFIED.);
#428=B_SPLINE_CURVE_WITH_KNOTS('',3,(#14361,#14362,#14363,#14364,#14365,
#14366,#14367,#14368,#14369,#14370,#14371,#14372,#14373,#14374,#14375,#14376,
#14377,#14378,#14379,#14380,#14381,#14382),.UNSPECIFIED.,.F.,.F.,(4,3,3,
3,3,3,3,4),(139.352818564412,139.725919357364,140.723961638488,141.722003919612,
142.720046200736,143.71808848186,144.716130762984,145.636003871592),
 .UNSPECIFIED.);
#429=B_SPLINE_CURVE_WITH_KNOTS('',3,(#14387,#14388,#14389,#14390,#14391,
#14392,#14393,#14394,#14395,#14396,#14397,#14398,#14399,#14400,#14401,#14402,
#14403,#14404,#14405,#14406,#14407,#14408,#14409,#14410,#14411),
 .UNSPECIFIED.,.F.,.F.,(4,3,3,3,3,3,3,3,4),(-154.888470892759,-154.634643433208,
-153.637000572349,-152.639357711489,-151.64171485063,-150.64407198977,-149.646429128911,
-148.648786268052,-148.605285585579),.UNSPECIFIED.);
#430=B_SPLINE_CURVE_WITH_KNOTS('',3,(#14412,#14413,#14414,#14415,#14416,
#14417,#14418,#14419,#14420,#14421,#14422,#14423,#14424,#14425,#14426,#14427,
#14428,#14429,#14430,#14431,#14432,#14433,#14434,#14435,#14436),
 .UNSPECIFIED.,.F.,.F.,(4,3,3,3,3,3,3,3,4),(145.636003871592,145.714173044108,
146.712215325232,147.710257606356,148.70829988748,149.706342168604,150.704384449728,
151.702426730852,151.919189178771),.UNSPECIFIED.);
#431=B_SPLINE_CURVE_WITH_KNOTS('',3,(#14441,#14442,#14443,#14444,#14445,
#14446,#14447,#14448,#14449,#14450,#14451,#14452,#14453,#14454,#14455,#14456,
#14457,#14458,#14459,#14460,#14461,#14462),.UNSPECIFIED.,.F.,.F.,(4,3,3,
3,3,3,3,4),(-161.171656199938,-160.620500598364,-159.622857737505,-158.625214876646,
-157.627572015786,-156.629929154927,-155.632286294067,-154.888470892759),
 .UNSPECIFIED.);
#432=B_SPLINE_CURVE_WITH_KNOTS('',3,(#14463,#14464,#14465,#14466,#14467,
#14468,#14469,#14470,#14471,#14472,#14473,#14474,#14475,#14476,#14477,#14478,
#14479,#14480,#14481,#14482,#14483,#14484),.UNSPECIFIED.,.F.,.F.,(4,3,3,
3,3,3,3,4),(151.919189178771,152.700469011976,153.6985112931,154.696553574224,
155.694595855348,156.692638136472,157.690680417596,158.202374485951),
 .UNSPECIFIED.);
#433=B_SPLINE_CURVE_WITH_KNOTS('',3,(#14489,#14490,#14491,#14492,#14493,
#14494,#14495,#14496,#14497,#14498,#14499,#14500,#14501,#14502,#14503,#14504,
#14505,#14506,#14507,#14508,#14509,#14510),.UNSPECIFIED.,.F.,.F.,(4,3,3,
3,3,3,3,4),(-167.454841507118,-166.606357763521,-165.608714902661,-164.611072041802,
-163.613429180943,-162.615786320083,-161.618143459224,-161.171656199938),
 .UNSPECIFIED.);
#434=B_SPLINE_CURVE_WITH_KNOTS('',3,(#14511,#14512,#14513,#14514,#14515,
#14516,#14517,#14518,#14519,#14520,#14521,#14522,#14523,#14524,#14525,#14526,
#14527,#14528,#14529,#14530,#14531,#14532),.UNSPECIFIED.,.F.,.F.,(4,3,3,
3,3,3,3,4),(158.202374485951,158.68872269872,159.686764979844,160.684807260968,
161.682849542092,162.680891823216,163.67893410434,164.48555979313),
 .UNSPECIFIED.);
#435=B_SPLINE_CURVE_WITH_KNOTS('',3,(#14537,#14538,#14539,#14540,#14541,
#14542,#14543,#14544,#14545,#14546,#14547,#14548,#14549,#14550,#14551,#14552,
#14553,#14554,#14555,#14556,#14557,#14558,#14559,#14560,#14561),
 .UNSPECIFIED.,.F.,.F.,(4,3,3,3,3,3,3,3,4),(-173.738026814297,-173.589857789537,
-172.592214928677,-171.594572067818,-170.596929206958,-169.599286346099,
-168.60164348524,-167.60400062438,-167.454841507118),.UNSPECIFIED.);
#436=B_SPLINE_CURVE_WITH_KNOTS('',3,(#14562,#14563,#14564,#14565,#14566,
#14567,#14568,#14569,#14570,#14571,#14572,#14573,#14574,#14575,#14576,#14577,
#14578,#14579,#14580,#14581,#14582,#14583,#14584,#14585,#14586),
 .UNSPECIFIED.,.F.,.F.,(4,3,3,3,3,3,3,3,4),(164.48555979313,164.676976385465,
165.675018666588,166.673060947713,167.671103228837,168.669145509961,169.667187791085,
170.665230072209,170.76874510031),.UNSPECIFIED.);
#437=B_SPLINE_CURVE_WITH_KNOTS('',3,(#14591,#14592,#14593,#14594,#14595,
#14596,#14597,#14598,#14599,#14600,#14601,#14602,#14603,#14604,#14605,#14606,
#14607,#14608,#14609,#14610,#14611,#14612),.UNSPECIFIED.,.F.,.F.,(4,3,3,
3,3,3,3,4),(-180.021212121477,-179.575714954693,-178.578072093834,-177.580429232974,
-176.582786372115,-175.585143511255,-174.587500650396,-173.738026814297),
 .UNSPECIFIED.);
#438=B_SPLINE_CURVE_WITH_KNOTS('',3,(#14613,#14614,#14615,#14616,#14617,
#14618,#14619,#14620,#14621,#14622,#14623,#14624,#14625,#14626,#14627,#14628,
#14629,#14630,#14631,#14632,#14633,#14634),.UNSPECIFIED.,.F.,.F.,(4,3,3,
3,3,3,3,4),(170.76874510031,171.663272353333,172.661314634457,173.659356915581,
174.657399196705,175.655441477829,176.653483758953,177.051930407489),
 .UNSPECIFIED.);
#439=B_SPLINE_CURVE_WITH_KNOTS('',3,(#14639,#14640,#14641,#14642,#14643,
#14644,#14645,#14646,#14647,#14648,#14649,#14650,#14651,#14652,#14653,#14654,
#14655,#14656,#14657,#14658,#14659,#14660),.UNSPECIFIED.,.F.,.F.,(4,3,3,
3,3,3,3,4),(-186.304397428656,-185.56157211985,-184.56392925899,-183.566286398131,
-182.568643537271,-181.571000676412,-180.573357815553,-180.021212121477),
 .UNSPECIFIED.);
#440=B_SPLINE_CURVE_WITH_KNOTS('',3,(#14661,#14662,#14663,#14664,#14665,
#14666,#14667,#14668,#14669,#14670,#14671,#14672,#14673,#14674,#14675,#14676,
#14677,#14678,#14679,#14680,#14681,#14682),.UNSPECIFIED.,.F.,.F.,(4,3,3,
3,3,3,3,4),(177.051930407489,177.651526040077,178.649568321201,179.647610602325,
180.645652883449,181.643695164573,182.641737445697,183.335115714669),
 .UNSPECIFIED.);
#441=B_SPLINE_CURVE_WITH_KNOTS('',3,(#14688,#14689,#14690,#14691,#14692,
#14693,#14694,#14695,#14696,#14697),.UNSPECIFIED.,.F.,.F.,(4,1,1,1,1,1,
1,4),(197.920337176157,198.17515472821,199.172797589069,200.170440449928,
201.168083310788,202.165726171647,203.163369032507,204.161011893366),
 .UNSPECIFIED.);
#442=B_SPLINE_CURVE_WITH_KNOTS('',3,(#14700,#14701,#14702,#14703,#14704,
#14705,#14706,#14707,#14708),.UNSPECIFIED.,.F.,.F.,(4,1,1,1,1,1,4),(197.920337176157,
197.930069567874,198.928111848998,199.926154130122,200.924196411246,201.92223869237,
202.920280973494),.UNSPECIFIED.);
#443=B_SPLINE_CURVE_WITH_KNOTS('',3,(#14713,#14714,#14715,#14716,#14717,
#14718,#14719,#14720,#14721,#14722),.UNSPECIFIED.,.F.,.F.,(4,1,1,1,1,1,
1,4),(191.637151868977,192.189297563053,193.186940423913,194.184583284772,
195.182226145631,196.179869006491,197.17751186735,197.920337176157),
 .UNSPECIFIED.);
#444=B_SPLINE_CURVE_WITH_KNOTS('',3,(#14723,#14724,#14725,#14726,#14727,
#14728,#14729,#14730,#14731,#14732),.UNSPECIFIED.,.F.,.F.,(4,1,1,1,1,1,
1,4),(191.637151868977,191.94181588113,192.939858162254,193.937900443378,
194.935942724502,195.933985005626,196.93202728675,197.920337176157),
 .UNSPECIFIED.);
#445=B_SPLINE_CURVE_WITH_KNOTS('',3,(#14737,#14738,#14739,#14740,#14741,
#14742,#14743,#14744,#14745,#14746),.UNSPECIFIED.,.F.,.F.,(4,1,1,1,1,1,
1,4),(185.353966561798,186.203440397897,187.201083258756,188.198726119616,
189.196368980475,190.194011841334,191.191654702194,191.637151868977),
 .UNSPECIFIED.);
#446=B_SPLINE_CURVE_WITH_KNOTS('',3,(#14747,#14748,#14749,#14750,#14751,
#14752,#14753,#14754,#14755,#14756),.UNSPECIFIED.,.F.,.F.,(4,1,1,1,1,1,
1,4),(185.353966561798,185.953562194385,186.951604475509,187.949646756633,
188.947689037757,189.945731318881,190.943773600006,191.637151868977),
 .UNSPECIFIED.);
#447=B_SPLINE_CURVE_WITH_KNOTS('',3,(#14761,#14762,#14763,#14764,#14765,
#14766,#14767,#14768,#14769,#14770,#14771),.UNSPECIFIED.,.F.,.F.,(4,1,1,
1,1,1,1,1,4),(179.070781254618,179.219940371881,180.21758323274,181.2152260936,
182.212868954459,183.210511815318,184.208154676178,185.205797537037,185.353966561798),
 .UNSPECIFIED.);
#448=B_SPLINE_CURVE_WITH_KNOTS('',3,(#14772,#14773,#14774,#14775,#14776,
#14777,#14778,#14779,#14780,#14781),.UNSPECIFIED.,.F.,.F.,(4,1,1,1,1,1,
1,4),(179.070781254618,179.965308507641,180.963350788765,181.961393069889,
182.959435351013,183.957477632137,184.955519913261,185.353966561798),
 .UNSPECIFIED.);
#449=B_SPLINE_CURVE_WITH_KNOTS('',3,(#14786,#14787,#14788,#14789,#14790,
#14791,#14792,#14793,#14794,#14795),.UNSPECIFIED.,.F.,.F.,(4,1,1,1,1,1,
1,4),(172.787595947439,173.234083206724,174.231726067584,175.229368928443,
176.227011789303,177.224654650162,178.222297511021,179.070781254618),
 .UNSPECIFIED.);
#450=B_SPLINE_CURVE_WITH_KNOTS('',3,(#14796,#14797,#14798,#14799,#14800,
#14801,#14802,#14803,#14804,#14805,#14806),.UNSPECIFIED.,.F.,.F.,(4,1,1,
1,1,1,1,1,4),(172.787595947439,172.979012539773,173.977054820897,174.975097102021,
175.973139383145,176.971181664269,177.969223945393,178.967266226517,179.070781254618),
 .UNSPECIFIED.);
#451=B_SPLINE_CURVE_WITH_KNOTS('',3,(#14811,#14812,#14813,#14814,#14815,
#14816,#14817,#14818,#14819,#14820),.UNSPECIFIED.,.F.,.F.,(4,1,1,1,1,1,
1,4),(166.504410640259,167.248226041568,168.245868902427,169.243511763287,
170.241154624146,171.238797485006,172.236440345865,172.787595947439),
 .UNSPECIFIED.);
#452=B_SPLINE_CURVE_WITH_KNOTS('',3,(#14821,#14822,#14823,#14824,#14825,
#14826,#14827,#14828,#14829,#14830),.UNSPECIFIED.,.F.,.F.,(4,1,1,1,1,1,
1,4),(166.504410640259,166.990758853029,167.988801134153,168.986843415277,
169.984885696401,170.982927977525,171.980970258649,172.787595947439),
 .UNSPECIFIED.);
#453=B_SPLINE_CURVE_WITH_KNOTS('',3,(#14835,#14836,#14837,#14838,#14839,
#14840,#14841,#14842,#14843,#14844,#14845),.UNSPECIFIED.,.F.,.F.,(4,1,1,
1,1,1,1,1,4),(160.22122533308,160.264726015552,161.262368876412,162.260011737271,
163.25765459813,164.25529745899,165.252940319849,166.250583180709,166.504410640259),
 .UNSPECIFIED.);
#454=B_SPLINE_CURVE_WITH_KNOTS('',3,(#14846,#14847,#14848,#14849,#14850,
#14851,#14852,#14853,#14854,#14855),.UNSPECIFIED.,.F.,.F.,(4,1,1,1,1,1,
1,4),(160.22122533308,161.002505166285,162.000547447409,162.998589728533,
163.996632009657,164.994674290781,165.992716571905,166.504410640259),
 .UNSPECIFIED.);
#455=B_SPLINE_CURVE_WITH_KNOTS('',3,(#14860,#14861,#14862,#14863,#14864,
#14865,#14866,#14867,#14868,#14869),.UNSPECIFIED.,.F.,.F.,(4,1,1,1,1,1,
1,4),(153.9380400259,154.278868850396,155.276511711255,156.274154572115,
157.271797432974,158.269440293833,159.267083154693,160.22122533308),
 .UNSPECIFIED.);
#456=B_SPLINE_CURVE_WITH_KNOTS('',3,(#14870,#14871,#14872,#14873,#14874,
#14875,#14876,#14877,#14878,#14879,#14880),.UNSPECIFIED.,.F.,.F.,(4,1,1,
1,1,1,1,1,4),(153.9380400259,154.016209198417,155.014251479541,156.012293760665,
157.010336041789,158.008378322913,159.006420604037,160.004462885161,160.22122533308),
 .UNSPECIFIED.);
#457=B_SPLINE_CURVE_WITH_KNOTS('',3,(#14885,#14886,#14887,#14888,#14889,
#14890,#14891,#14892,#14893,#14894),.UNSPECIFIED.,.F.,.F.,(4,1,1,1,1,1,
1,4),(147.65485471872,148.293011685239,149.290654546099,150.288297406958,
151.285940267817,152.283583128677,153.281225989536,153.9380400259),
 .UNSPECIFIED.);
#458=B_SPLINE_CURVE_WITH_KNOTS('',3,(#14895,#14896,#14897,#14898,#14899,
#14900,#14901,#14902,#14903,#14904),.UNSPECIFIED.,.F.,.F.,(4,1,1,1,1,1,
1,4),(147.65485471872,148.027955511672,149.025997792796,150.02404007392,
151.022082355044,152.020124636168,153.018166917292,153.9380400259),
 .UNSPECIFIED.);
#459=B_SPLINE_CURVE_WITH_KNOTS('',3,(#14909,#14910,#14911,#14912,#14913,
#14914,#14915,#14916,#14917,#14918),.UNSPECIFIED.,.F.,.F.,(4,1,1,1,1,1,
1,4),(141.371669411541,142.307154520083,143.304797380942,144.302440241802,
145.300083102661,146.29772596352,147.29536882438,147.65485471872),
 .UNSPECIFIED.);
#460=B_SPLINE_CURVE_WITH_KNOTS('',3,(#14919,#14920,#14921,#14922,#14923,
#14924,#14925,#14926,#14927,#14928),.UNSPECIFIED.,.F.,.F.,(4,1,1,1,1,1,
1,4),(141.371669411541,142.039701824928,143.037744106052,144.035786387176,
145.0338286683,146.031870949424,147.029913230548,147.65485471872),
 .UNSPECIFIED.);
#461=B_SPLINE_CURVE_WITH_KNOTS('',3,(#14933,#14934,#14935,#14936,#14937,
#14938,#14939,#14940,#14941,#14942,#14943),.UNSPECIFIED.,.F.,.F.,(4,1,1,
1,1,1,1,1,4),(135.088484104361,135.323654494067,136.321297354926,137.318940215786,
138.316583076645,139.314225937505,140.311868798364,141.309511659223,141.371669411541),
 .UNSPECIFIED.);
#462=B_SPLINE_CURVE_WITH_KNOTS('',3,(#14944,#14945,#14946,#14947,#14948,
#14949,#14950,#14951,#14952,#14953),.UNSPECIFIED.,.F.,.F.,(4,1,1,1,1,1,
1,4),(135.088484104361,136.051448138184,137.049490419308,138.047532700432,
139.045574981556,140.04361726268,141.041659543804,141.371669411541),
 .UNSPECIFIED.);
#463=B_SPLINE_CURVE_WITH_KNOTS('',3,(#14958,#14959,#14960,#14961,#14962,
#14963,#14964,#14965,#14966,#14967),.UNSPECIFIED.,.F.,.F.,(4,1,1,1,1,1,
1,4),(128.805298797182,129.337797328911,130.33544018977,131.333083050629,
132.330725911489,133.328368772348,134.326011633208,135.088484104361),
 .UNSPECIFIED.);
#464=B_SPLINE_CURVE_WITH_KNOTS('',3,(#14968,#14969,#14970,#14971,#14972,
#14973,#14974,#14975,#14976,#14977,#14978),.UNSPECIFIED.,.F.,.F.,(4,1,1,
1,1,1,1,1,4),(128.805298797182,129.065152170316,130.06319445144,131.061236732564,
132.059279013688,133.057321294812,134.055363575936,135.05340585706,135.088484104361),
 .UNSPECIFIED.);
#465=B_SPLINE_CURVE_WITH_KNOTS('',3,(#14983,#14984,#14985,#14986,#14987,
#14988,#14989,#14990,#14991,#14992),.UNSPECIFIED.,.F.,.F.,(4,1,1,1,1,1,
1,4),(122.522113490002,123.351940163754,124.349583024614,125.347225885473,
126.344868746332,127.342511607192,128.340154468051,128.805298797182),
 .UNSPECIFIED.);
#466=B_SPLINE_CURVE_WITH_KNOTS('',3,(#14993,#14994,#14995,#14996,#14997,
#14998,#14999,#15000,#15001,#15002),.UNSPECIFIED.,.F.,.F.,(4,1,1,1,1,1,
1,4),(122.522113490002,123.076898483572,124.074940764696,125.07298304582,
126.071025326944,127.069067608068,128.067109889192,128.805298797182),
 .UNSPECIFIED.);
#467=B_SPLINE_CURVE_WITH_KNOTS('',3,(#15007,#15008,#15009,#15010,#15011,
#15012,#15013,#15014,#15015,#15016,#15017),.UNSPECIFIED.,.F.,.F.,(4,1,1,
1,1,1,1,1,4),(116.238928182823,116.368440137738,117.366082998598,118.363725859457,
119.361368720316,120.359011581176,121.356654442035,122.354297302895,122.522113490002),
 .UNSPECIFIED.);
#468=B_SPLINE_CURVE_WITH_KNOTS('',3,(#15018,#15019,#15020,#15021,#15022,
#15023,#15024,#15025,#15026,#15027),.UNSPECIFIED.,.F.,.F.,(4,1,1,1,1,1,
1,4),(116.238928182823,117.088644796828,118.086687077952,119.084729359076,
120.0827716402,121.080813921324,122.078856202448,122.522113490002),
 .UNSPECIFIED.);
#469=B_SPLINE_CURVE_WITH_KNOTS('',3,(#15032,#15033,#15034,#15035,#15036,
#15037,#15038,#15039,#15040,#15041),.UNSPECIFIED.,.F.,.F.,(4,1,1,1,1,1,
1,4),(109.955742875643,110.382582972582,111.380225833441,112.377868694301,
113.37551155516,114.373154416019,115.370797276879,116.238928182823),
 .UNSPECIFIED.);
#470=B_SPLINE_CURVE_WITH_KNOTS('',3,(#15042,#15043,#15044,#15045,#15046,
#15047,#15048,#15049,#15050,#15051,#15052),.UNSPECIFIED.,.F.,.F.,(4,1,1,
1,1,1,1,1,4),(109.955742875643,110.102348828959,111.100391110083,112.098433391207,
113.096475672331,114.094517953455,115.092560234579,116.090602515703,116.238928182823),
 .UNSPECIFIED.);
#471=B_SPLINE_CURVE_WITH_KNOTS('',3,(#15057,#15058,#15059,#15060,#15061,
#15062,#15063,#15064,#15065,#15066),.UNSPECIFIED.,.F.,.F.,(4,1,1,1,1,1,
1,4),(103.672557568463,104.396725807425,105.394368668285,106.392011529144,
107.389654390004,108.387297250863,109.384940111722,109.955742875643),
 .UNSPECIFIED.);
#472=B_SPLINE_CURVE_WITH_KNOTS('',3,(#15067,#15068,#15069,#15070,#15071,
#15072,#15073,#15074,#15075,#15076),.UNSPECIFIED.,.F.,.F.,(4,1,1,1,1,1,
1,4),(103.672557568463,104.114095142215,105.112137423339,106.110179704463,
107.108221985587,108.106264266711,109.104306547835,109.955742875643),
 .UNSPECIFIED.);
#473=B_SPLINE_CURVE_WITH_KNOTS('',3,(#15081,#15082,#15083,#15084,#15085,
#15086,#15087,#15088,#15089,#15090,#15091),.UNSPECIFIED.,.F.,.F.,(4,1,1,
1,1,1,1,1,4),(97.3893722612837,97.4132257814096,98.410868642269,99.4085115031284,
100.406154363988,101.403797224847,102.401440085707,103.399082946566,103.672557568463),
 .UNSPECIFIED.);
#474=B_SPLINE_CURVE_WITH_KNOTS('',3,(#15092,#15093,#15094,#15095,#15096,
#15097,#15098,#15099,#15100,#15101),.UNSPECIFIED.,.F.,.F.,(4,1,1,1,1,1,
1,4),(97.3893722612838,98.125841455471,99.123883736595,100.121926017719,
101.119968298843,102.118010579967,103.116052861091,103.672557568463),
 .UNSPECIFIED.);
#475=B_SPLINE_CURVE_WITH_KNOTS('',3,(#15106,#15107,#15108,#15109,#15110,
#15111,#15112,#15113,#15114,#15115),.UNSPECIFIED.,.F.,.F.,(4,1,1,1,1,1,
1,4),(91.1061869541041,91.4273686162531,92.4250114771125,93.4226543379719,
94.4202971988313,95.4179400596907,96.4155829205502,97.3893722612837),
 .UNSPECIFIED.);
#476=B_SPLINE_CURVE_WITH_KNOTS('',3,(#15116,#15117,#15118,#15119,#15120,
#15121,#15122,#15123,#15124,#15125,#15126),.UNSPECIFIED.,.F.,.F.,(4,1,1,
1,1,1,1,1,4),(91.1061869541042,91.1395454876028,92.1375877687268,93.1356300498508,
94.1336723309749,95.1317146120989,96.1297568932229,97.127799174347,97.3893722612838),
 .UNSPECIFIED.);
#477=B_SPLINE_CURVE_WITH_KNOTS('',3,(#15131,#15132,#15133,#15134,#15135,
#15136,#15137,#15138,#15139,#15140),.UNSPECIFIED.,.F.,.F.,(4,1,1,1,1,1,
1,4),(84.8230016469245,85.4415114510967,86.4391543119561,87.4367971728155,
88.4344400336749,89.4320828945343,90.4297257553937,91.1061869541041),
 .UNSPECIFIED.);
#478=B_SPLINE_CURVE_WITH_KNOTS('',3,(#15141,#15142,#15143,#15144,#15145,
#15146,#15147,#15148,#15149,#15150),.UNSPECIFIED.,.F.,.F.,(4,1,1,1,1,1,
1,4),(84.8230016469246,85.1512918008586,86.1493340819827,87.1473763631067,
88.1454186442307,89.1434609253548,90.1415032064788,91.1061869541042),
 .UNSPECIFIED.);
#479=B_SPLINE_CURVE_WITH_KNOTS('',3,(#15155,#15156,#15157,#15158,#15159,
#15160,#15161,#15162,#15163,#15164),.UNSPECIFIED.,.F.,.F.,(4,1,1,1,1,1,
1,4),(78.539816339745,79.4556542859402,80.4532971467996,81.4509400076591,
82.4485828685185,83.4462257293779,84.4438685902373,84.8230016469245),
 .UNSPECIFIED.);
#480=B_SPLINE_CURVE_WITH_KNOTS('',3,(#15165,#15166,#15167,#15168,#15169,
#15170,#15171,#15172,#15173,#15174),.UNSPECIFIED.,.F.,.F.,(4,1,1,1,1,1,
1,4),(78.539816339745,79.1630381141145,80.1610803952385,81.1591226763625,
82.1571649574865,83.1552072386106,84.1532495197346,84.8230016469246),
 .UNSPECIFIED.);
#481=B_SPLINE_CURVE_WITH_KNOTS('',3,(#15179,#15180,#15181,#15182,#15183,
#15184,#15185,#15186,#15187,#15188,#15189),.UNSPECIFIED.,.F.,.F.,(4,1,1,
1,1,1,1,1,4),(72.2566310325654,72.4721542599244,73.4697971207838,74.4674399816432,
75.4650828425026,76.462725703362,77.4603685642214,78.4580114250808,78.539816339745),
 .UNSPECIFIED.);
#482=B_SPLINE_CURVE_WITH_KNOTS('',3,(#15190,#15191,#15192,#15193,#15194,
#15195,#15196,#15197,#15198,#15199),.UNSPECIFIED.,.F.,.F.,(4,1,1,1,1,1,
1,4),(72.2566310325654,73.1747844273703,74.1728267084943,75.1708689896184,
76.1689112707424,77.1669535518664,78.1649958329905,78.539816339745),
 .UNSPECIFIED.);
#483=B_SPLINE_CURVE_WITH_KNOTS('',3,(#15204,#15205,#15206,#15207,#15208,
#15209,#15210,#15211,#15212,#15213),.UNSPECIFIED.,.F.,.F.,(4,1,1,1,1,1,
1,4),(65.9734457253858,66.486297094768,67.4839399556274,68.4815828164868,
69.4792256773462,70.4768685382056,71.474511399065,72.2566310325654),
 .UNSPECIFIED.);
#484=B_SPLINE_CURVE_WITH_KNOTS('',3,(#15214,#15215,#15216,#15217,#15218,
#15219,#15220,#15221,#15222,#15223,#15224),.UNSPECIFIED.,.F.,.F.,(4,1,1,
1,1,1,1,1,4),(65.9734457253858,66.1884884595021,67.1865307406262,68.1845730217502,
69.1826153028742,70.1806575839982,71.1786998651223,72.1767421462463,72.2566310325654),
 .UNSPECIFIED.);
#485=B_SPLINE_CURVE_WITH_KNOTS('',3,(#15229,#15230,#15231,#15232,#15233,
#15234,#15235,#15236,#15237,#15238),.UNSPECIFIED.,.F.,.F.,(4,1,1,1,1,1,
1,4),(59.6902604182062,60.5004399296115,61.4980827904709,62.4957256513303,
63.4933685121897,64.4910113730492,65.4886542339086,65.9734457253858),
 .UNSPECIFIED.);
#486=B_SPLINE_CURVE_WITH_KNOTS('',3,(#15239,#15240,#15241,#15242,#15243,
#15244,#15245,#15246,#15247,#15248),.UNSPECIFIED.,.F.,.F.,(4,1,1,1,1,1,
1,4),(59.6902604182062,60.200234772758,61.198277053882,62.196319335006,
63.19436161613,64.1924038972541,65.1904461783781,65.9734457253858),
 .UNSPECIFIED.);
#487=B_SPLINE_CURVE_WITH_KNOTS('',3,(#15253,#15254,#15255,#15256,#15257,
#15258,#15259,#15260,#15261,#15262,#15263),.UNSPECIFIED.,.F.,.F.,(4,1,1,
1,1,1,1,1,4),(53.4070751110266,53.5169399035957,54.5145827644551,55.5122256253145,
56.5098684861739,57.5075113470333,58.5051542078927,59.5027970687521,59.6902604182062),
 .UNSPECIFIED.);
#488=B_SPLINE_CURVE_WITH_KNOTS('',3,(#15264,#15265,#15266,#15267,#15268,
#15269,#15270,#15271,#15272,#15273),.UNSPECIFIED.,.F.,.F.,(4,1,1,1,1,1,
1,4),(53.4070751110266,54.2119810860138,55.2100233671378,56.2080656482619,
57.2061079293859,58.2041502105099,59.2021924916339,59.6902604182062),
 .UNSPECIFIED.);
#489=B_SPLINE_CURVE_WITH_KNOTS('',3,(#15278,#15279,#15280,#15281,#15282,
#15283,#15284,#15285,#15286,#15287),.UNSPECIFIED.,.F.,.F.,(4,1,1,1,1,1,
1,4),(47.123889803847,47.5310827384393,48.5287255992987,49.5263684601581,
50.5240113210175,51.5216541818769,52.5192970427363,53.4070751110266),
 .UNSPECIFIED.);
#490=B_SPLINE_CURVE_WITH_KNOTS('',3,(#15288,#15289,#15290,#15291,#15292,
#15293,#15294,#15295,#15296,#15297,#15298),.UNSPECIFIED.,.F.,.F.,(4,1,1,
1,1,1,1,1,4),(47.123889803847,47.2256851181456,48.2237273992696,49.2217696803937,
50.2198119615177,51.2178542426417,52.2158965237657,53.2139388048898,53.4070751110266),
 .UNSPECIFIED.);
#491=B_SPLINE_CURVE_WITH_KNOTS('',3,(#15303,#15304,#15305,#15306,#15307,
#15308,#15309,#15310,#15311,#15312),.UNSPECIFIED.,.F.,.F.,(4,1,1,1,1,1,
1,4),(40.8407044966674,41.5452255732828,42.5428684341422,43.5405112950016,
44.538154155861,45.5357970167204,46.5334398775799,47.123889803847),
 .UNSPECIFIED.);
#492=B_SPLINE_CURVE_WITH_KNOTS('',3,(#15313,#15314,#15315,#15316,#15317,
#15318,#15319,#15320,#15321,#15322),.UNSPECIFIED.,.F.,.F.,(4,1,1,1,1,1,
1,4),(40.8407044966675,41.2374314314014,42.2354737125255,43.2335159936495,
44.2315582747735,45.2296005558975,46.2276428370216,47.123889803847),
 .UNSPECIFIED.);
#493=B_SPLINE_CURVE_WITH_KNOTS('',3,(#15327,#15328,#15329,#15330,#15331,
#15332,#15333,#15334,#15335,#15336,#15337),.UNSPECIFIED.,.F.,.F.,(4,1,1,
1,1,1,1,1,4),(34.5575191894878,34.561725547267,35.5593684081264,36.5570112689858,
37.5546541298452,38.5522969907046,39.549939851564,40.5475827124234,40.8407044966674),
 .UNSPECIFIED.);
#494=B_SPLINE_CURVE_WITH_KNOTS('',3,(#15338,#15339,#15340,#15341,#15342,
#15343,#15344,#15345,#15346,#15347),.UNSPECIFIED.,.F.,.F.,(4,1,1,1,1,1,
1,4),(34.5575191894879,35.2491777446573,36.2472200257813,37.2452623069053,
38.2433045880294,39.2413468691534,40.2393891502774,40.8407044966675),
 .UNSPECIFIED.);
#495=B_SPLINE_CURVE_WITH_KNOTS('',3,(#15352,#15353,#15354,#15355,#15356,
#15357,#15358,#15359,#15360,#15361),.UNSPECIFIED.,.F.,.F.,(4,1,1,1,1,1,
1,4),(28.2743338823082,28.5758683821105,29.5735112429699,30.5711541038294,
31.5687969646888,32.5664398255482,33.5640826864076,34.5575191894878),
 .UNSPECIFIED.);
#496=B_SPLINE_CURVE_WITH_KNOTS('',3,(#15362,#15363,#15364,#15365,#15366,
#15367,#15368,#15369,#15370,#15371),.UNSPECIFIED.,.F.,.F.,(4,1,1,1,1,1,
1,4),(28.2743338823083,29.2609240579131,30.2589663390371,31.2570086201612,
32.2550509012852,33.2530931824092,34.2511354635333,34.5575191894879),
 .UNSPECIFIED.);
#497=B_SPLINE_CURVE_WITH_KNOTS('',3,(#15376,#15377,#15378,#15379,#15380,
#15381,#15382,#15383,#15384,#15385),.UNSPECIFIED.,.F.,.F.,(4,1,1,1,1,1,
1,4),(21.9911485751286,22.5900112169541,23.5876540778135,24.5852969386729,
25.5829397995323,26.5805826603917,27.5782255212511,28.2743338823082),
 .UNSPECIFIED.);
#498=B_SPLINE_CURVE_WITH_KNOTS('',3,(#15386,#15387,#15388,#15389,#15390,
#15391,#15392,#15393,#15394,#15395,#15396),.UNSPECIFIED.,.F.,.F.,(4,1,1,
1,1,1,1,1,4),(21.9911485751287,22.2746280900449,23.272670371169,24.270712652293,
25.268754933417,26.266797214541,27.2648394956651,28.2628817767891,28.2743338823083),
 .UNSPECIFIED.);
#499=B_SPLINE_CURVE_WITH_KNOTS('',3,(#15401,#15402,#15403,#15404,#15405,
#15406,#15407,#15408,#15409,#15410),.UNSPECIFIED.,.F.,.F.,(4,1,1,1,1,1,
1,4),(15.707963267949,16.6041540517977,17.6017969126571,18.5994397735165,
19.5970826343759,20.5947254952353,21.5923683560947,21.9911485751286),
 .UNSPECIFIED.);
#500=B_SPLINE_CURVE_WITH_KNOTS('',3,(#15411,#15412,#15413,#15414,#15415,
#15416,#15417,#15418,#15419,#15420),.UNSPECIFIED.,.F.,.F.,(4,1,1,1,1,1,
1,4),(15.7079632679491,16.2863744033008,17.2844166844248,18.2824589655488,
19.2805012466728,20.2785435277969,21.2765858089209,21.9911485751287),
 .UNSPECIFIED.);
#501=B_SPLINE_CURVE_WITH_KNOTS('',3,(#15423,#15424,#15425,#15426,#15427,
#15428,#15429,#15430,#15431,#15432,#15433,#15434,#15435,#15436,#15437,#15438,
#15439,#15440,#15441,#15442,#15443,#15444,#15445,#15446,#15447,#15448,#15449,
#15450,#15451,#15452,#15453,#15454,#15455,#15456,#15457,#15458,#15459,#15460,
#15461,#15462,#15463,#15464,#15465,#15466,#15467,#15468,#15469,#15470,#15471,
#15472,#15473,#15474,#15475,#15476,#15477,#15478,#15479,#15480,#15481,#15482,
#15483,#15484,#15485,#15486,#15487,#15488,#15489,#15490,#15491,#15492,#15493,
#15494,#15495,#15496,#15497,#15498,#15499,#15500,#15501,#15502,#15503,#15504,
#15505,#15506,#15507,#15508,#15509,#15510,#15511,#15512,#15513,#15514,#15515,
#15516,#15517,#15518,#15519,#15520,#15521,#15522,#15523,#15524,#15525,#15526,
#15527,#15528,#15529,#15530,#15531,#15532,#15533,#15534,#15535,#15536,#15537,
#15538,#15539,#15540,#15541,#15542,#15543),.UNSPECIFIED.,.F.,.F.,(4,3,3,
3,3,3,3,3,3,3,3,3,3,3,3,3,3,3,3,3,3,3,3,3,3,3,3,3,3,3,3,3,3,3,3,3,3,3,3,
3,4),(-0.753008129282056,-0.726412283548368,-0.715911613874471,-0.694893371653716,
-0.683361029549332,-0.673826434412814,-0.652889016486892,-0.639679181765185,
-0.63195159856097,-0.60480408471638,-0.59150990338668,-0.582561183693184,
-0.554067746128576,-0.540494882749548,-0.528208608719221,-0.505843484121927,
-0.4921308028701,-0.483102814228457,-0.456032674248847,-0.436199115577779,
-0.427073928162626,-0.400948091236321,-0.382860905241332,-0.374822254310016,
-0.34584221065474,-0.333939649620793,-0.324058619604945,-0.29393738163796,
-0.278576588250954,-0.269234263278142,-0.238815915606663,-0.225742435796944,
-0.216239773488962,-0.18666367230127,-0.170750005528772,-0.161294486761502,
-0.129614927749849,-0.114924930935507,-0.106250072717365,-0.0979353687381955,
-0.0965360155478562),.UNSPECIFIED.);
#502=B_SPLINE_CURVE_WITH_KNOTS('',3,(#15545,#15546,#15547,#15548,#15549,
#15550,#15551,#15552,#15553,#15554,#15555,#15556,#15557,#15558,#15559,#15560,
#15561,#15562,#15563,#15564,#15565,#15566,#15567,#15568,#15569,#15570,#15571,
#15572,#15573,#15574,#15575,#15576,#15577,#15578,#15579,#15580,#15581),
 .UNSPECIFIED.,.F.,.F.,(4,3,3,3,3,3,3,3,3,3,3,3,4),(-0.204609524178132,
-0.173922074105667,-0.152149392827302,-0.142793959810126,-0.12983323009626,
-0.11308637627832,-0.0998536142809363,-0.090547498816978,-0.0679106241127335,
-0.0514558350659385,-0.042025593252969,-0.0155529233063705,0.),
 .UNSPECIFIED.);
#503=B_SPLINE_CURVE_WITH_KNOTS('',3,(#15584,#15585,#15586,#15587,#15588,
#15589,#15590,#15591,#15592,#15593,#15594,#15595,#15596,#15597,#15598,#15599),
 .UNSPECIFIED.,.F.,.F.,(4,3,3,3,3,4),(-0.0965360155478562,-0.0724020116608921,
-0.0590232605257019,-0.050388474335024,-0.0186937936910934,0.),
 .UNSPECIFIED.);
#504=B_SPLINE_CURVE_WITH_KNOTS('',3,(#16388,#16389,#16390,#16391,#16392,
#16393,#16394,#16395),.UNSPECIFIED.,.F.,.F.,(4,1,1,1,1,4),(11.6159397475006,
12.61358260836,13.6112254692194,14.6088683300789,15.6065111909383,15.707963267949),
 .UNSPECIFIED.);
#505=B_SPLINE_CURVE_WITH_KNOTS('',3,(#16396,#16397,#16398,#16399,#16400,
#16401,#16402,#16403,#16404,#16405,#16406,#16407,#16408,#16409,#16410,#16411,
#16412,#16413,#16414,#16415,#16416,#16417,#16418,#16419,#16420,#16421,#16422,
#16423,#16424,#16425,#16426,#16427,#16428,#16429,#16430,#16431,#16432,#16433,
#16434,#16435,#16436,#16437,#16438,#16439,#16440,#16441,#16442,#16443,#16444),
 .UNSPECIFIED.,.F.,.F.,(4,3,3,3,3,3,3,3,3,3,3,3,3,3,3,3,4),(-0.275362278356892,
-0.263988733943187,-0.242277787653762,-0.228409792083558,-0.208856161945484,
-0.197709057767663,-0.168075464588018,-0.150222803571495,-0.140083955862437,
-0.125365894046572,-0.0997819296507484,-0.0889593225835958,-0.0667194919376969,
-0.0511923416312717,-0.0404361839568205,-0.0141940669149386,0.),
 .UNSPECIFIED.);
#506=B_SPLINE_CURVE_WITH_KNOTS('',3,(#16445,#16446,#16447,#16448,#16449,
#16450,#16451,#16452,#16453,#16454,#16455,#16456,#16457,#16458,#16459,#16460,
#16461,#16462,#16463),.UNSPECIFIED.,.F.,.F.,(4,3,3,3,3,3,4),(-191.027404416132,
-190.549786424147,-189.552143563287,-188.554500702428,-187.556857841568,
-186.559214980709,-186.304397428656),.UNSPECIFIED.);
#507=B_SPLINE_CURVE_WITH_KNOTS('',3,(#16466,#16467,#16468,#16469,#16470,
#16471,#16472,#16473,#16474),.UNSPECIFIED.,.F.,.F.,(4,1,1,1,1,1,4),(10.3752088276283,
11.2961629976806,12.2942052788047,13.2922475599287,14.2902898410527,15.2883321221767,
15.7079632679491),.UNSPECIFIED.);
#508=B_SPLINE_CURVE_WITH_KNOTS('',3,(#17268,#17269,#17270,#17271,#17272,
#17273,#17274,#17275,#17276,#17277,#17278,#17279,#17280,#17281,#17282,#17283,
#17284,#17285,#17286,#17287,#17288,#17289),.UNSPECIFIED.,.F.,.F.,(4,3,3,
3,3,3,3,4),(183.335115714669,183.639779726821,184.637822007945,185.635864289069,
186.633906570193,187.631948851317,188.629991132441,188.954231742812),
 .UNSPECIFIED.);
#509=B_SPLINE_CURVE_WITH_KNOTS('',3,(#17290,#17291,#17292,#17293,#17294,
#17295,#17296,#17297,#17298,#17299,#17300,#17301,#17302,#17303,#17304,#17305,
#17306,#17307,#17308,#17309,#17310,#17311,#17312,#17313,#17314,#17315,#17316,
#17317,#17318,#17319,#17320,#17321,#17322,#17323,#17324,#17325,#17326,#17327,
#17328,#17329,#17330,#17331,#17332,#17333,#17334,#17335,#17336,#17337,#17338,
#17339,#17340,#17341),.UNSPECIFIED.,.F.,.F.,(4,3,3,3,3,3,3,3,3,3,3,3,3,
3,3,3,3,4),(-0.276631791712714,-0.267404104599176,-0.245529112929484,-0.233826742508505,
-0.212230201958684,-0.201819484750363,-0.173281546649687,-0.162756755581661,
-0.152537502224722,-0.140478169692516,-0.120739781640826,-0.110641775261762,
-0.100726383882944,-0.0755447879122082,-0.0587891884452614,-0.0493012364577666,
-0.0182848522583483,0.),.UNSPECIFIED.);
#543=SHAPE_REPRESENTATION_RELATIONSHIP('SRR','None',#18404,#552);
#552=ADVANCED_BREP_SHAPE_REPRESENTATION('',(#570),#18350);
#561=STYLED_ITEM('',(#18458),#570);
#570=MANIFOLD_SOLID_BREP('Body1',#6492);
#632=FACE_BOUND('',#1556,.T.);
#633=FACE_BOUND('',#1559,.T.);
#639=CONICAL_SURFACE('',#7012,0.1,0.785398163397448);
#762=PLANE('',#7018);
#763=PLANE('',#7019);
#764=PLANE('',#7020);
#765=PLANE('',#7021);
#766=PLANE('',#7022);
#767=PLANE('',#7023);
#768=PLANE('',#7024);
#769=PLANE('',#7025);
#770=PLANE('',#7029);
#771=PLANE('',#7030);
#1053=FACE_OUTER_BOUND('',#1483,.T.);
#1054=FACE_OUTER_BOUND('',#1484,.T.);
#1055=FACE_OUTER_BOUND('',#1485,.T.);
#1056=FACE_OUTER_BOUND('',#1486,.T.);
#1057=FACE_OUTER_BOUND('',#1487,.T.);
#1058=FACE_OUTER_BOUND('',#1488,.T.);
#1059=FACE_OUTER_BOUND('',#1489,.T.);
#1060=FACE_OUTER_BOUND('',#1490,.T.);
#1061=FACE_OUTER_BOUND('',#1491,.T.);
#1062=FACE_OUTER_BOUND('',#1492,.T.);
#1063=FACE_OUTER_BOUND('',#1493,.T.);
#1064=FACE_OUTER_BOUND('',#1494,.T.);
#1065=FACE_OUTER_BOUND('',#1495,.T.);
#1066=FACE_OUTER_BOUND('',#1496,.T.);
#1067=FACE_OUTER_BOUND('',#1497,.T.);
#1068=FACE_OUTER_BOUND('',#1498,.T.);
#1069=FACE_OUTER_BOUND('',#1499,.T.);
#1070=FACE_OUTER_BOUND('',#1500,.T.);
#1071=FACE_OUTER_BOUND('',#1501,.T.);
#1072=FACE_OUTER_BOUND('',#1502,.T.);
#1073=FACE_OUTER_BOUND('',#1503,.T.);
#1074=FACE_OUTER_BOUND('',#1504,.T.);
#1075=FACE_OUTER_BOUND('',#1505,.T.);
#1076=FACE_OUTER_BOUND('',#1506,.T.);
#1077=FACE_OUTER_BOUND('',#1507,.T.);
#1078=FACE_OUTER_BOUND('',#1508,.T.);
#1079=FACE_OUTER_BOUND('',#1509,.T.);
#1080=FACE_OUTER_BOUND('',#1510,.T.);
#1081=FACE_OUTER_BOUND('',#1511,.T.);
#1082=FACE_OUTER_BOUND('',#1512,.T.);
#1083=FACE_OUTER_BOUND('',#1513,.T.);
#1084=FACE_OUTER_BOUND('',#1514,.T.);
#1085=FACE_OUTER_BOUND('',#1515,.T.);
#1086=FACE_OUTER_BOUND('',#1516,.T.);
#1087=FACE_OUTER_BOUND('',#1517,.T.);
#1088=FACE_OUTER_BOUND('',#1518,.T.);
#1089=FACE_OUTER_BOUND('',#1519,.T.);
#1090=FACE_OUTER_BOUND('',#1520,.T.);
#1091=FACE_OUTER_BOUND('',#1521,.T.);
#1092=FACE_OUTER_BOUND('',#1522,.T.);
#1093=FACE_OUTER_BOUND('',#1523,.T.);
#1094=FACE_OUTER_BOUND('',#1524,.T.);
#1095=FACE_OUTER_BOUND('',#1525,.T.);
#1096=FACE_OUTER_BOUND('',#1526,.T.);
#1097=FACE_OUTER_BOUND('',#1527,.T.);
#1098=FACE_OUTER_BOUND('',#1528,.T.);
#1099=FACE_OUTER_BOUND('',#1529,.T.);
#1100=FACE_OUTER_BOUND('',#1530,.T.);
#1101=FACE_OUTER_BOUND('',#1531,.T.);
#1102=FACE_OUTER_BOUND('',#1532,.T.);
#1103=FACE_OUTER_BOUND('',#1533,.T.);
#1104=FACE_OUTER_BOUND('',#1534,.T.);
#1105=FACE_OUTER_BOUND('',#1535,.T.);
#1106=FACE_OUTER_BOUND('',#1536,.T.);
#1107=FACE_OUTER_BOUND('',#1537,.T.);
#1108=FACE_OUTER_BOUND('',#1538,.T.);
#1109=FACE_OUTER_BOUND('',#1539,.T.);
#1110=FACE_OUTER_BOUND('',#1540,.T.);
#1111=FACE_OUTER_BOUND('',#1541,.T.);
#1112=FACE_OUTER_BOUND('',#1542,.T.);
#1113=FACE_OUTER_BOUND('',#1543,.T.);
#1114=FACE_OUTER_BOUND('',#1544,.T.);
#1115=FACE_OUTER_BOUND('',#1545,.T.);
#1116=FACE_OUTER_BOUND('',#1546,.T.);
#1117=FACE_OUTER_BOUND('',#1547,.T.);
#1118=FACE_OUTER_BOUND('',#1548,.T.);
#1119=FACE_OUTER_BOUND('',#1549,.T.);
#1120=FACE_OUTER_BOUND('',#1550,.T.);
#1121=FACE_OUTER_BOUND('',#1551,.T.);
#1122=FACE_OUTER_BOUND('',#1552,.T.);
#1123=FACE_OUTER_BOUND('',#1553,.T.);
#1124=FACE_OUTER_BOUND('',#1554,.T.);
#1125=FACE_OUTER_BOUND('',#1555,.T.);
#1126=FACE_OUTER_BOUND('',#1557,.T.);
#1127=FACE_OUTER_BOUND('',#1558,.T.);
#1128=FACE_OUTER_BOUND('',#1560,.T.);
#1483=EDGE_LOOP('',(#5418,#5419,#5420,#5421));
#1484=EDGE_LOOP('',(#5422,#5423,#5424,#5425));
#1485=EDGE_LOOP('',(#5426,#5427,#5428,#5429));
#1486=EDGE_LOOP('',(#5430,#5431,#5432,#5433));
#1487=EDGE_LOOP('',(#5434,#5435,#5436,#5437));
#1488=EDGE_LOOP('',(#5438,#5439,#5440,#5441));
#1489=EDGE_LOOP('',(#5442,#5443,#5444,#5445));
#1490=EDGE_LOOP('',(#5446,#5447,#5448,#5449));
#1491=EDGE_LOOP('',(#5450,#5451,#5452,#5453));
#1492=EDGE_LOOP('',(#5454,#5455,#5456,#5457));
#1493=EDGE_LOOP('',(#5458,#5459,#5460,#5461));
#1494=EDGE_LOOP('',(#5462,#5463,#5464,#5465));
#1495=EDGE_LOOP('',(#5466,#5467,#5468,#5469));
#1496=EDGE_LOOP('',(#5470,#5471,#5472,#5473));
#1497=EDGE_LOOP('',(#5474,#5475,#5476,#5477));
#1498=EDGE_LOOP('',(#5478,#5479,#5480,#5481));
#1499=EDGE_LOOP('',(#5482,#5483,#5484,#5485));
#1500=EDGE_LOOP('',(#5486,#5487,#5488,#5489));
#1501=EDGE_LOOP('',(#5490,#5491,#5492,#5493));
#1502=EDGE_LOOP('',(#5494,#5495,#5496,#5497));
#1503=EDGE_LOOP('',(#5498,#5499,#5500,#5501));
#1504=EDGE_LOOP('',(#5502,#5503,#5504,#5505));
#1505=EDGE_LOOP('',(#5506,#5507,#5508,#5509));
#1506=EDGE_LOOP('',(#5510,#5511,#5512,#5513));
#1507=EDGE_LOOP('',(#5514,#5515,#5516,#5517));
#1508=EDGE_LOOP('',(#5518,#5519,#5520,#5521));
#1509=EDGE_LOOP('',(#5522,#5523,#5524,#5525));
#1510=EDGE_LOOP('',(#5526,#5527,#5528,#5529));
#1511=EDGE_LOOP('',(#5530,#5531,#5532,#5533));
#1512=EDGE_LOOP('',(#5534,#5535,#5536,#5537));
#1513=EDGE_LOOP('',(#5538,#5539,#5540,#5541));
#1514=EDGE_LOOP('',(#5542,#5543,#5544,#5545));
#1515=EDGE_LOOP('',(#5546,#5547,#5548,#5549));
#1516=EDGE_LOOP('',(#5550,#5551,#5552,#5553));
#1517=EDGE_LOOP('',(#5554,#5555,#5556,#5557));
#1518=EDGE_LOOP('',(#5558,#5559,#5560,#5561));
#1519=EDGE_LOOP('',(#5562,#5563,#5564,#5565));
#1520=EDGE_LOOP('',(#5566,#5567,#5568,#5569));
#1521=EDGE_LOOP('',(#5570,#5571,#5572,#5573));
#1522=EDGE_LOOP('',(#5574,#5575,#5576,#5577));
#1523=EDGE_LOOP('',(#5578,#5579,#5580,#5581));
#1524=EDGE_LOOP('',(#5582,#5583,#5584,#5585));
#1525=EDGE_LOOP('',(#5586,#5587,#5588,#5589));
#1526=EDGE_LOOP('',(#5590,#5591,#5592,#5593));
#1527=EDGE_LOOP('',(#5594,#5595,#5596,#5597));
#1528=EDGE_LOOP('',(#5598,#5599,#5600,#5601));
#1529=EDGE_LOOP('',(#5602,#5603,#5604,#5605));
#1530=EDGE_LOOP('',(#5606,#5607,#5608,#5609));
#1531=EDGE_LOOP('',(#5610,#5611,#5612,#5613));
#1532=EDGE_LOOP('',(#5614,#5615,#5616,#5617));
#1533=EDGE_LOOP('',(#5618,#5619,#5620,#5621));
#1534=EDGE_LOOP('',(#5622,#5623,#5624,#5625));
#1535=EDGE_LOOP('',(#5626,#5627,#5628,#5629));
#1536=EDGE_LOOP('',(#5630,#5631,#5632,#5633));
#1537=EDGE_LOOP('',(#5634,#5635,#5636,#5637));
#1538=EDGE_LOOP('',(#5638,#5639,#5640,#5641));
#1539=EDGE_LOOP('',(#5642,#5643,#5644,#5645));
#1540=EDGE_LOOP('',(#5646,#5647,#5648,#5649));
#1541=EDGE_LOOP('',(#5650,#5651,#5652,#5653));
#1542=EDGE_LOOP('',(#5654,#5655,#5656,#5657));
#1543=EDGE_LOOP('',(#5658,#5659,#5660,#5661,#5662,#5663,#5664,#5665));
#1544=EDGE_LOOP('',(#5666,#5667,#5668,#5669,#5670,#5671,#5672,#5673,#5674,
#5675,#5676,#5677,#5678,#5679,#5680,#5681,#5682,#5683,#5684,#5685,#5686,
#5687,#5688,#5689,#5690,#5691,#5692,#5693,#5694,#5695,#5696,#5697,#5698,
#5699,#5700,#5701,#5702,#5703,#5704,#5705,#5706,#5707,#5708,#5709,#5710,
#5711,#5712,#5713,#5714,#5715,#5716,#5717,#5718,#5719,#5720,#5721,#5722,
#5723,#5724,#5725,#5726,#5727,#5728,#5729));
#1545=EDGE_LOOP('',(#5730,#5731,#5732,#5733));
#1546=EDGE_LOOP('',(#5734,#5735,#5736,#5737,#5738,#5739,#5740,#5741,#5742,
#5743,#5744,#5745,#5746,#5747,#5748,#5749,#5750,#5751,#5752,#5753,#5754,
#5755,#5756,#5757,#5758,#5759,#5760,#5761,#5762,#5763,#5764,#5765,#5766,
#5767,#5768,#5769,#5770,#5771,#5772,#5773,#5774,#5775,#5776,#5777,#5778,
#5779,#5780,#5781,#5782,#5783,#5784,#5785,#5786,#5787,#5788,#5789,#5790,
#5791,#5792,#5793,#5794,#5795,#5796,#5797,#5798));
#1547=EDGE_LOOP('',(#5799,#5800,#5801,#5802));
#1548=EDGE_LOOP('',(#5803,#5804,#5805,#5806));
#1549=EDGE_LOOP('',(#5807,#5808,#5809,#5810));
#1550=EDGE_LOOP('',(#5811,#5812,#5813,#5814));
#1551=EDGE_LOOP('',(#5815,#5816,#5817,#5818));
#1552=EDGE_LOOP('',(#5819,#5820,#5821,#5822));
#1553=EDGE_LOOP('',(#5823,#5824,#5825,#5826));
#1554=EDGE_LOOP('',(#5827,#5828,#5829,#5830,#5831,#5832));
#1555=EDGE_LOOP('',(#5833));
#1556=EDGE_LOOP('',(#5834,#5835,#5836,#5837));
#1557=EDGE_LOOP('',(#5838,#5839,#5840,#5841));
#1558=EDGE_LOOP('',(#5842));
#1559=EDGE_LOOP('',(#5843,#5844,#5845,#5846,#5847,#5848));
#1560=EDGE_LOOP('',(#5849));
#1885=LINE('',#13225,#2289);
#1886=LINE('',#13249,#2290);
#1887=LINE('',#13297,#2291);
#1888=LINE('',#13345,#2292);
#1889=LINE('',#13396,#2293);
#1890=LINE('',#13444,#2294);
#1891=LINE('',#13492,#2295);
#1892=LINE('',#13540,#2296);
#1893=LINE('',#13594,#2297);
#1894=LINE('',#13642,#2298);
#1895=LINE('',#13690,#2299);
#1896=LINE('',#13744,#2300);
#1897=LINE('',#13792,#2301);
#1898=LINE('',#13840,#2302);
#1899=LINE('',#13888,#2303);
#1900=LINE('',#13942,#2304);
#1901=LINE('',#13990,#2305);
#1902=LINE('',#14038,#2306);
#1903=LINE('',#14092,#2307);
#1904=LINE('',#14140,#2308);
#1905=LINE('',#14188,#2309);
#1906=LINE('',#14242,#2310);
#1907=LINE('',#14290,#2311);
#1908=LINE('',#14338,#2312);
#1909=LINE('',#14386,#2313);
#1910=LINE('',#14440,#2314);
#1911=LINE('',#14488,#2315);
#1912=LINE('',#14536,#2316);
#1913=LINE('',#14590,#2317);
#1914=LINE('',#14638,#2318);
#1915=LINE('',#14686,#2319);
#1916=LINE('',#14712,#2320);
#1917=LINE('',#14736,#2321);
#1918=LINE('',#14760,#2322);
#1919=LINE('',#14785,#2323);
#1920=LINE('',#14810,#2324);
#1921=LINE('',#14834,#2325);
#1922=LINE('',#14859,#2326);
#1923=LINE('',#14884,#2327);
#1924=LINE('',#14908,#2328);
#1925=LINE('',#14932,#2329);
#1926=LINE('',#14957,#2330);
#1927=LINE('',#14982,#2331);
#1928=LINE('',#15006,#2332);
#1929=LINE('',#15031,#2333);
#1930=LINE('',#15056,#2334);
#1931=LINE('',#15080,#2335);
#1932=LINE('',#15105,#2336);
#1933=LINE('',#15130,#2337);
#1934=LINE('',#15154,#2338);
#1935=LINE('',#15178,#2339);
#1936=LINE('',#15203,#2340);
#1937=LINE('',#15228,#2341);
#1938=LINE('',#15252,#2342);
#1939=LINE('',#15277,#2343);
#1940=LINE('',#15302,#2344);
#1941=LINE('',#15326,#2345);
#1942=LINE('',#15351,#2346);
#1943=LINE('',#15375,#2347);
#1944=LINE('',#15400,#2348);
#1945=LINE('',#15601,#2349);
#1946=LINE('',#17346,#2350);
#1947=LINE('',#17348,#2351);
#1948=LINE('',#17350,#2352);
#1949=LINE('',#17351,#2353);
#1950=LINE('',#17354,#2354);
#1951=LINE('',#17356,#2355);
#1952=LINE('',#17357,#2356);
#1953=LINE('',#17360,#2357);
#1954=LINE('',#17362,#2358);
#1955=LINE('',#17363,#2359);
#1956=LINE('',#17366,#2360);
#1957=LINE('',#17368,#2361);
#1958=LINE('',#17369,#2362);
#1959=LINE('',#17372,#2363);
#1960=LINE('',#17374,#2364);
#1961=LINE('',#17375,#2365);
#1962=LINE('',#17377,#2366);
#1963=LINE('',#17378,#2367);
#1964=LINE('',#17385,#2368);
#2289=VECTOR('',#8088,0.15);
#2290=VECTOR('',#8093,0.15);
#2291=VECTOR('',#8096,0.15);
#2292=VECTOR('',#8099,0.15);
#2293=VECTOR('',#8102,0.15);
#2294=VECTOR('',#8105,0.15);
#2295=VECTOR('',#8108,0.15);
#2296=VECTOR('',#8111,0.15);
#2297=VECTOR('',#8114,0.15);
#2298=VECTOR('',#8117,0.15);
#2299=VECTOR('',#8120,0.15);
#2300=VECTOR('',#8123,0.15);
#2301=VECTOR('',#8126,0.15);
#2302=VECTOR('',#8129,0.15);
#2303=VECTOR('',#8132,0.15);
#2304=VECTOR('',#8135,0.15);
#2305=VECTOR('',#8138,0.15);
#2306=VECTOR('',#8141,0.15);
#2307=VECTOR('',#8144,0.15);
#2308=VECTOR('',#8147,0.15);
#2309=VECTOR('',#8150,0.15);
#2310=VECTOR('',#8153,0.15);
#2311=VECTOR('',#8156,0.15);
#2312=VECTOR('',#8159,0.15);
#2313=VECTOR('',#8162,0.15);
#2314=VECTOR('',#8165,0.15);
#2315=VECTOR('',#8168,0.15);
#2316=VECTOR('',#8171,0.15);
#2317=VECTOR('',#8174,0.15);
#2318=VECTOR('',#8177,0.15);
#2319=VECTOR('',#8180,0.117775);
#2320=VECTOR('',#8185,0.117775);
#2321=VECTOR('',#8188,0.117775);
#2322=VECTOR('',#8191,0.117775);
#2323=VECTOR('',#8194,0.117775);
#2324=VECTOR('',#8197,0.117775);
#2325=VECTOR('',#8200,0.117775);
#2326=VECTOR('',#8203,0.117775);
#2327=VECTOR('',#8206,0.117775);
#2328=VECTOR('',#8209,0.117775);
#2329=VECTOR('',#8212,0.117775);
#2330=VECTOR('',#8215,0.117775);
#2331=VECTOR('',#8218,0.117775);
#2332=VECTOR('',#8221,0.117775);
#2333=VECTOR('',#8224,0.117775);
#2334=VECTOR('',#8227,0.117775);
#2335=VECTOR('',#8230,0.117775);
#2336=VECTOR('',#8233,0.117775);
#2337=VECTOR('',#8236,0.117775);
#2338=VECTOR('',#8239,0.117775);
#2339=VECTOR('',#8242,0.117775);
#2340=VECTOR('',#8245,0.117775);
#2341=VECTOR('',#8248,0.117775);
#2342=VECTOR('',#8251,0.117775);
#2343=VECTOR('',#8254,0.117775);
#2344=VECTOR('',#8257,0.117775);
#2345=VECTOR('',#8260,0.117775);
#2346=VECTOR('',#8263,0.117775);
#2347=VECTOR('',#8266,0.117775);
#2348=VECTOR('',#8269,0.117775);
#2349=VECTOR('',#8274,0.1);
#2350=VECTOR('',#8285,1.);
#2351=VECTOR('',#8286,1.);
#2352=VECTOR('',#8287,1.);
#2353=VECTOR('',#8288,1.);
#2354=VECTOR('',#8291,1.);
#2355=VECTOR('',#8292,1.);
#2356=VECTOR('',#8293,1.);
#2357=VECTOR('',#8296,1.);
#2358=VECTOR('',#8297,1.);
#2359=VECTOR('',#8298,1.);
#2360=VECTOR('',#8301,1.);
#2361=VECTOR('',#8302,1.);
#2362=VECTOR('',#8303,1.);
#2363=VECTOR('',#8306,1.);
#2364=VECTOR('',#8307,1.);
#2365=VECTOR('',#8308,1.);
#2366=VECTOR('',#8311,1.);
#2367=VECTOR('',#8312,1.);
#2368=VECTOR('',#8321,0.275);
#2550=CIRCLE('',#6951,0.14635);
#2551=CIRCLE('',#6982,0.117775);
#2552=CIRCLE('',#7013,0.14635);
#2553=CIRCLE('',#7014,0.05);
#2554=CIRCLE('',#7016,0.117775);
#2555=CIRCLE('',#7026,0.275);
#2556=CIRCLE('',#7028,0.275);
#2983=VERTEX_POINT('',#13223);
#2984=VERTEX_POINT('',#13224);
#2985=VERTEX_POINT('',#13226);
#2986=VERTEX_POINT('',#13237);
#2987=VERTEX_POINT('',#13247);
#2988=VERTEX_POINT('',#13248);
#2989=VERTEX_POINT('',#13295);
#2990=VERTEX_POINT('',#13296);
#2991=VERTEX_POINT('',#13343);
#2992=VERTEX_POINT('',#13344);
#2993=VERTEX_POINT('',#13394);
#2994=VERTEX_POINT('',#13395);
#2995=VERTEX_POINT('',#13442);
#2996=VERTEX_POINT('',#13443);
#2997=VERTEX_POINT('',#13490);
#2998=VERTEX_POINT('',#13491);
#2999=VERTEX_POINT('',#13538);
#3000=VERTEX_POINT('',#13539);
#3001=VERTEX_POINT('',#13592);
#3002=VERTEX_POINT('',#13593);
#3003=VERTEX_POINT('',#13640);
#3004=VERTEX_POINT('',#13641);
#3005=VERTEX_POINT('',#13688);
#3006=VERTEX_POINT('',#13689);
#3007=VERTEX_POINT('',#13742);
#3008=VERTEX_POINT('',#13743);
#3009=VERTEX_POINT('',#13790);
#3010=VERTEX_POINT('',#13791);
#3011=VERTEX_POINT('',#13838);
#3012=VERTEX_POINT('',#13839);
#3013=VERTEX_POINT('',#13886);
#3014=VERTEX_POINT('',#13887);
#3015=VERTEX_POINT('',#13940);
#3016=VERTEX_POINT('',#13941);
#3017=VERTEX_POINT('',#13988);
#3018=VERTEX_POINT('',#13989);
#3019=VERTEX_POINT('',#14036);
#3020=VERTEX_POINT('',#14037);
#3021=VERTEX_POINT('',#14090);
#3022=VERTEX_POINT('',#14091);
#3023=VERTEX_POINT('',#14138);
#3024=VERTEX_POINT('',#14139);
#3025=VERTEX_POINT('',#14186);
#3026=VERTEX_POINT('',#14187);
#3027=VERTEX_POINT('',#14240);
#3028=VERTEX_POINT('',#14241);
#3029=VERTEX_POINT('',#14288);
#3030=VERTEX_POINT('',#14289);
#3031=VERTEX_POINT('',#14336);
#3032=VERTEX_POINT('',#14337);
#3033=VERTEX_POINT('',#14384);
#3034=VERTEX_POINT('',#14385);
#3035=VERTEX_POINT('',#14438);
#3036=VERTEX_POINT('',#14439);
#3037=VERTEX_POINT('',#14486);
#3038=VERTEX_POINT('',#14487);
#3039=VERTEX_POINT('',#14534);
#3040=VERTEX_POINT('',#14535);
#3041=VERTEX_POINT('',#14588);
#3042=VERTEX_POINT('',#14589);
#3043=VERTEX_POINT('',#14636);
#3044=VERTEX_POINT('',#14637);
#3045=VERTEX_POINT('',#14684);
#3046=VERTEX_POINT('',#14685);
#3047=VERTEX_POINT('',#14687);
#3048=VERTEX_POINT('',#14698);
#3049=VERTEX_POINT('',#14710);
#3050=VERTEX_POINT('',#14711);
#3051=VERTEX_POINT('',#14734);
#3052=VERTEX_POINT('',#14735);
#3053=VERTEX_POINT('',#14758);
#3054=VERTEX_POINT('',#14759);
#3055=VERTEX_POINT('',#14783);
#3056=VERTEX_POINT('',#14784);
#3057=VERTEX_POINT('',#14808);
#3058=VERTEX_POINT('',#14809);
#3059=VERTEX_POINT('',#14832);
#3060=VERTEX_POINT('',#14833);
#3061=VERTEX_POINT('',#14857);
#3062=VERTEX_POINT('',#14858);
#3063=VERTEX_POINT('',#14882);
#3064=VERTEX_POINT('',#14883);
#3065=VERTEX_POINT('',#14906);
#3066=VERTEX_POINT('',#14907);
#3067=VERTEX_POINT('',#14930);
#3068=VERTEX_POINT('',#14931);
#3069=VERTEX_POINT('',#14955);
#3070=VERTEX_POINT('',#14956);
#3071=VERTEX_POINT('',#14980);
#3072=VERTEX_POINT('',#14981);
#3073=VERTEX_POINT('',#15004);
#3074=VERTEX_POINT('',#15005);
#3075=VERTEX_POINT('',#15029);
#3076=VERTEX_POINT('',#15030);
#3077=VERTEX_POINT('',#15054);
#3078=VERTEX_POINT('',#15055);
#3079=VERTEX_POINT('',#15078);
#3080=VERTEX_POINT('',#15079);
#3081=VERTEX_POINT('',#15103);
#3082=VERTEX_POINT('',#15104);
#3083=VERTEX_POINT('',#15128);
#3084=VERTEX_POINT('',#15129);
#3085=VERTEX_POINT('',#15152);
#3086=VERTEX_POINT('',#15153);
#3087=VERTEX_POINT('',#15176);
#3088=VERTEX_POINT('',#15177);
#3089=VERTEX_POINT('',#15201);
#3090=VERTEX_POINT('',#15202);
#3091=VERTEX_POINT('',#15226);
#3092=VERTEX_POINT('',#15227);
#3093=VERTEX_POINT('',#15250);
#3094=VERTEX_POINT('',#15251);
#3095=VERTEX_POINT('',#15275);
#3096=VERTEX_POINT('',#15276);
#3097=VERTEX_POINT('',#15300);
#3098=VERTEX_POINT('',#15301);
#3099=VERTEX_POINT('',#15324);
#3100=VERTEX_POINT('',#15325);
#3101=VERTEX_POINT('',#15349);
#3102=VERTEX_POINT('',#15350);
#3103=VERTEX_POINT('',#15373);
#3104=VERTEX_POINT('',#15374);
#3105=VERTEX_POINT('',#15398);
#3106=VERTEX_POINT('',#15399);
#3107=VERTEX_POINT('',#15422);
#3108=VERTEX_POINT('',#15544);
#3109=VERTEX_POINT('',#15582);
#3110=VERTEX_POINT('',#15600);
#3111=VERTEX_POINT('',#16387);
#3112=VERTEX_POINT('',#16465);
#3113=VERTEX_POINT('',#17344);
#3114=VERTEX_POINT('',#17345);
#3115=VERTEX_POINT('',#17347);
#3116=VERTEX_POINT('',#17349);
#3117=VERTEX_POINT('',#17353);
#3118=VERTEX_POINT('',#17355);
#3119=VERTEX_POINT('',#17359);
#3120=VERTEX_POINT('',#17361);
#3121=VERTEX_POINT('',#17365);
#3122=VERTEX_POINT('',#17367);
#3123=VERTEX_POINT('',#17371);
#3124=VERTEX_POINT('',#17373);
#3125=VERTEX_POINT('',#17381);
#3126=VERTEX_POINT('',#17384);
#3826=EDGE_CURVE('',#2983,#2984,#1885,.T.);
#3827=EDGE_CURVE('',#2983,#2985,#381,.T.);
#3828=EDGE_CURVE('',#2985,#2986,#2550,.F.);
#3829=EDGE_CURVE('',#2986,#2984,#382,.T.);
#3830=EDGE_CURVE('',#2987,#2988,#1886,.T.);
#3831=EDGE_CURVE('',#2987,#2983,#383,.T.);
#3832=EDGE_CURVE('',#2984,#2988,#384,.T.);
#3833=EDGE_CURVE('',#2989,#2990,#1887,.T.);
#3834=EDGE_CURVE('',#2989,#2987,#385,.T.);
#3835=EDGE_CURVE('',#2988,#2990,#386,.T.);
#3836=EDGE_CURVE('',#2991,#2992,#1888,.T.);
#3837=EDGE_CURVE('',#2991,#2989,#387,.T.);
#3838=EDGE_CURVE('',#2990,#2992,#388,.T.);
#3839=EDGE_CURVE('',#2993,#2994,#1889,.T.);
#3840=EDGE_CURVE('',#2993,#2991,#389,.T.);
#3841=EDGE_CURVE('',#2992,#2994,#390,.T.);
#3842=EDGE_CURVE('',#2995,#2996,#1890,.T.);
#3843=EDGE_CURVE('',#2995,#2993,#391,.T.);
#3844=EDGE_CURVE('',#2994,#2996,#392,.T.);
#3845=EDGE_CURVE('',#2997,#2998,#1891,.T.);
#3846=EDGE_CURVE('',#2997,#2995,#393,.T.);
#3847=EDGE_CURVE('',#2996,#2998,#394,.T.);
#3848=EDGE_CURVE('',#2999,#3000,#1892,.T.);
#3849=EDGE_CURVE('',#2999,#2997,#395,.T.);
#3850=EDGE_CURVE('',#2998,#3000,#396,.T.);
#3851=EDGE_CURVE('',#3001,#3002,#1893,.T.);
#3852=EDGE_CURVE('',#3001,#2999,#397,.T.);
#3853=EDGE_CURVE('',#3000,#3002,#398,.T.);
#3854=EDGE_CURVE('',#3003,#3004,#1894,.T.);
#3855=EDGE_CURVE('',#3003,#3001,#399,.T.);
#3856=EDGE_CURVE('',#3002,#3004,#400,.T.);
#3857=EDGE_CURVE('',#3005,#3006,#1895,.T.);
#3858=EDGE_CURVE('',#3005,#3003,#401,.T.);
#3859=EDGE_CURVE('',#3004,#3006,#402,.T.);
#3860=EDGE_CURVE('',#3007,#3008,#1896,.T.);
#3861=EDGE_CURVE('',#3007,#3005,#403,.T.);
#3862=EDGE_CURVE('',#3006,#3008,#404,.T.);
#3863=EDGE_CURVE('',#3009,#3010,#1897,.T.);
#3864=EDGE_CURVE('',#3009,#3007,#405,.T.);
#3865=EDGE_CURVE('',#3008,#3010,#406,.T.);
#3866=EDGE_CURVE('',#3011,#3012,#1898,.T.);
#3867=EDGE_CURVE('',#3011,#3009,#407,.T.);
#3868=EDGE_CURVE('',#3010,#3012,#408,.T.);
#3869=EDGE_CURVE('',#3013,#3014,#1899,.T.);
#3870=EDGE_CURVE('',#3013,#3011,#409,.T.);
#3871=EDGE_CURVE('',#3012,#3014,#410,.T.);
#3872=EDGE_CURVE('',#3015,#3016,#1900,.T.);
#3873=EDGE_CURVE('',#3015,#3013,#411,.T.);
#3874=EDGE_CURVE('',#3014,#3016,#412,.T.);
#3875=EDGE_CURVE('',#3017,#3018,#1901,.T.);
#3876=EDGE_CURVE('',#3017,#3015,#413,.T.);
#3877=EDGE_CURVE('',#3016,#3018,#414,.T.);
#3878=EDGE_CURVE('',#3019,#3020,#1902,.T.);
#3879=EDGE_CURVE('',#3019,#3017,#415,.T.);
#3880=EDGE_CURVE('',#3018,#3020,#416,.T.);
#3881=EDGE_CURVE('',#3021,#3022,#1903,.T.);
#3882=EDGE_CURVE('',#3021,#3019,#417,.T.);
#3883=EDGE_CURVE('',#3020,#3022,#418,.T.);
#3884=EDGE_CURVE('',#3023,#3024,#1904,.T.);
#3885=EDGE_CURVE('',#3023,#3021,#419,.T.);
#3886=EDGE_CURVE('',#3022,#3024,#420,.T.);
#3887=EDGE_CURVE('',#3025,#3026,#1905,.T.);
#3888=EDGE_CURVE('',#3025,#3023,#421,.T.);
#3889=EDGE_CURVE('',#3024,#3026,#422,.T.);
#3890=EDGE_CURVE('',#3027,#3028,#1906,.T.);
#3891=EDGE_CURVE('',#3027,#3025,#423,.T.);
#3892=EDGE_CURVE('',#3026,#3028,#424,.T.);
#3893=EDGE_CURVE('',#3029,#3030,#1907,.T.);
#3894=EDGE_CURVE('',#3029,#3027,#425,.T.);
#3895=EDGE_CURVE('',#3028,#3030,#426,.T.);
#3896=EDGE_CURVE('',#3031,#3032,#1908,.T.);
#3897=EDGE_CURVE('',#3031,#3029,#427,.T.);
#3898=EDGE_CURVE('',#3030,#3032,#428,.T.);
#3899=EDGE_CURVE('',#3033,#3034,#1909,.T.);
#3900=EDGE_CURVE('',#3033,#3031,#429,.T.);
#3901=EDGE_CURVE('',#3032,#3034,#430,.T.);
#3902=EDGE_CURVE('',#3035,#3036,#1910,.T.);
#3903=EDGE_CURVE('',#3035,#3033,#431,.T.);
#3904=EDGE_CURVE('',#3034,#3036,#432,.T.);
#3905=EDGE_CURVE('',#3037,#3038,#1911,.T.);
#3906=EDGE_CURVE('',#3037,#3035,#433,.T.);
#3907=EDGE_CURVE('',#3036,#3038,#434,.T.);
#3908=EDGE_CURVE('',#3039,#3040,#1912,.T.);
#3909=EDGE_CURVE('',#3039,#3037,#435,.T.);
#3910=EDGE_CURVE('',#3038,#3040,#436,.T.);
#3911=EDGE_CURVE('',#3041,#3042,#1913,.T.);
#3912=EDGE_CURVE('',#3041,#3039,#437,.T.);
#3913=EDGE_CURVE('',#3040,#3042,#438,.T.);
#3914=EDGE_CURVE('',#3043,#3044,#1914,.T.);
#3915=EDGE_CURVE('',#3043,#3041,#439,.T.);
#3916=EDGE_CURVE('',#3042,#3044,#440,.T.);
#3917=EDGE_CURVE('',#3045,#3046,#1915,.T.);
#3918=EDGE_CURVE('',#3045,#3047,#441,.T.);
#3919=EDGE_CURVE('',#3047,#3048,#2551,.T.);
#3920=EDGE_CURVE('',#3046,#3048,#442,.T.);
#3921=EDGE_CURVE('',#3049,#3050,#1916,.T.);
#3922=EDGE_CURVE('',#3049,#3045,#443,.T.);
#3923=EDGE_CURVE('',#3050,#3046,#444,.T.);
#3924=EDGE_CURVE('',#3051,#3052,#1917,.T.);
#3925=EDGE_CURVE('',#3051,#3049,#445,.T.);
#3926=EDGE_CURVE('',#3052,#3050,#446,.T.);
#3927=EDGE_CURVE('',#3053,#3054,#1918,.T.);
#3928=EDGE_CURVE('',#3053,#3051,#447,.T.);
#3929=EDGE_CURVE('',#3054,#3052,#448,.T.);
#3930=EDGE_CURVE('',#3055,#3056,#1919,.T.);
#3931=EDGE_CURVE('',#3055,#3053,#449,.T.);
#3932=EDGE_CURVE('',#3056,#3054,#450,.T.);
#3933=EDGE_CURVE('',#3057,#3058,#1920,.T.);
#3934=EDGE_CURVE('',#3057,#3055,#451,.T.);
#3935=EDGE_CURVE('',#3058,#3056,#452,.T.);
#3936=EDGE_CURVE('',#3059,#3060,#1921,.T.);
#3937=EDGE_CURVE('',#3059,#3057,#453,.T.);
#3938=EDGE_CURVE('',#3060,#3058,#454,.T.);
#3939=EDGE_CURVE('',#3061,#3062,#1922,.T.);
#3940=EDGE_CURVE('',#3061,#3059,#455,.T.);
#3941=EDGE_CURVE('',#3062,#3060,#456,.T.);
#3942=EDGE_CURVE('',#3063,#3064,#1923,.T.);
#3943=EDGE_CURVE('',#3063,#3061,#457,.T.);
#3944=EDGE_CURVE('',#3064,#3062,#458,.T.);
#3945=EDGE_CURVE('',#3065,#3066,#1924,.T.);
#3946=EDGE_CURVE('',#3065,#3063,#459,.T.);
#3947=EDGE_CURVE('',#3066,#3064,#460,.T.);
#3948=EDGE_CURVE('',#3067,#3068,#1925,.T.);
#3949=EDGE_CURVE('',#3067,#3065,#461,.T.);
#3950=EDGE_CURVE('',#3068,#3066,#462,.T.);
#3951=EDGE_CURVE('',#3069,#3070,#1926,.T.);
#3952=EDGE_CURVE('',#3069,#3067,#463,.T.);
#3953=EDGE_CURVE('',#3070,#3068,#464,.T.);
#3954=EDGE_CURVE('',#3071,#3072,#1927,.T.);
#3955=EDGE_CURVE('',#3071,#3069,#465,.T.);
#3956=EDGE_CURVE('',#3072,#3070,#466,.T.);
#3957=EDGE_CURVE('',#3073,#3074,#1928,.T.);
#3958=EDGE_CURVE('',#3073,#3071,#467,.T.);
#3959=EDGE_CURVE('',#3074,#3072,#468,.T.);
#3960=EDGE_CURVE('',#3075,#3076,#1929,.T.);
#3961=EDGE_CURVE('',#3075,#3073,#469,.T.);
#3962=EDGE_CURVE('',#3076,#3074,#470,.T.);
#3963=EDGE_CURVE('',#3077,#3078,#1930,.T.);
#3964=EDGE_CURVE('',#3077,#3075,#471,.T.);
#3965=EDGE_CURVE('',#3078,#3076,#472,.T.);
#3966=EDGE_CURVE('',#3079,#3080,#1931,.T.);
#3967=EDGE_CURVE('',#3079,#3077,#473,.T.);
#3968=EDGE_CURVE('',#3080,#3078,#474,.T.);
#3969=EDGE_CURVE('',#3081,#3082,#1932,.T.);
#3970=EDGE_CURVE('',#3081,#3079,#475,.T.);
#3971=EDGE_CURVE('',#3082,#3080,#476,.T.);
#3972=EDGE_CURVE('',#3083,#3084,#1933,.T.);
#3973=EDGE_CURVE('',#3083,#3081,#477,.T.);
#3974=EDGE_CURVE('',#3084,#3082,#478,.T.);
#3975=EDGE_CURVE('',#3085,#3086,#1934,.T.);
#3976=EDGE_CURVE('',#3085,#3083,#479,.T.);
#3977=EDGE_CURVE('',#3086,#3084,#480,.T.);
#3978=EDGE_CURVE('',#3087,#3088,#1935,.T.);
#3979=EDGE_CURVE('',#3087,#3085,#481,.T.);
#3980=EDGE_CURVE('',#3088,#3086,#482,.T.);
#3981=EDGE_CURVE('',#3089,#3090,#1936,.T.);
#3982=EDGE_CURVE('',#3089,#3087,#483,.T.);
#3983=EDGE_CURVE('',#3090,#3088,#484,.T.);
#3984=EDGE_CURVE('',#3091,#3092,#1937,.T.);
#3985=EDGE_CURVE('',#3091,#3089,#485,.T.);
#3986=EDGE_CURVE('',#3092,#3090,#486,.T.);
#3987=EDGE_CURVE('',#3093,#3094,#1938,.T.);
#3988=EDGE_CURVE('',#3093,#3091,#487,.T.);
#3989=EDGE_CURVE('',#3094,#3092,#488,.T.);
#3990=EDGE_CURVE('',#3095,#3096,#1939,.T.);
#3991=EDGE_CURVE('',#3095,#3093,#489,.T.);
#3992=EDGE_CURVE('',#3096,#3094,#490,.T.);
#3993=EDGE_CURVE('',#3097,#3098,#1940,.T.);
#3994=EDGE_CURVE('',#3097,#3095,#491,.T.);
#3995=EDGE_CURVE('',#3098,#3096,#492,.T.);
#3996=EDGE_CURVE('',#3099,#3100,#1941,.T.);
#3997=EDGE_CURVE('',#3099,#3097,#493,.T.);
#3998=EDGE_CURVE('',#3100,#3098,#494,.T.);
#3999=EDGE_CURVE('',#3101,#3102,#1942,.T.);
#4000=EDGE_CURVE('',#3101,#3099,#495,.T.);
#4001=EDGE_CURVE('',#3102,#3100,#496,.T.);
#4002=EDGE_CURVE('',#3103,#3104,#1943,.T.);
#4003=EDGE_CURVE('',#3103,#3101,#497,.T.);
#4004=EDGE_CURVE('',#3104,#3102,#498,.T.);
#4005=EDGE_CURVE('',#3105,#3106,#1944,.T.);
#4006=EDGE_CURVE('',#3105,#3103,#499,.T.);
#4007=EDGE_CURVE('',#3106,#3104,#500,.T.);
#4008=EDGE_CURVE('',#3048,#3107,#501,.T.);
#4009=EDGE_CURVE('',#3108,#3047,#502,.T.);
#4010=EDGE_CURVE('',#3109,#3108,#2552,.T.);
#4011=EDGE_CURVE('',#3107,#3109,#503,.T.);
#4012=EDGE_CURVE('',#3107,#3110,#1945,.T.);
#4013=EDGE_CURVE('',#3110,#3110,#2553,.T.);
#4014=EDGE_CURVE('',#3111,#3105,#504,.T.);
#4015=EDGE_CURVE('',#2985,#3111,#505,.T.);
#4016=EDGE_CURVE('',#3108,#3043,#506,.T.);
#4017=EDGE_CURVE('',#3112,#3106,#507,.T.);
#4018=EDGE_CURVE('',#3111,#3112,#2554,.T.);
#4019=EDGE_CURVE('',#3044,#3109,#508,.T.);
#4020=EDGE_CURVE('',#3112,#2986,#509,.T.);
#4021=EDGE_CURVE('',#3113,#3114,#1946,.T.);
#4022=EDGE_CURVE('',#3113,#3115,#1947,.T.);
#4023=EDGE_CURVE('',#3115,#3116,#1948,.T.);
#4024=EDGE_CURVE('',#3114,#3116,#1949,.T.);
#4025=EDGE_CURVE('',#3117,#3113,#1950,.T.);
#4026=EDGE_CURVE('',#3117,#3118,#1951,.T.);
#4027=EDGE_CURVE('',#3118,#3115,#1952,.T.);
#4028=EDGE_CURVE('',#3119,#3117,#1953,.T.);
#4029=EDGE_CURVE('',#3119,#3120,#1954,.T.);
#4030=EDGE_CURVE('',#3120,#3118,#1955,.T.);
#4031=EDGE_CURVE('',#3121,#3119,#1956,.T.);
#4032=EDGE_CURVE('',#3121,#3122,#1957,.T.);
#4033=EDGE_CURVE('',#3122,#3120,#1958,.T.);
#4034=EDGE_CURVE('',#3123,#3121,#1959,.T.);
#4035=EDGE_CURVE('',#3123,#3124,#1960,.T.);
#4036=EDGE_CURVE('',#3124,#3122,#1961,.T.);
#4037=EDGE_CURVE('',#3114,#3123,#1962,.T.);
#4038=EDGE_CURVE('',#3116,#3124,#1963,.T.);
#4039=EDGE_CURVE('',#3125,#3125,#2555,.T.);
#4040=EDGE_CURVE('',#3125,#3126,#1964,.T.);
#4041=EDGE_CURVE('',#3126,#3126,#2556,.T.);
#5418=ORIENTED_EDGE('',*,*,#3826,.F.);
#5419=ORIENTED_EDGE('',*,*,#3827,.T.);
#5420=ORIENTED_EDGE('',*,*,#3828,.T.);
#5421=ORIENTED_EDGE('',*,*,#3829,.T.);
#5422=ORIENTED_EDGE('',*,*,#3830,.F.);
#5423=ORIENTED_EDGE('',*,*,#3831,.T.);
#5424=ORIENTED_EDGE('',*,*,#3826,.T.);
#5425=ORIENTED_EDGE('',*,*,#3832,.T.);
#5426=ORIENTED_EDGE('',*,*,#3833,.F.);
#5427=ORIENTED_EDGE('',*,*,#3834,.T.);
#5428=ORIENTED_EDGE('',*,*,#3830,.T.);
#5429=ORIENTED_EDGE('',*,*,#3835,.T.);
#5430=ORIENTED_EDGE('',*,*,#3836,.F.);
#5431=ORIENTED_EDGE('',*,*,#3837,.T.);
#5432=ORIENTED_EDGE('',*,*,#3833,.T.);
#5433=ORIENTED_EDGE('',*,*,#3838,.T.);
#5434=ORIENTED_EDGE('',*,*,#3839,.F.);
#5435=ORIENTED_EDGE('',*,*,#3840,.T.);
#5436=ORIENTED_EDGE('',*,*,#3836,.T.);
#5437=ORIENTED_EDGE('',*,*,#3841,.T.);
#5438=ORIENTED_EDGE('',*,*,#3842,.F.);
#5439=ORIENTED_EDGE('',*,*,#3843,.T.);
#5440=ORIENTED_EDGE('',*,*,#3839,.T.);
#5441=ORIENTED_EDGE('',*,*,#3844,.T.);
#5442=ORIENTED_EDGE('',*,*,#3845,.F.);
#5443=ORIENTED_EDGE('',*,*,#3846,.T.);
#5444=ORIENTED_EDGE('',*,*,#3842,.T.);
#5445=ORIENTED_EDGE('',*,*,#3847,.T.);
#5446=ORIENTED_EDGE('',*,*,#3848,.F.);
#5447=ORIENTED_EDGE('',*,*,#3849,.T.);
#5448=ORIENTED_EDGE('',*,*,#3845,.T.);
#5449=ORIENTED_EDGE('',*,*,#3850,.T.);
#5450=ORIENTED_EDGE('',*,*,#3851,.F.);
#5451=ORIENTED_EDGE('',*,*,#3852,.T.);
#5452=ORIENTED_EDGE('',*,*,#3848,.T.);
#5453=ORIENTED_EDGE('',*,*,#3853,.T.);
#5454=ORIENTED_EDGE('',*,*,#3854,.F.);
#5455=ORIENTED_EDGE('',*,*,#3855,.T.);
#5456=ORIENTED_EDGE('',*,*,#3851,.T.);
#5457=ORIENTED_EDGE('',*,*,#3856,.T.);
#5458=ORIENTED_EDGE('',*,*,#3857,.F.);
#5459=ORIENTED_EDGE('',*,*,#3858,.T.);
#5460=ORIENTED_EDGE('',*,*,#3854,.T.);
#5461=ORIENTED_EDGE('',*,*,#3859,.T.);
#5462=ORIENTED_EDGE('',*,*,#3860,.F.);
#5463=ORIENTED_EDGE('',*,*,#3861,.T.);
#5464=ORIENTED_EDGE('',*,*,#3857,.T.);
#5465=ORIENTED_EDGE('',*,*,#3862,.T.);
#5466=ORIENTED_EDGE('',*,*,#3863,.F.);
#5467=ORIENTED_EDGE('',*,*,#3864,.T.);
#5468=ORIENTED_EDGE('',*,*,#3860,.T.);
#5469=ORIENTED_EDGE('',*,*,#3865,.T.);
#5470=ORIENTED_EDGE('',*,*,#3866,.F.);
#5471=ORIENTED_EDGE('',*,*,#3867,.T.);
#5472=ORIENTED_EDGE('',*,*,#3863,.T.);
#5473=ORIENTED_EDGE('',*,*,#3868,.T.);
#5474=ORIENTED_EDGE('',*,*,#3869,.F.);
#5475=ORIENTED_EDGE('',*,*,#3870,.T.);
#5476=ORIENTED_EDGE('',*,*,#3866,.T.);
#5477=ORIENTED_EDGE('',*,*,#3871,.T.);
#5478=ORIENTED_EDGE('',*,*,#3872,.F.);
#5479=ORIENTED_EDGE('',*,*,#3873,.T.);
#5480=ORIENTED_EDGE('',*,*,#3869,.T.);
#5481=ORIENTED_EDGE('',*,*,#3874,.T.);
#5482=ORIENTED_EDGE('',*,*,#3875,.F.);
#5483=ORIENTED_EDGE('',*,*,#3876,.T.);
#5484=ORIENTED_EDGE('',*,*,#3872,.T.);
#5485=ORIENTED_EDGE('',*,*,#3877,.T.);
#5486=ORIENTED_EDGE('',*,*,#3878,.F.);
#5487=ORIENTED_EDGE('',*,*,#3879,.T.);
#5488=ORIENTED_EDGE('',*,*,#3875,.T.);
#5489=ORIENTED_EDGE('',*,*,#3880,.T.);
#5490=ORIENTED_EDGE('',*,*,#3881,.F.);
#5491=ORIENTED_EDGE('',*,*,#3882,.T.);
#5492=ORIENTED_EDGE('',*,*,#3878,.T.);
#5493=ORIENTED_EDGE('',*,*,#3883,.T.);
#5494=ORIENTED_EDGE('',*,*,#3884,.F.);
#5495=ORIENTED_EDGE('',*,*,#3885,.T.);
#5496=ORIENTED_EDGE('',*,*,#3881,.T.);
#5497=ORIENTED_EDGE('',*,*,#3886,.T.);
#5498=ORIENTED_EDGE('',*,*,#3887,.F.);
#5499=ORIENTED_EDGE('',*,*,#3888,.T.);
#5500=ORIENTED_EDGE('',*,*,#3884,.T.);
#5501=ORIENTED_EDGE('',*,*,#3889,.T.);
#5502=ORIENTED_EDGE('',*,*,#3890,.F.);
#5503=ORIENTED_EDGE('',*,*,#3891,.T.);
#5504=ORIENTED_EDGE('',*,*,#3887,.T.);
#5505=ORIENTED_EDGE('',*,*,#3892,.T.);
#5506=ORIENTED_EDGE('',*,*,#3893,.F.);
#5507=ORIENTED_EDGE('',*,*,#3894,.T.);
#5508=ORIENTED_EDGE('',*,*,#3890,.T.);
#5509=ORIENTED_EDGE('',*,*,#3895,.T.);
#5510=ORIENTED_EDGE('',*,*,#3896,.F.);
#5511=ORIENTED_EDGE('',*,*,#3897,.T.);
#5512=ORIENTED_EDGE('',*,*,#3893,.T.);
#5513=ORIENTED_EDGE('',*,*,#3898,.T.);
#5514=ORIENTED_EDGE('',*,*,#3899,.F.);
#5515=ORIENTED_EDGE('',*,*,#3900,.T.);
#5516=ORIENTED_EDGE('',*,*,#3896,.T.);
#5517=ORIENTED_EDGE('',*,*,#3901,.T.);
#5518=ORIENTED_EDGE('',*,*,#3902,.F.);
#5519=ORIENTED_EDGE('',*,*,#3903,.T.);
#5520=ORIENTED_EDGE('',*,*,#3899,.T.);
#5521=ORIENTED_EDGE('',*,*,#3904,.T.);
#5522=ORIENTED_EDGE('',*,*,#3905,.F.);
#5523=ORIENTED_EDGE('',*,*,#3906,.T.);
#5524=ORIENTED_EDGE('',*,*,#3902,.T.);
#5525=ORIENTED_EDGE('',*,*,#3907,.T.);
#5526=ORIENTED_EDGE('',*,*,#3908,.F.);
#5527=ORIENTED_EDGE('',*,*,#3909,.T.);
#5528=ORIENTED_EDGE('',*,*,#3905,.T.);
#5529=ORIENTED_EDGE('',*,*,#3910,.T.);
#5530=ORIENTED_EDGE('',*,*,#3911,.F.);
#5531=ORIENTED_EDGE('',*,*,#3912,.T.);
#5532=ORIENTED_EDGE('',*,*,#3908,.T.);
#5533=ORIENTED_EDGE('',*,*,#3913,.T.);
#5534=ORIENTED_EDGE('',*,*,#3914,.F.);
#5535=ORIENTED_EDGE('',*,*,#3915,.T.);
#5536=ORIENTED_EDGE('',*,*,#3911,.T.);
#5537=ORIENTED_EDGE('',*,*,#3916,.T.);
#5538=ORIENTED_EDGE('',*,*,#3917,.F.);
#5539=ORIENTED_EDGE('',*,*,#3918,.T.);
#5540=ORIENTED_EDGE('',*,*,#3919,.T.);
#5541=ORIENTED_EDGE('',*,*,#3920,.F.);
#5542=ORIENTED_EDGE('',*,*,#3921,.F.);
#5543=ORIENTED_EDGE('',*,*,#3922,.T.);
#5544=ORIENTED_EDGE('',*,*,#3917,.T.);
#5545=ORIENTED_EDGE('',*,*,#3923,.F.);
#5546=ORIENTED_EDGE('',*,*,#3924,.F.);
#5547=ORIENTED_EDGE('',*,*,#3925,.T.);
#5548=ORIENTED_EDGE('',*,*,#3921,.T.);
#5549=ORIENTED_EDGE('',*,*,#3926,.F.);
#5550=ORIENTED_EDGE('',*,*,#3927,.F.);
#5551=ORIENTED_EDGE('',*,*,#3928,.T.);
#5552=ORIENTED_EDGE('',*,*,#3924,.T.);
#5553=ORIENTED_EDGE('',*,*,#3929,.F.);
#5554=ORIENTED_EDGE('',*,*,#3930,.F.);
#5555=ORIENTED_EDGE('',*,*,#3931,.T.);
#5556=ORIENTED_EDGE('',*,*,#3927,.T.);
#5557=ORIENTED_EDGE('',*,*,#3932,.F.);
#5558=ORIENTED_EDGE('',*,*,#3933,.F.);
#5559=ORIENTED_EDGE('',*,*,#3934,.T.);
#5560=ORIENTED_EDGE('',*,*,#3930,.T.);
#5561=ORIENTED_EDGE('',*,*,#3935,.F.);
#5562=ORIENTED_EDGE('',*,*,#3936,.F.);
#5563=ORIENTED_EDGE('',*,*,#3937,.T.);
#5564=ORIENTED_EDGE('',*,*,#3933,.T.);
#5565=ORIENTED_EDGE('',*,*,#3938,.F.);
#5566=ORIENTED_EDGE('',*,*,#3939,.F.);
#5567=ORIENTED_EDGE('',*,*,#3940,.T.);
#5568=ORIENTED_EDGE('',*,*,#3936,.T.);
#5569=ORIENTED_EDGE('',*,*,#3941,.F.);
#5570=ORIENTED_EDGE('',*,*,#3942,.F.);
#5571=ORIENTED_EDGE('',*,*,#3943,.T.);
#5572=ORIENTED_EDGE('',*,*,#3939,.T.);
#5573=ORIENTED_EDGE('',*,*,#3944,.F.);
#5574=ORIENTED_EDGE('',*,*,#3945,.F.);
#5575=ORIENTED_EDGE('',*,*,#3946,.T.);
#5576=ORIENTED_EDGE('',*,*,#3942,.T.);
#5577=ORIENTED_EDGE('',*,*,#3947,.F.);
#5578=ORIENTED_EDGE('',*,*,#3948,.F.);
#5579=ORIENTED_EDGE('',*,*,#3949,.T.);
#5580=ORIENTED_EDGE('',*,*,#3945,.T.);
#5581=ORIENTED_EDGE('',*,*,#3950,.F.);
#5582=ORIENTED_EDGE('',*,*,#3951,.F.);
#5583=ORIENTED_EDGE('',*,*,#3952,.T.);
#5584=ORIENTED_EDGE('',*,*,#3948,.T.);
#5585=ORIENTED_EDGE('',*,*,#3953,.F.);
#5586=ORIENTED_EDGE('',*,*,#3954,.F.);
#5587=ORIENTED_EDGE('',*,*,#3955,.T.);
#5588=ORIENTED_EDGE('',*,*,#3951,.T.);
#5589=ORIENTED_EDGE('',*,*,#3956,.F.);
#5590=ORIENTED_EDGE('',*,*,#3957,.F.);
#5591=ORIENTED_EDGE('',*,*,#3958,.T.);
#5592=ORIENTED_EDGE('',*,*,#3954,.T.);
#5593=ORIENTED_EDGE('',*,*,#3959,.F.);
#5594=ORIENTED_EDGE('',*,*,#3960,.F.);
#5595=ORIENTED_EDGE('',*,*,#3961,.T.);
#5596=ORIENTED_EDGE('',*,*,#3957,.T.);
#5597=ORIENTED_EDGE('',*,*,#3962,.F.);
#5598=ORIENTED_EDGE('',*,*,#3963,.F.);
#5599=ORIENTED_EDGE('',*,*,#3964,.T.);
#5600=ORIENTED_EDGE('',*,*,#3960,.T.);
#5601=ORIENTED_EDGE('',*,*,#3965,.F.);
#5602=ORIENTED_EDGE('',*,*,#3966,.F.);
#5603=ORIENTED_EDGE('',*,*,#3967,.T.);
#5604=ORIENTED_EDGE('',*,*,#3963,.T.);
#5605=ORIENTED_EDGE('',*,*,#3968,.F.);
#5606=ORIENTED_EDGE('',*,*,#3969,.F.);
#5607=ORIENTED_EDGE('',*,*,#3970,.T.);
#5608=ORIENTED_EDGE('',*,*,#3966,.T.);
#5609=ORIENTED_EDGE('',*,*,#3971,.F.);
#5610=ORIENTED_EDGE('',*,*,#3972,.F.);
#5611=ORIENTED_EDGE('',*,*,#3973,.T.);
#5612=ORIENTED_EDGE('',*,*,#3969,.T.);
#5613=ORIENTED_EDGE('',*,*,#3974,.F.);
#5614=ORIENTED_EDGE('',*,*,#3975,.F.);
#5615=ORIENTED_EDGE('',*,*,#3976,.T.);
#5616=ORIENTED_EDGE('',*,*,#3972,.T.);
#5617=ORIENTED_EDGE('',*,*,#3977,.F.);
#5618=ORIENTED_EDGE('',*,*,#3978,.F.);
#5619=ORIENTED_EDGE('',*,*,#3979,.T.);
#5620=ORIENTED_EDGE('',*,*,#3975,.T.);
#5621=ORIENTED_EDGE('',*,*,#3980,.F.);
#5622=ORIENTED_EDGE('',*,*,#3981,.F.);
#5623=ORIENTED_EDGE('',*,*,#3982,.T.);
#5624=ORIENTED_EDGE('',*,*,#3978,.T.);
#5625=ORIENTED_EDGE('',*,*,#3983,.F.);
#5626=ORIENTED_EDGE('',*,*,#3984,.F.);
#5627=ORIENTED_EDGE('',*,*,#3985,.T.);
#5628=ORIENTED_EDGE('',*,*,#3981,.T.);
#5629=ORIENTED_EDGE('',*,*,#3986,.F.);
#5630=ORIENTED_EDGE('',*,*,#3987,.F.);
#5631=ORIENTED_EDGE('',*,*,#3988,.T.);
#5632=ORIENTED_EDGE('',*,*,#3984,.T.);
#5633=ORIENTED_EDGE('',*,*,#3989,.F.);
#5634=ORIENTED_EDGE('',*,*,#3990,.F.);
#5635=ORIENTED_EDGE('',*,*,#3991,.T.);
#5636=ORIENTED_EDGE('',*,*,#3987,.T.);
#5637=ORIENTED_EDGE('',*,*,#3992,.F.);
#5638=ORIENTED_EDGE('',*,*,#3993,.F.);
#5639=ORIENTED_EDGE('',*,*,#3994,.T.);
#5640=ORIENTED_EDGE('',*,*,#3990,.T.);
#5641=ORIENTED_EDGE('',*,*,#3995,.F.);
#5642=ORIENTED_EDGE('',*,*,#3996,.F.);
#5643=ORIENTED_EDGE('',*,*,#3997,.T.);
#5644=ORIENTED_EDGE('',*,*,#3993,.T.);
#5645=ORIENTED_EDGE('',*,*,#3998,.F.);
#5646=ORIENTED_EDGE('',*,*,#3999,.F.);
#5647=ORIENTED_EDGE('',*,*,#4000,.T.);
#5648=ORIENTED_EDGE('',*,*,#3996,.T.);
#5649=ORIENTED_EDGE('',*,*,#4001,.F.);
#5650=ORIENTED_EDGE('',*,*,#4002,.F.);
#5651=ORIENTED_EDGE('',*,*,#4003,.T.);
#5652=ORIENTED_EDGE('',*,*,#3999,.T.);
#5653=ORIENTED_EDGE('',*,*,#4004,.F.);
#5654=ORIENTED_EDGE('',*,*,#4005,.F.);
#5655=ORIENTED_EDGE('',*,*,#4006,.T.);
#5656=ORIENTED_EDGE('',*,*,#4002,.T.);
#5657=ORIENTED_EDGE('',*,*,#4007,.F.);
#5658=ORIENTED_EDGE('',*,*,#4008,.F.);
#5659=ORIENTED_EDGE('',*,*,#3919,.F.);
#5660=ORIENTED_EDGE('',*,*,#4009,.F.);
#5661=ORIENTED_EDGE('',*,*,#4010,.F.);
#5662=ORIENTED_EDGE('',*,*,#4011,.F.);
#5663=ORIENTED_EDGE('',*,*,#4012,.T.);
#5664=ORIENTED_EDGE('',*,*,#4013,.F.);
#5665=ORIENTED_EDGE('',*,*,#4012,.F.);
#5666=ORIENTED_EDGE('',*,*,#4009,.T.);
#5667=ORIENTED_EDGE('',*,*,#3918,.F.);
#5668=ORIENTED_EDGE('',*,*,#3922,.F.);
#5669=ORIENTED_EDGE('',*,*,#3925,.F.);
#5670=ORIENTED_EDGE('',*,*,#3928,.F.);
#5671=ORIENTED_EDGE('',*,*,#3931,.F.);
#5672=ORIENTED_EDGE('',*,*,#3934,.F.);
#5673=ORIENTED_EDGE('',*,*,#3937,.F.);
#5674=ORIENTED_EDGE('',*,*,#3940,.F.);
#5675=ORIENTED_EDGE('',*,*,#3943,.F.);
#5676=ORIENTED_EDGE('',*,*,#3946,.F.);
#5677=ORIENTED_EDGE('',*,*,#3949,.F.);
#5678=ORIENTED_EDGE('',*,*,#3952,.F.);
#5679=ORIENTED_EDGE('',*,*,#3955,.F.);
#5680=ORIENTED_EDGE('',*,*,#3958,.F.);
#5681=ORIENTED_EDGE('',*,*,#3961,.F.);
#5682=ORIENTED_EDGE('',*,*,#3964,.F.);
#5683=ORIENTED_EDGE('',*,*,#3967,.F.);
#5684=ORIENTED_EDGE('',*,*,#3970,.F.);
#5685=ORIENTED_EDGE('',*,*,#3973,.F.);
#5686=ORIENTED_EDGE('',*,*,#3976,.F.);
#5687=ORIENTED_EDGE('',*,*,#3979,.F.);
#5688=ORIENTED_EDGE('',*,*,#3982,.F.);
#5689=ORIENTED_EDGE('',*,*,#3985,.F.);
#5690=ORIENTED_EDGE('',*,*,#3988,.F.);
#5691=ORIENTED_EDGE('',*,*,#3991,.F.);
#5692=ORIENTED_EDGE('',*,*,#3994,.F.);
#5693=ORIENTED_EDGE('',*,*,#3997,.F.);
#5694=ORIENTED_EDGE('',*,*,#4000,.F.);
#5695=ORIENTED_EDGE('',*,*,#4003,.F.);
#5696=ORIENTED_EDGE('',*,*,#4006,.F.);
#5697=ORIENTED_EDGE('',*,*,#4014,.F.);
#5698=ORIENTED_EDGE('',*,*,#4015,.F.);
#5699=ORIENTED_EDGE('',*,*,#3827,.F.);
#5700=ORIENTED_EDGE('',*,*,#3831,.F.);
#5701=ORIENTED_EDGE('',*,*,#3834,.F.);
#5702=ORIENTED_EDGE('',*,*,#3837,.F.);
#5703=ORIENTED_EDGE('',*,*,#3840,.F.);
#5704=ORIENTED_EDGE('',*,*,#3843,.F.);
#5705=ORIENTED_EDGE('',*,*,#3846,.F.);
#5706=ORIENTED_EDGE('',*,*,#3849,.F.);
#5707=ORIENTED_EDGE('',*,*,#3852,.F.);
#5708=ORIENTED_EDGE('',*,*,#3855,.F.);
#5709=ORIENTED_EDGE('',*,*,#3858,.F.);
#5710=ORIENTED_EDGE('',*,*,#3861,.F.);
#5711=ORIENTED_EDGE('',*,*,#3864,.F.);
#5712=ORIENTED_EDGE('',*,*,#3867,.F.);
#5713=ORIENTED_EDGE('',*,*,#3870,.F.);
#5714=ORIENTED_EDGE('',*,*,#3873,.F.);
#5715=ORIENTED_EDGE('',*,*,#3876,.F.);
#5716=ORIENTED_EDGE('',*,*,#3879,.F.);
#5717=ORIENTED_EDGE('',*,*,#3882,.F.);
#5718=ORIENTED_EDGE('',*,*,#3885,.F.);
#5719=ORIENTED_EDGE('',*,*,#3888,.F.);
#5720=ORIENTED_EDGE('',*,*,#3891,.F.);
#5721=ORIENTED_EDGE('',*,*,#3894,.F.);
#5722=ORIENTED_EDGE('',*,*,#3897,.F.);
#5723=ORIENTED_EDGE('',*,*,#3900,.F.);
#5724=ORIENTED_EDGE('',*,*,#3903,.F.);
#5725=ORIENTED_EDGE('',*,*,#3906,.F.);
#5726=ORIENTED_EDGE('',*,*,#3909,.F.);
#5727=ORIENTED_EDGE('',*,*,#3912,.F.);
#5728=ORIENTED_EDGE('',*,*,#3915,.F.);
#5729=ORIENTED_EDGE('',*,*,#4016,.F.);
#5730=ORIENTED_EDGE('',*,*,#4005,.T.);
#5731=ORIENTED_EDGE('',*,*,#4017,.F.);
#5732=ORIENTED_EDGE('',*,*,#4018,.F.);
#5733=ORIENTED_EDGE('',*,*,#4014,.T.);
#5734=ORIENTED_EDGE('',*,*,#4008,.T.);
#5735=ORIENTED_EDGE('',*,*,#4011,.T.);
#5736=ORIENTED_EDGE('',*,*,#4019,.F.);
#5737=ORIENTED_EDGE('',*,*,#3916,.F.);
#5738=ORIENTED_EDGE('',*,*,#3913,.F.);
#5739=ORIENTED_EDGE('',*,*,#3910,.F.);
#5740=ORIENTED_EDGE('',*,*,#3907,.F.);
#5741=ORIENTED_EDGE('',*,*,#3904,.F.);
#5742=ORIENTED_EDGE('',*,*,#3901,.F.);
#5743=ORIENTED_EDGE('',*,*,#3898,.F.);
#5744=ORIENTED_EDGE('',*,*,#3895,.F.);
#5745=ORIENTED_EDGE('',*,*,#3892,.F.);
#5746=ORIENTED_EDGE('',*,*,#3889,.F.);
#5747=ORIENTED_EDGE('',*,*,#3886,.F.);
#5748=ORIENTED_EDGE('',*,*,#3883,.F.);
#5749=ORIENTED_EDGE('',*,*,#3880,.F.);
#5750=ORIENTED_EDGE('',*,*,#3877,.F.);
#5751=ORIENTED_EDGE('',*,*,#3874,.F.);
#5752=ORIENTED_EDGE('',*,*,#3871,.F.);
#5753=ORIENTED_EDGE('',*,*,#3868,.F.);
#5754=ORIENTED_EDGE('',*,*,#3865,.F.);
#5755=ORIENTED_EDGE('',*,*,#3862,.F.);
#5756=ORIENTED_EDGE('',*,*,#3859,.F.);
#5757=ORIENTED_EDGE('',*,*,#3856,.F.);
#5758=ORIENTED_EDGE('',*,*,#3853,.F.);
#5759=ORIENTED_EDGE('',*,*,#3850,.F.);
#5760=ORIENTED_EDGE('',*,*,#3847,.F.);
#5761=ORIENTED_EDGE('',*,*,#3844,.F.);
#5762=ORIENTED_EDGE('',*,*,#3841,.F.);
#5763=ORIENTED_EDGE('',*,*,#3838,.F.);
#5764=ORIENTED_EDGE('',*,*,#3835,.F.);
#5765=ORIENTED_EDGE('',*,*,#3832,.F.);
#5766=ORIENTED_EDGE('',*,*,#3829,.F.);
#5767=ORIENTED_EDGE('',*,*,#4020,.F.);
#5768=ORIENTED_EDGE('',*,*,#4017,.T.);
#5769=ORIENTED_EDGE('',*,*,#4007,.T.);
#5770=ORIENTED_EDGE('',*,*,#4004,.T.);
#5771=ORIENTED_EDGE('',*,*,#4001,.T.);
#5772=ORIENTED_EDGE('',*,*,#3998,.T.);
#5773=ORIENTED_EDGE('',*,*,#3995,.T.);
#5774=ORIENTED_EDGE('',*,*,#3992,.T.);
#5775=ORIENTED_EDGE('',*,*,#3989,.T.);
#5776=ORIENTED_EDGE('',*,*,#3986,.T.);
#5777=ORIENTED_EDGE('',*,*,#3983,.T.);
#5778=ORIENTED_EDGE('',*,*,#3980,.T.);
#5779=ORIENTED_EDGE('',*,*,#3977,.T.);
#5780=ORIENTED_EDGE('',*,*,#3974,.T.);
#5781=ORIENTED_EDGE('',*,*,#3971,.T.);
#5782=ORIENTED_EDGE('',*,*,#3968,.T.);
#5783=ORIENTED_EDGE('',*,*,#3965,.T.);
#5784=ORIENTED_EDGE('',*,*,#3962,.T.);
#5785=ORIENTED_EDGE('',*,*,#3959,.T.);
#5786=ORIENTED_EDGE('',*,*,#3956,.T.);
#5787=ORIENTED_EDGE('',*,*,#3953,.T.);
#5788=ORIENTED_EDGE('',*,*,#3950,.T.);
#5789=ORIENTED_EDGE('',*,*,#3947,.T.);
#5790=ORIENTED_EDGE('',*,*,#3944,.T.);
#5791=ORIENTED_EDGE('',*,*,#3941,.T.);
#5792=ORIENTED_EDGE('',*,*,#3938,.T.);
#5793=ORIENTED_EDGE('',*,*,#3935,.T.);
#5794=ORIENTED_EDGE('',*,*,#3932,.T.);
#5795=ORIENTED_EDGE('',*,*,#3929,.T.);
#5796=ORIENTED_EDGE('',*,*,#3926,.T.);
#5797=ORIENTED_EDGE('',*,*,#3923,.T.);
#5798=ORIENTED_EDGE('',*,*,#3920,.T.);
#5799=ORIENTED_EDGE('',*,*,#3914,.T.);
#5800=ORIENTED_EDGE('',*,*,#4019,.T.);
#5801=ORIENTED_EDGE('',*,*,#4010,.T.);
#5802=ORIENTED_EDGE('',*,*,#4016,.T.);
#5803=ORIENTED_EDGE('',*,*,#4021,.F.);
#5804=ORIENTED_EDGE('',*,*,#4022,.T.);
#5805=ORIENTED_EDGE('',*,*,#4023,.T.);
#5806=ORIENTED_EDGE('',*,*,#4024,.F.);
#5807=ORIENTED_EDGE('',*,*,#4025,.F.);
#5808=ORIENTED_EDGE('',*,*,#4026,.T.);
#5809=ORIENTED_EDGE('',*,*,#4027,.T.);
#5810=ORIENTED_EDGE('',*,*,#4022,.F.);
#5811=ORIENTED_EDGE('',*,*,#4028,.F.);
#5812=ORIENTED_EDGE('',*,*,#4029,.T.);
#5813=ORIENTED_EDGE('',*,*,#4030,.T.);
#5814=ORIENTED_EDGE('',*,*,#4026,.F.);
#5815=ORIENTED_EDGE('',*,*,#4031,.F.);
#5816=ORIENTED_EDGE('',*,*,#4032,.T.);
#5817=ORIENTED_EDGE('',*,*,#4033,.T.);
#5818=ORIENTED_EDGE('',*,*,#4029,.F.);
#5819=ORIENTED_EDGE('',*,*,#4034,.F.);
#5820=ORIENTED_EDGE('',*,*,#4035,.T.);
#5821=ORIENTED_EDGE('',*,*,#4036,.T.);
#5822=ORIENTED_EDGE('',*,*,#4032,.F.);
#5823=ORIENTED_EDGE('',*,*,#4037,.F.);
#5824=ORIENTED_EDGE('',*,*,#4024,.T.);
#5825=ORIENTED_EDGE('',*,*,#4038,.T.);
#5826=ORIENTED_EDGE('',*,*,#4035,.F.);
#5827=ORIENTED_EDGE('',*,*,#4038,.F.);
#5828=ORIENTED_EDGE('',*,*,#4023,.F.);
#5829=ORIENTED_EDGE('',*,*,#4027,.F.);
#5830=ORIENTED_EDGE('',*,*,#4030,.F.);
#5831=ORIENTED_EDGE('',*,*,#4033,.F.);
#5832=ORIENTED_EDGE('',*,*,#4036,.F.);
#5833=ORIENTED_EDGE('',*,*,#4039,.T.);
#5834=ORIENTED_EDGE('',*,*,#4015,.T.);
#5835=ORIENTED_EDGE('',*,*,#4018,.T.);
#5836=ORIENTED_EDGE('',*,*,#4020,.T.);
#5837=ORIENTED_EDGE('',*,*,#3828,.F.);
#5838=ORIENTED_EDGE('',*,*,#4039,.F.);
#5839=ORIENTED_EDGE('',*,*,#4040,.T.);
#5840=ORIENTED_EDGE('',*,*,#4041,.T.);
#5841=ORIENTED_EDGE('',*,*,#4040,.F.);
#5842=ORIENTED_EDGE('',*,*,#4041,.F.);
#5843=ORIENTED_EDGE('',*,*,#4021,.T.);
#5844=ORIENTED_EDGE('',*,*,#4037,.T.);
#5845=ORIENTED_EDGE('',*,*,#4034,.T.);
#5846=ORIENTED_EDGE('',*,*,#4031,.T.);
#5847=ORIENTED_EDGE('',*,*,#4028,.T.);
#5848=ORIENTED_EDGE('',*,*,#4025,.T.);
#5849=ORIENTED_EDGE('',*,*,#4013,.T.);
#6036=CYLINDRICAL_SURFACE('',#6950,0.14635);
#6037=CYLINDRICAL_SURFACE('',#6952,0.14635);
#6038=CYLINDRICAL_SURFACE('',#6953,0.14635);
#6039=CYLINDRICAL_SURFACE('',#6954,0.14635);
#6040=CYLINDRICAL_SURFACE('',#6955,0.14635);
#6041=CYLINDRICAL_SURFACE('',#6956,0.14635);
#6042=CYLINDRICAL_SURFACE('',#6957,0.14635);
#6043=CYLINDRICAL_SURFACE('',#6958,0.14635);
#6044=CYLINDRICAL_SURFACE('',#6959,0.14635);
#6045=CYLINDRICAL_SURFACE('',#6960,0.14635);
#6046=CYLINDRICAL_SURFACE('',#6961,0.14635);
#6047=CYLINDRICAL_SURFACE('',#6962,0.14635);
#6048=CYLINDRICAL_SURFACE('',#6963,0.14635);
#6049=CYLINDRICAL_SURFACE('',#6964,0.14635);
#6050=CYLINDRICAL_SURFACE('',#6965,0.14635);
#6051=CYLINDRICAL_SURFACE('',#6966,0.14635);
#6052=CYLINDRICAL_SURFACE('',#6967,0.14635);
#6053=CYLINDRICAL_SURFACE('',#6968,0.14635);
#6054=CYLINDRICAL_SURFACE('',#6969,0.14635);
#6055=CYLINDRICAL_SURFACE('',#6970,0.14635);
#6056=CYLINDRICAL_SURFACE('',#6971,0.14635);
#6057=CYLINDRICAL_SURFACE('',#6972,0.14635);
#6058=CYLINDRICAL_SURFACE('',#6973,0.14635);
#6059=CYLINDRICAL_SURFACE('',#6974,0.14635);
#6060=CYLINDRICAL_SURFACE('',#6975,0.14635);
#6061=CYLINDRICAL_SURFACE('',#6976,0.14635);
#6062=CYLINDRICAL_SURFACE('',#6977,0.14635);
#6063=CYLINDRICAL_SURFACE('',#6978,0.14635);
#6064=CYLINDRICAL_SURFACE('',#6979,0.14635);
#6065=CYLINDRICAL_SURFACE('',#6980,0.14635);
#6066=CYLINDRICAL_SURFACE('',#6981,0.117775);
#6067=CYLINDRICAL_SURFACE('',#6983,0.117775);
#6068=CYLINDRICAL_SURFACE('',#6984,0.117775);
#6069=CYLINDRICAL_SURFACE('',#6985,0.117775);
#6070=CYLINDRICAL_SURFACE('',#6986,0.117775);
#6071=CYLINDRICAL_SURFACE('',#6987,0.117775);
#6072=CYLINDRICAL_SURFACE('',#6988,0.117775);
#6073=CYLINDRICAL_SURFACE('',#6989,0.117775);
#6074=CYLINDRICAL_SURFACE('',#6990,0.117775);
#6075=CYLINDRICAL_SURFACE('',#6991,0.117775);
#6076=CYLINDRICAL_SURFACE('',#6992,0.117775);
#6077=CYLINDRICAL_SURFACE('',#6993,0.117775);
#6078=CYLINDRICAL_SURFACE('',#6994,0.117775);
#6079=CYLINDRICAL_SURFACE('',#6995,0.117775);
#6080=CYLINDRICAL_SURFACE('',#6996,0.117775);
#6081=CYLINDRICAL_SURFACE('',#6997,0.117775);
#6082=CYLINDRICAL_SURFACE('',#6998,0.117775);
#6083=CYLINDRICAL_SURFACE('',#6999,0.117775);
#6084=CYLINDRICAL_SURFACE('',#7000,0.117775);
#6085=CYLINDRICAL_SURFACE('',#7001,0.117775);
#6086=CYLINDRICAL_SURFACE('',#7002,0.117775);
#6087=CYLINDRICAL_SURFACE('',#7003,0.117775);
#6088=CYLINDRICAL_SURFACE('',#7004,0.117775);
#6089=CYLINDRICAL_SURFACE('',#7005,0.117775);
#6090=CYLINDRICAL_SURFACE('',#7006,0.117775);
#6091=CYLINDRICAL_SURFACE('',#7007,0.117775);
#6092=CYLINDRICAL_SURFACE('',#7008,0.117775);
#6093=CYLINDRICAL_SURFACE('',#7009,0.117775);
#6094=CYLINDRICAL_SURFACE('',#7010,0.117775);
#6095=CYLINDRICAL_SURFACE('',#7011,0.117775);
#6096=CYLINDRICAL_SURFACE('',#7015,0.117775);
#6097=CYLINDRICAL_SURFACE('',#7017,0.14635);
#6098=CYLINDRICAL_SURFACE('',#7027,0.275);
#6384=ADVANCED_FACE('',(#1053),#6036,.T.);
#6385=ADVANCED_FACE('',(#1054),#6037,.T.);
#6386=ADVANCED_FACE('',(#1055),#6038,.T.);
#6387=ADVANCED_FACE('',(#1056),#6039,.T.);
#6388=ADVANCED_FACE('',(#1057),#6040,.T.);
#6389=ADVANCED_FACE('',(#1058),#6041,.T.);
#6390=ADVANCED_FACE('',(#1059),#6042,.T.);
#6391=ADVANCED_FACE('',(#1060),#6043,.T.);
#6392=ADVANCED_FACE('',(#1061),#6044,.T.);
#6393=ADVANCED_FACE('',(#1062),#6045,.T.);
#6394=ADVANCED_FACE('',(#1063),#6046,.T.);
#6395=ADVANCED_FACE('',(#1064),#6047,.T.);
#6396=ADVANCED_FACE('',(#1065),#6048,.T.);
#6397=ADVANCED_FACE('',(#1066),#6049,.T.);
#6398=ADVANCED_FACE('',(#1067),#6050,.T.);
#6399=ADVANCED_FACE('',(#1068),#6051,.T.);
#6400=ADVANCED_FACE('',(#1069),#6052,.T.);
#6401=ADVANCED_FACE('',(#1070),#6053,.T.);
#6402=ADVANCED_FACE('',(#1071),#6054,.T.);
#6403=ADVANCED_FACE('',(#1072),#6055,.T.);
#6404=ADVANCED_FACE('',(#1073),#6056,.T.);
#6405=ADVANCED_FACE('',(#1074),#6057,.T.);
#6406=ADVANCED_FACE('',(#1075),#6058,.T.);
#6407=ADVANCED_FACE('',(#1076),#6059,.T.);
#6408=ADVANCED_FACE('',(#1077),#6060,.T.);
#6409=ADVANCED_FACE('',(#1078),#6061,.T.);
#6410=ADVANCED_FACE('',(#1079),#6062,.T.);
#6411=ADVANCED_FACE('',(#1080),#6063,.T.);
#6412=ADVANCED_FACE('',(#1081),#6064,.T.);
#6413=ADVANCED_FACE('',(#1082),#6065,.T.);
#6414=ADVANCED_FACE('',(#1083),#6066,.T.);
#6415=ADVANCED_FACE('',(#1084),#6067,.T.);
#6416=ADVANCED_FACE('',(#1085),#6068,.T.);
#6417=ADVANCED_FACE('',(#1086),#6069,.T.);
#6418=ADVANCED_FACE('',(#1087),#6070,.T.);
#6419=ADVANCED_FACE('',(#1088),#6071,.T.);
#6420=ADVANCED_FACE('',(#1089),#6072,.T.);
#6421=ADVANCED_FACE('',(#1090),#6073,.T.);
#6422=ADVANCED_FACE('',(#1091),#6074,.T.);
#6423=ADVANCED_FACE('',(#1092),#6075,.T.);
#6424=ADVANCED_FACE('',(#1093),#6076,.T.);
#6425=ADVANCED_FACE('',(#1094),#6077,.T.);
#6426=ADVANCED_FACE('',(#1095),#6078,.T.);
#6427=ADVANCED_FACE('',(#1096),#6079,.T.);
#6428=ADVANCED_FACE('',(#1097),#6080,.T.);
#6429=ADVANCED_FACE('',(#1098),#6081,.T.);
#6430=ADVANCED_FACE('',(#1099),#6082,.T.);
#6431=ADVANCED_FACE('',(#1100),#6083,.T.);
#6432=ADVANCED_FACE('',(#1101),#6084,.T.);
#6433=ADVANCED_FACE('',(#1102),#6085,.T.);
#6434=ADVANCED_FACE('',(#1103),#6086,.T.);
#6435=ADVANCED_FACE('',(#1104),#6087,.T.);
#6436=ADVANCED_FACE('',(#1105),#6088,.T.);
#6437=ADVANCED_FACE('',(#1106),#6089,.T.);
#6438=ADVANCED_FACE('',(#1107),#6090,.T.);
#6439=ADVANCED_FACE('',(#1108),#6091,.T.);
#6440=ADVANCED_FACE('',(#1109),#6092,.T.);
#6441=ADVANCED_FACE('',(#1110),#6093,.T.);
#6442=ADVANCED_FACE('',(#1111),#6094,.T.);
#6443=ADVANCED_FACE('',(#1112),#6095,.T.);
#6444=ADVANCED_FACE('',(#1113),#639,.T.);
#6445=ADVANCED_FACE('',(#1114),#167,.F.);
#6446=ADVANCED_FACE('',(#1115),#6096,.T.);
#6447=ADVANCED_FACE('',(#1116),#168,.F.);
#6448=ADVANCED_FACE('',(#1117),#6097,.T.);
#6449=ADVANCED_FACE('',(#1118),#762,.F.);
#6450=ADVANCED_FACE('',(#1119),#763,.F.);
#6451=ADVANCED_FACE('',(#1120),#764,.F.);
#6452=ADVANCED_FACE('',(#1121),#765,.F.);
#6453=ADVANCED_FACE('',(#1122),#766,.F.);
#6454=ADVANCED_FACE('',(#1123),#767,.F.);
#6455=ADVANCED_FACE('',(#1124),#768,.F.);
#6456=ADVANCED_FACE('',(#1125,#632),#769,.T.);
#6457=ADVANCED_FACE('',(#1126),#6098,.T.);
#6458=ADVANCED_FACE('',(#1127,#633),#770,.F.);
#6459=ADVANCED_FACE('',(#1128),#771,.T.);
#6492=CLOSED_SHELL('',(#6384,#6385,#6386,#6387,#6388,#6389,#6390,#6391,
#6392,#6393,#6394,#6395,#6396,#6397,#6398,#6399,#6400,#6401,#6402,#6403,
#6404,#6405,#6406,#6407,#6408,#6409,#6410,#6411,#6412,#6413,#6414,#6415,
#6416,#6417,#6418,#6419,#6420,#6421,#6422,#6423,#6424,#6425,#6426,#6427,
#6428,#6429,#6430,#6431,#6432,#6433,#6434,#6435,#6436,#6437,#6438,#6439,
#6440,#6441,#6442,#6443,#6444,#6445,#6446,#6447,#6448,#6449,#6450,#6451,
#6452,#6453,#6454,#6455,#6456,#6457,#6458,#6459));
#6949=AXIS2_PLACEMENT_3D('',#13221,#8084,#8085);
#6950=AXIS2_PLACEMENT_3D('',#13222,#8086,#8087);
#6951=AXIS2_PLACEMENT_3D('',#13238,#8089,#8090);
#6952=AXIS2_PLACEMENT_3D('',#13246,#8091,#8092);
#6953=AXIS2_PLACEMENT_3D('',#13294,#8094,#8095);
#6954=AXIS2_PLACEMENT_3D('',#13342,#8097,#8098);
#6955=AXIS2_PLACEMENT_3D('',#13393,#8100,#8101);
#6956=AXIS2_PLACEMENT_3D('',#13441,#8103,#8104);
#6957=AXIS2_PLACEMENT_3D('',#13489,#8106,#8107);
#6958=AXIS2_PLACEMENT_3D('',#13537,#8109,#8110);
#6959=AXIS2_PLACEMENT_3D('',#13591,#8112,#8113);
#6960=AXIS2_PLACEMENT_3D('',#13639,#8115,#8116);
#6961=AXIS2_PLACEMENT_3D('',#13687,#8118,#8119);
#6962=AXIS2_PLACEMENT_3D('',#13741,#8121,#8122);
#6963=AXIS2_PLACEMENT_3D('',#13789,#8124,#8125);
#6964=AXIS2_PLACEMENT_3D('',#13837,#8127,#8128);
#6965=AXIS2_PLACEMENT_3D('',#13885,#8130,#8131);
#6966=AXIS2_PLACEMENT_3D('',#13939,#8133,#8134);
#6967=AXIS2_PLACEMENT_3D('',#13987,#8136,#8137);
#6968=AXIS2_PLACEMENT_3D('',#14035,#8139,#8140);
#6969=AXIS2_PLACEMENT_3D('',#14089,#8142,#8143);
#6970=AXIS2_PLACEMENT_3D('',#14137,#8145,#8146);
#6971=AXIS2_PLACEMENT_3D('',#14185,#8148,#8149);
#6972=AXIS2_PLACEMENT_3D('',#14239,#8151,#8152);
#6973=AXIS2_PLACEMENT_3D('',#14287,#8154,#8155);
#6974=AXIS2_PLACEMENT_3D('',#14335,#8157,#8158);
#6975=AXIS2_PLACEMENT_3D('',#14383,#8160,#8161);
#6976=AXIS2_PLACEMENT_3D('',#14437,#8163,#8164);
#6977=AXIS2_PLACEMENT_3D('',#14485,#8166,#8167);
#6978=AXIS2_PLACEMENT_3D('',#14533,#8169,#8170);
#6979=AXIS2_PLACEMENT_3D('',#14587,#8172,#8173);
#6980=AXIS2_PLACEMENT_3D('',#14635,#8175,#8176);
#6981=AXIS2_PLACEMENT_3D('',#14683,#8178,#8179);
#6982=AXIS2_PLACEMENT_3D('',#14699,#8181,#8182);
#6983=AXIS2_PLACEMENT_3D('',#14709,#8183,#8184);
#6984=AXIS2_PLACEMENT_3D('',#14733,#8186,#8187);
#6985=AXIS2_PLACEMENT_3D('',#14757,#8189,#8190);
#6986=AXIS2_PLACEMENT_3D('',#14782,#8192,#8193);
#6987=AXIS2_PLACEMENT_3D('',#14807,#8195,#8196);
#6988=AXIS2_PLACEMENT_3D('',#14831,#8198,#8199);
#6989=AXIS2_PLACEMENT_3D('',#14856,#8201,#8202);
#6990=AXIS2_PLACEMENT_3D('',#14881,#8204,#8205);
#6991=AXIS2_PLACEMENT_3D('',#14905,#8207,#8208);
#6992=AXIS2_PLACEMENT_3D('',#14929,#8210,#8211);
#6993=AXIS2_PLACEMENT_3D('',#14954,#8213,#8214);
#6994=AXIS2_PLACEMENT_3D('',#14979,#8216,#8217);
#6995=AXIS2_PLACEMENT_3D('',#15003,#8219,#8220);
#6996=AXIS2_PLACEMENT_3D('',#15028,#8222,#8223);
#6997=AXIS2_PLACEMENT_3D('',#15053,#8225,#8226);
#6998=AXIS2_PLACEMENT_3D('',#15077,#8228,#8229);
#6999=AXIS2_PLACEMENT_3D('',#15102,#8231,#8232);
#7000=AXIS2_PLACEMENT_3D('',#15127,#8234,#8235);
#7001=AXIS2_PLACEMENT_3D('',#15151,#8237,#8238);
#7002=AXIS2_PLACEMENT_3D('',#15175,#8240,#8241);
#7003=AXIS2_PLACEMENT_3D('',#15200,#8243,#8244);
#7004=AXIS2_PLACEMENT_3D('',#15225,#8246,#8247);
#7005=AXIS2_PLACEMENT_3D('',#15249,#8249,#8250);
#7006=AXIS2_PLACEMENT_3D('',#15274,#8252,#8253);
#7007=AXIS2_PLACEMENT_3D('',#15299,#8255,#8256);
#7008=AXIS2_PLACEMENT_3D('',#15323,#8258,#8259);
#7009=AXIS2_PLACEMENT_3D('',#15348,#8261,#8262);
#7010=AXIS2_PLACEMENT_3D('',#15372,#8264,#8265);
#7011=AXIS2_PLACEMENT_3D('',#15397,#8267,#8268);
#7012=AXIS2_PLACEMENT_3D('',#15421,#8270,#8271);
#7013=AXIS2_PLACEMENT_3D('',#15583,#8272,#8273);
#7014=AXIS2_PLACEMENT_3D('',#15602,#8275,#8276);
#7015=AXIS2_PLACEMENT_3D('',#16464,#8277,#8278);
#7016=AXIS2_PLACEMENT_3D('',#16475,#8279,#8280);
#7017=AXIS2_PLACEMENT_3D('',#17342,#8281,#8282);
#7018=AXIS2_PLACEMENT_3D('',#17343,#8283,#8284);
#7019=AXIS2_PLACEMENT_3D('',#17352,#8289,#8290);
#7020=AXIS2_PLACEMENT_3D('',#17358,#8294,#8295);
#7021=AXIS2_PLACEMENT_3D('',#17364,#8299,#8300);
#7022=AXIS2_PLACEMENT_3D('',#17370,#8304,#8305);
#7023=AXIS2_PLACEMENT_3D('',#17376,#8309,#8310);
#7024=AXIS2_PLACEMENT_3D('',#17379,#8313,#8314);
#7025=AXIS2_PLACEMENT_3D('',#17380,#8315,#8316);
#7026=AXIS2_PLACEMENT_3D('',#17382,#8317,#8318);
#7027=AXIS2_PLACEMENT_3D('',#17383,#8319,#8320);
#7028=AXIS2_PLACEMENT_3D('',#17386,#8322,#8323);
#7029=AXIS2_PLACEMENT_3D('',#17387,#8324,#8325);
#7030=AXIS2_PLACEMENT_3D('',#17388,#8326,#8327);
#8084=DIRECTION('axis',(0.,0.,1.));
#8085=DIRECTION('refdir',(1.,0.,0.));
#8086=DIRECTION('center_axis',(0.,0.,1.));
#8087=DIRECTION('ref_axis',(1.,0.,0.));
#8088=DIRECTION('',(0.,0.,-1.));
#8089=DIRECTION('center_axis',(0.,0.,-1.));
#8090=DIRECTION('ref_axis',(1.,0.,0.));
#8091=DIRECTION('center_axis',(0.,0.,1.));
#8092=DIRECTION('ref_axis',(1.,0.,0.));
#8093=DIRECTION('',(0.,0.,-1.));
#8094=DIRECTION('center_axis',(0.,0.,1.));
#8095=DIRECTION('ref_axis',(1.,0.,0.));
#8096=DIRECTION('',(0.,0.,-1.));
#8097=DIRECTION('center_axis',(0.,0.,1.));
#8098=DIRECTION('ref_axis',(1.,0.,0.));
#8099=DIRECTION('',(0.,0.,-1.));
#8100=DIRECTION('center_axis',(0.,0.,1.));
#8101=DIRECTION('ref_axis',(1.,0.,0.));
#8102=DIRECTION('',(0.,0.,-1.));
#8103=DIRECTION('center_axis',(0.,0.,1.));
#8104=DIRECTION('ref_axis',(1.,0.,0.));
#8105=DIRECTION('',(0.,0.,-1.));
#8106=DIRECTION('center_axis',(0.,0.,1.));
#8107=DIRECTION('ref_axis',(1.,0.,0.));
#8108=DIRECTION('',(0.,0.,-1.));
#8109=DIRECTION('center_axis',(0.,0.,1.));
#8110=DIRECTION('ref_axis',(1.,0.,0.));
#8111=DIRECTION('',(0.,0.,-1.));
#8112=DIRECTION('center_axis',(0.,0.,1.));
#8113=DIRECTION('ref_axis',(1.,0.,0.));
#8114=DIRECTION('',(0.,0.,-1.));
#8115=DIRECTION('center_axis',(0.,0.,1.));
#8116=DIRECTION('ref_axis',(1.,0.,0.));
#8117=DIRECTION('',(0.,0.,-1.));
#8118=DIRECTION('center_axis',(0.,0.,1.));
#8119=DIRECTION('ref_axis',(1.,0.,0.));
#8120=DIRECTION('',(0.,0.,-1.));
#8121=DIRECTION('center_axis',(0.,0.,1.));
#8122=DIRECTION('ref_axis',(1.,0.,0.));
#8123=DIRECTION('',(0.,0.,-1.));
#8124=DIRECTION('center_axis',(0.,0.,1.));
#8125=DIRECTION('ref_axis',(1.,0.,0.));
#8126=DIRECTION('',(0.,0.,-1.));
#8127=DIRECTION('center_axis',(0.,0.,1.));
#8128=DIRECTION('ref_axis',(1.,0.,0.));
#8129=DIRECTION('',(0.,0.,-1.));
#8130=DIRECTION('center_axis',(0.,0.,1.));
#8131=DIRECTION('ref_axis',(1.,0.,0.));
#8132=DIRECTION('',(0.,0.,-1.));
#8133=DIRECTION('center_axis',(0.,0.,1.));
#8134=DIRECTION('ref_axis',(1.,0.,0.));
#8135=DIRECTION('',(0.,0.,-1.));
#8136=DIRECTION('center_axis',(0.,0.,1.));
#8137=DIRECTION('ref_axis',(1.,0.,0.));
#8138=DIRECTION('',(0.,0.,-1.));
#8139=DIRECTION('center_axis',(0.,0.,1.));
#8140=DIRECTION('ref_axis',(1.,0.,0.));
#8141=DIRECTION('',(0.,0.,-1.));
#8142=DIRECTION('center_axis',(0.,0.,1.));
#8143=DIRECTION('ref_axis',(1.,0.,0.));
#8144=DIRECTION('',(0.,0.,-1.));
#8145=DIRECTION('center_axis',(0.,0.,1.));
#8146=DIRECTION('ref_axis',(1.,0.,0.));
#8147=DIRECTION('',(0.,0.,-1.));
#8148=DIRECTION('center_axis',(0.,0.,1.));
#8149=DIRECTION('ref_axis',(1.,0.,0.));
#8150=DIRECTION('',(0.,0.,-1.));
#8151=DIRECTION('center_axis',(0.,0.,1.));
#8152=DIRECTION('ref_axis',(1.,0.,0.));
#8153=DIRECTION('',(0.,0.,-1.));
#8154=DIRECTION('center_axis',(0.,0.,1.));
#8155=DIRECTION('ref_axis',(1.,0.,0.));
#8156=DIRECTION('',(0.,0.,-1.));
#8157=DIRECTION('center_axis',(0.,0.,1.));
#8158=DIRECTION('ref_axis',(1.,0.,0.));
#8159=DIRECTION('',(0.,0.,-1.));
#8160=DIRECTION('center_axis',(0.,0.,1.));
#8161=DIRECTION('ref_axis',(1.,0.,0.));
#8162=DIRECTION('',(0.,0.,-1.));
#8163=DIRECTION('center_axis',(0.,0.,1.));
#8164=DIRECTION('ref_axis',(1.,0.,0.));
#8165=DIRECTION('',(0.,0.,-1.));
#8166=DIRECTION('center_axis',(0.,0.,1.));
#8167=DIRECTION('ref_axis',(1.,0.,0.));
#8168=DIRECTION('',(0.,0.,-1.));
#8169=DIRECTION('center_axis',(0.,0.,1.));
#8170=DIRECTION('ref_axis',(1.,0.,0.));
#8171=DIRECTION('',(0.,0.,-1.));
#8172=DIRECTION('center_axis',(0.,0.,1.));
#8173=DIRECTION('ref_axis',(1.,0.,0.));
#8174=DIRECTION('',(0.,0.,-1.));
#8175=DIRECTION('center_axis',(0.,0.,1.));
#8176=DIRECTION('ref_axis',(1.,0.,0.));
#8177=DIRECTION('',(0.,0.,-1.));
#8178=DIRECTION('center_axis',(0.,0.,1.));
#8179=DIRECTION('ref_axis',(1.,-2.42503376499884E-13,0.));
#8180=DIRECTION('',(0.,0.,1.));
#8181=DIRECTION('center_axis',(0.,0.,-1.));
#8182=DIRECTION('ref_axis',(1.,-2.42503376499884E-13,0.));
#8183=DIRECTION('center_axis',(0.,0.,1.));
#8184=DIRECTION('ref_axis',(1.,-2.42503376499884E-13,0.));
#8185=DIRECTION('',(0.,0.,1.));
#8186=DIRECTION('center_axis',(0.,0.,1.));
#8187=DIRECTION('ref_axis',(1.,-2.42503376499884E-13,0.));
#8188=DIRECTION('',(0.,0.,1.));
#8189=DIRECTION('center_axis',(0.,0.,1.));
#8190=DIRECTION('ref_axis',(1.,-2.42503376499884E-13,0.));
#8191=DIRECTION('',(0.,0.,1.));
#8192=DIRECTION('center_axis',(0.,0.,1.));
#8193=DIRECTION('ref_axis',(1.,-2.42503376499884E-13,0.));
#8194=DIRECTION('',(0.,0.,1.));
#8195=DIRECTION('center_axis',(0.,0.,1.));
#8196=DIRECTION('ref_axis',(1.,-2.42503376499884E-13,0.));
#8197=DIRECTION('',(0.,0.,1.));
#8198=DIRECTION('center_axis',(0.,0.,1.));
#8199=DIRECTION('ref_axis',(1.,-2.42503376499884E-13,0.));
#8200=DIRECTION('',(0.,0.,1.));
#8201=DIRECTION('center_axis',(0.,0.,1.));
#8202=DIRECTION('ref_axis',(1.,-2.42503376499884E-13,0.));
#8203=DIRECTION('',(0.,0.,1.));
#8204=DIRECTION('center_axis',(0.,0.,1.));
#8205=DIRECTION('ref_axis',(1.,-2.42503376499884E-13,0.));
#8206=DIRECTION('',(0.,0.,1.));
#8207=DIRECTION('center_axis',(0.,0.,1.));
#8208=DIRECTION('ref_axis',(1.,-2.42503376499884E-13,0.));
#8209=DIRECTION('',(0.,0.,1.));
#8210=DIRECTION('center_axis',(0.,0.,1.));
#8211=DIRECTION('ref_axis',(1.,-2.42503376499884E-13,0.));
#8212=DIRECTION('',(0.,0.,1.));
#8213=DIRECTION('center_axis',(0.,0.,1.));
#8214=DIRECTION('ref_axis',(1.,-2.42503376499884E-13,0.));
#8215=DIRECTION('',(0.,0.,1.));
#8216=DIRECTION('center_axis',(0.,0.,1.));
#8217=DIRECTION('ref_axis',(1.,-2.42503376499884E-13,0.));
#8218=DIRECTION('',(0.,0.,1.));
#8219=DIRECTION('center_axis',(0.,0.,1.));
#8220=DIRECTION('ref_axis',(1.,-2.42503376499884E-13,0.));
#8221=DIRECTION('',(0.,0.,1.));
#8222=DIRECTION('center_axis',(0.,0.,1.));
#8223=DIRECTION('ref_axis',(1.,-2.42503376499884E-13,0.));
#8224=DIRECTION('',(0.,0.,1.));
#8225=DIRECTION('center_axis',(0.,0.,1.));
#8226=DIRECTION('ref_axis',(1.,-2.42503376499884E-13,0.));
#8227=DIRECTION('',(0.,0.,1.));
#8228=DIRECTION('center_axis',(0.,0.,1.));
#8229=DIRECTION('ref_axis',(1.,-2.42503376499884E-13,0.));
#8230=DIRECTION('',(0.,0.,1.));
#8231=DIRECTION('center_axis',(0.,0.,1.));
#8232=DIRECTION('ref_axis',(1.,-2.42503376499884E-13,0.));
#8233=DIRECTION('',(0.,0.,1.));
#8234=DIRECTION('center_axis',(0.,0.,1.));
#8235=DIRECTION('ref_axis',(1.,-2.42503376499884E-13,0.));
#8236=DIRECTION('',(0.,0.,1.));
#8237=DIRECTION('center_axis',(0.,0.,1.));
#8238=DIRECTION('ref_axis',(1.,-2.42503376499884E-13,0.));
#8239=DIRECTION('',(0.,0.,1.));
#8240=DIRECTION('center_axis',(0.,0.,1.));
#8241=DIRECTION('ref_axis',(1.,-2.42503376499884E-13,0.));
#8242=DIRECTION('',(0.,0.,1.));
#8243=DIRECTION('center_axis',(0.,0.,1.));
#8244=DIRECTION('ref_axis',(1.,-2.42503376499884E-13,0.));
#8245=DIRECTION('',(0.,0.,1.));
#8246=DIRECTION('center_axis',(0.,0.,1.));
#8247=DIRECTION('ref_axis',(1.,-2.42503376499884E-13,0.));
#8248=DIRECTION('',(0.,0.,1.));
#8249=DIRECTION('center_axis',(0.,0.,1.));
#8250=DIRECTION('ref_axis',(1.,-2.42503376499884E-13,0.));
#8251=DIRECTION('',(0.,0.,1.));
#8252=DIRECTION('center_axis',(0.,0.,1.));
#8253=DIRECTION('ref_axis',(1.,-2.42503376499884E-13,0.));
#8254=DIRECTION('',(0.,0.,1.));
#8255=DIRECTION('center_axis',(0.,0.,1.));
#8256=DIRECTION('ref_axis',(1.,-2.42503376499884E-13,0.));
#8257=DIRECTION('',(0.,0.,1.));
#8258=DIRECTION('center_axis',(0.,0.,1.));
#8259=DIRECTION('ref_axis',(1.,-2.42503376499884E-13,0.));
#8260=DIRECTION('',(0.,0.,1.));
#8261=DIRECTION('center_axis',(0.,0.,1.));
#8262=DIRECTION('ref_axis',(1.,-2.42503376499884E-13,0.));
#8263=DIRECTION('',(0.,0.,1.));
#8264=DIRECTION('center_axis',(0.,0.,1.));
#8265=DIRECTION('ref_axis',(1.,-2.42503376499884E-13,0.));
#8266=DIRECTION('',(0.,0.,1.));
#8267=DIRECTION('center_axis',(0.,0.,1.));
#8268=DIRECTION('ref_axis',(1.,-2.42503376499884E-13,0.));
#8269=DIRECTION('',(0.,0.,1.));
#8270=DIRECTION('center_axis',(0.,0.,-1.));
#8271=DIRECTION('ref_axis',(1.,0.,0.));
#8272=DIRECTION('center_axis',(0.,0.,-1.));
#8273=DIRECTION('ref_axis',(1.,0.,0.));
#8274=DIRECTION('',(0.707106781186547,8.65956056235493E-17,0.707106781186548));
#8275=DIRECTION('center_axis',(0.,0.,1.));
#8276=DIRECTION('ref_axis',(1.,0.,0.));
#8277=DIRECTION('center_axis',(0.,0.,1.));
#8278=DIRECTION('ref_axis',(1.,-2.42503376499884E-13,0.));
#8279=DIRECTION('center_axis',(0.,0.,-1.));
#8280=DIRECTION('ref_axis',(1.,-2.42503376499884E-13,0.));
#8281=DIRECTION('center_axis',(0.,0.,1.));
#8282=DIRECTION('ref_axis',(1.,0.,0.));
#8283=DIRECTION('center_axis',(-1.92296268638356E-16,-1.,0.));
#8284=DIRECTION('ref_axis',(1.,-1.92296268638356E-16,0.));
#8285=DIRECTION('',(1.,-1.92296268638356E-16,0.));
#8286=DIRECTION('',(0.,0.,1.));
#8287=DIRECTION('',(1.,-1.92296268638356E-16,0.));
#8288=DIRECTION('',(0.,0.,1.));
#8289=DIRECTION('center_axis',(-0.866025403784439,-0.5,0.));
#8290=DIRECTION('ref_axis',(0.5,-0.866025403784439,0.));
#8291=DIRECTION('',(0.5,-0.866025403784439,0.));
#8292=DIRECTION('',(0.,0.,1.));
#8293=DIRECTION('',(0.5,-0.866025403784439,0.));
#8294=DIRECTION('center_axis',(-0.866025403784439,0.5,0.));
#8295=DIRECTION('ref_axis',(-0.5,-0.866025403784439,0.));
#8296=DIRECTION('',(-0.5,-0.866025403784439,0.));
#8297=DIRECTION('',(0.,0.,1.));
#8298=DIRECTION('',(-0.5,-0.866025403784438,0.));
#8299=DIRECTION('center_axis',(1.92296268638356E-16,1.,0.));
#8300=DIRECTION('ref_axis',(-1.,1.92296268638356E-16,0.));
#8301=DIRECTION('',(-1.,1.92296268638356E-16,0.));
#8302=DIRECTION('',(0.,0.,1.));
#8303=DIRECTION('',(-1.,1.92296268638356E-16,0.));
#8304=DIRECTION('center_axis',(0.866025403784439,0.5,0.));
#8305=DIRECTION('ref_axis',(-0.5,0.866025403784439,0.));
#8306=DIRECTION('',(-0.5,0.866025403784439,0.));
#8307=DIRECTION('',(0.,0.,1.));
#8308=DIRECTION('',(-0.5,0.866025403784439,0.));
#8309=DIRECTION('center_axis',(0.866025403784439,-0.5,0.));
#8310=DIRECTION('ref_axis',(0.5,0.866025403784439,0.));
#8311=DIRECTION('',(0.5,0.866025403784439,0.));
#8312=DIRECTION('',(0.5,0.866025403784439,0.));
#8313=DIRECTION('center_axis',(0.,0.,1.));
#8314=DIRECTION('ref_axis',(1.,0.,0.));
#8315=DIRECTION('center_axis',(0.,0.,1.));
#8316=DIRECTION('ref_axis',(1.,0.,0.));
#8317=DIRECTION('center_axis',(0.,0.,1.));
#8318=DIRECTION('ref_axis',(1.,0.,0.));
#8319=DIRECTION('center_axis',(0.,0.,1.));
#8320=DIRECTION('ref_axis',(1.,0.,0.));
#8321=DIRECTION('',(0.,0.,-1.));
#8322=DIRECTION('center_axis',(0.,0.,1.));
#8323=DIRECTION('ref_axis',(1.,0.,0.));
#8324=DIRECTION('center_axis',(0.,0.,1.));
#8325=DIRECTION('ref_axis',(1.,0.,0.));
#8326=DIRECTION('center_axis',(0.,0.,1.));
#8327=DIRECTION('ref_axis',(1.,0.,0.));
#13221=CARTESIAN_POINT('',(0.,0.,0.));
#13222=CARTESIAN_POINT('Origin',(0.,0.,0.));
#13223=CARTESIAN_POINT('',(-0.14652705620645,9.44412402177196E-5,0.0160655045842905));
#13224=CARTESIAN_POINT('',(-0.146479946776166,0.000162062070299865,0.00893449541571059));
#13225=CARTESIAN_POINT('',(-0.14635,-1.79227059055215E-17,0.));
#13226=CARTESIAN_POINT('',(0.0634007094575209,0.131904027763685,0.));
#13227=CARTESIAN_POINT('Ctrl Pts',(-0.14652705620645,9.44412402177196E-5,
0.0160655045842905));
#13228=CARTESIAN_POINT('Ctrl Pts',(-0.146560923555419,0.00502618404349199,
0.0157963945919035));
#13229=CARTESIAN_POINT('Ctrl Pts',(-0.146333578783787,0.00995455679532004,
0.0155272845995164));
#13230=CARTESIAN_POINT('Ctrl Pts',(-0.14583475180505,0.0148550342388422,
0.0152581746071293));
#13231=CARTESIAN_POINT('Ctrl Pts',(-0.140929468554047,0.0630445487404258,
0.0126118447280274));
#13232=CARTESIAN_POINT('Ctrl Pts',(-0.10977174472993,0.108536575508351,
0.0099655148489255));
#13233=CARTESIAN_POINT('Ctrl Pts',(-0.0666135938566871,0.13056551637767,
0.00731918496982359));
#13234=CARTESIAN_POINT('Ctrl Pts',(-0.0268248419338395,0.150874636338504,
0.00487945664654906));
#13235=CARTESIAN_POINT('Ctrl Pts',(0.0231637104697219,0.151241233100125,
0.00243972832327453));
#13236=CARTESIAN_POINT('Ctrl Pts',(0.0635546915223951,0.132092229195826,
-2.16840434497101E-19));
#13237=CARTESIAN_POINT('',(-0.0634007094575146,0.131904027763688,0.));
#13238=CARTESIAN_POINT('Origin',(0.,0.,0.));
#13239=CARTESIAN_POINT('Ctrl Pts',(-0.0634007094575145,0.131904027763688,
-3.88578058618805E-16));
#13240=CARTESIAN_POINT('Ctrl Pts',(-0.107282641710421,0.110811831533068,
0.00264738937425961));
#13241=CARTESIAN_POINT('Ctrl Pts',(-0.139432201149969,0.0662847592091173,
0.00529477874851962));
#13242=CARTESIAN_POINT('Ctrl Pts',(-0.145436119191498,0.0182745223106641,
0.00794216812277962));
#13243=CARTESIAN_POINT('Ctrl Pts',(-0.146186273512714,0.0122759249909008,
0.00827294388708994));
#13244=CARTESIAN_POINT('Ctrl Pts',(-0.146528267289359,0.00622295186417552,
0.00860371965140026));
#13245=CARTESIAN_POINT('Ctrl Pts',(-0.146479946776166,0.000162062070299865,
0.00893449541571059));
#13246=CARTESIAN_POINT('Origin',(0.,0.,0.));
#13247=CARTESIAN_POINT('',(-0.146148830924315,7.59978318484386E-5,0.0660655045842905));
#13248=CARTESIAN_POINT('',(-0.146133770585873,6.2751561688711E-5,0.0589344954157103));
#13249=CARTESIAN_POINT('',(-0.14635,-1.79227059055215E-17,0.));
#13250=CARTESIAN_POINT('Ctrl Pts',(-0.146148830924315,7.59978318484386E-5,
0.0660655045842905));
#13251=CARTESIAN_POINT('Ctrl Pts',(-0.146240443598182,0.0195917497831913,
0.0650077071998482));
#13252=CARTESIAN_POINT('Ctrl Pts',(-0.142607114239671,0.0390747476468127,
0.0639499098154059));
#13253=CARTESIAN_POINT('Ctrl Pts',(-0.135087779856993,0.056920264102034,
0.0628921124309636));
#13254=CARTESIAN_POINT('Ctrl Pts',(-0.116276389754784,0.10156503643559,
0.0602457825518617));
#13255=CARTESIAN_POINT('Ctrl Pts',(-0.073143724514267,0.135961331060063,
0.0575994526727599));
#13256=CARTESIAN_POINT('Ctrl Pts',(-0.025432083612881,0.144366623974243,
0.054953122793658));
#13257=CARTESIAN_POINT('Ctrl Pts',(0.0222795572885053,0.152771916888423,
0.0523067929145561));
#13258=CARTESIAN_POINT('Ctrl Pts',(0.0745701738507606,0.135186208092309,
0.0496604630354541));
#13259=CARTESIAN_POINT('Ctrl Pts',(0.107505148494886,0.0996564726649905,
0.0470141331563522));
#13260=CARTESIAN_POINT('Ctrl Pts',(0.140440123139012,0.0641267372376721,
0.0443678032772503));
#13261=CARTESIAN_POINT('Ctrl Pts',(0.154019455865009,0.010652975179149,
0.0417214733981484));
#13262=CARTESIAN_POINT('Ctrl Pts',(0.14202839331759,-0.0362847016460775,
0.0390751435190465));
#13263=CARTESIAN_POINT('Ctrl Pts',(0.130037330770172,-0.0832223784713041,
0.0364288136399446));
#13264=CARTESIAN_POINT('Ctrl Pts',(0.0924758729493388,-0.123623970063234,
0.0337824837608427));
#13265=CARTESIAN_POINT('Ctrl Pts',(0.0465351214488668,-0.139005253038876,
0.0311361538817407));
#13266=CARTESIAN_POINT('Ctrl Pts',(0.000594369948394902,-0.154386536014517,
0.0284898240026388));
#13267=CARTESIAN_POINT('Ctrl Pts',(-0.0537256752317158,-0.144747510373871,
0.025843494123537));
#13268=CARTESIAN_POINT('Ctrl Pts',(-0.0915592764828275,-0.114484496435928,
0.0231971642444351));
#13269=CARTESIAN_POINT('Ctrl Pts',(-0.125545511528741,-0.0872989822136326,
0.0208199443577202));
#13270=CARTESIAN_POINT('Ctrl Pts',(-0.146227884351973,-0.0434707826450544,
0.0184427244710054));
#13271=CARTESIAN_POINT('Ctrl Pts',(-0.14652705620645,9.44412402177196E-5,
0.0160655045842905));
#13272=CARTESIAN_POINT('Ctrl Pts',(-0.146479946776166,0.000162062070299865,
0.00893449541571059));
#13273=CARTESIAN_POINT('Ctrl Pts',(-0.146141530330399,-0.0422858476614564,
0.0112511090256603));
#13274=CARTESIAN_POINT('Ctrl Pts',(-0.126658161292025,-0.0851220706608281,
0.0135677226356099));
#13275=CARTESIAN_POINT('Ctrl Pts',(-0.0941604943243988,-0.112386678841155,
0.0158843362455596));
#13276=CARTESIAN_POINT('Ctrl Pts',(-0.0570226747722624,-0.143544241621566,
0.0185317256198196));
#13277=CARTESIAN_POINT('Ctrl Pts',(-0.00288875902448078,-0.154365965709432,
0.0211791149940796));
#13278=CARTESIAN_POINT('Ctrl Pts',(0.0434083729543798,-0.140002007265973,
0.0238265043683396));
#13279=CARTESIAN_POINT('Ctrl Pts',(0.0897055049332404,-0.125638048822514,
0.0264738937425996));
#13280=CARTESIAN_POINT('Ctrl Pts',(0.12816585314318,-0.0860884078477292,
0.0291212831168596));
#13281=CARTESIAN_POINT('Ctrl Pts',(0.141191617966992,-0.0394144013492358,
0.0317686724911196));
#13282=CARTESIAN_POINT('Ctrl Pts',(0.154217382790803,0.00725960514925768,
0.0344160618653796));
#13283=CARTESIAN_POINT('Ctrl Pts',(0.141808564228487,0.0610579771714599,
0.0370634512396396));
#13284=CARTESIAN_POINT('Ctrl Pts',(0.109639063769471,0.0973098477439542,
0.0397108406138996));
#13285=CARTESIAN_POINT('Ctrl Pts',(0.0774695633104545,0.133561718316448,
0.0423582299881596));
#13286=CARTESIAN_POINT('Ctrl Pts',(0.0255393809547383,0.152267087439235,
0.0450056193624196));
#13287=CARTESIAN_POINT('Ctrl Pts',(-0.0223595433272462,0.144872892294413,
0.0476530087366796));
#13288=CARTESIAN_POINT('Ctrl Pts',(-0.070258467609231,0.137478697149591,
0.0503003981109396));
#13289=CARTESIAN_POINT('Ctrl Pts',(-0.114126133817484,0.10398493773716,
0.0529477874851996));
#13290=CARTESIAN_POINT('Ctrl Pts',(-0.133871661545403,0.059725601630819,
0.0555951768594596));
#13291=CARTESIAN_POINT('Ctrl Pts',(-0.142173753131161,0.0411165744656389,
0.0567082830448765));
#13292=CARTESIAN_POINT('Ctrl Pts',(-0.146211489678532,0.0206043892842972,
0.0578213892302934));
#13293=CARTESIAN_POINT('Ctrl Pts',(-0.146133770585873,6.2751561688711E-5,
0.0589344954157103));
#13294=CARTESIAN_POINT('Origin',(0.,0.,0.));
#13295=CARTESIAN_POINT('',(-0.146252097264499,-0.000124487410312429,0.116065504584291));
#13296=CARTESIAN_POINT('',(-0.146276374479508,-0.000129480650117819,0.10893449541571));
#13297=CARTESIAN_POINT('',(-0.14635,-1.79227059055215E-17,0.));
#13298=CARTESIAN_POINT('Ctrl Pts',(-0.146252097264499,-0.000124487410312429,
0.116065504584291));
#13299=CARTESIAN_POINT('Ctrl Pts',(-0.145977101830714,0.0338815411246725,
0.114219019807793));
#13300=CARTESIAN_POINT('Ctrl Pts',(-0.134160879762789,0.0680598926014691,
0.112372535031295));
#13301=CARTESIAN_POINT('Ctrl Pts',(-0.112484833627769,0.0939988017516943,
0.110526050254798));
#13302=CARTESIAN_POINT('Ctrl Pts',(-0.0814193359437304,0.131173714423195,
0.107879720375696));
#13303=CARTESIAN_POINT('Ctrl Pts',(-0.0301019434218634,0.151424966146533,
0.105233390496594));
#13304=CARTESIAN_POINT('Ctrl Pts',(0.0179785702873004,0.145483266051774,
0.102587060617492));
#13305=CARTESIAN_POINT('Ctrl Pts',(0.0660590839964643,0.139541565957016,
0.0999407307383904));
#13306=CARTESIAN_POINT('Ctrl Pts',(0.110902718892925,0.107406914044162,
0.0972944008592884));
#13307=CARTESIAN_POINT('Ctrl Pts',(0.131983829661647,0.0637877973597534,
0.0946480709801865));
#13308=CARTESIAN_POINT('Ctrl Pts',(0.15306494043037,0.0201686806753445,
0.0920017411010846));
#13309=CARTESIAN_POINT('Ctrl Pts',(0.150383527071356,-0.0349349007806195,
0.0893554112219828));
#13310=CARTESIAN_POINT('Ctrl Pts',(0.125166930059577,-0.0763010783846813,
0.0867090813428809));
#13311=CARTESIAN_POINT('Ctrl Pts',(0.0999503330477985,-0.117667255988743,
0.084062751463779));
#13312=CARTESIAN_POINT('Ctrl Pts',(0.0521985523832557,-0.145296029740903,
0.081416421584677));
#13313=CARTESIAN_POINT('Ctrl Pts',(0.00376830011669856,-0.146541450754272,
0.0787700917055751));
#13314=CARTESIAN_POINT('Ctrl Pts',(-0.0446619521498586,-0.147786871767642,
0.0761237618264732));
#13315=CARTESIAN_POINT('Ctrl Pts',(-0.09377067601843,-0.122648940042221,
0.0734774319473713));
#13316=CARTESIAN_POINT('Ctrl Pts',(-0.121079980470766,-0.0826333491581908,
0.0708311020682694));
#13317=CARTESIAN_POINT('Ctrl Pts',(-0.137473143648068,-0.0586128871159229,
0.0692425695736098));
#13318=CARTESIAN_POINT('Ctrl Pts',(-0.146011252866834,-0.02923151094855,
0.0676540370789502));
#13319=CARTESIAN_POINT('Ctrl Pts',(-0.146148830924315,7.59978318484386E-5,
0.0660655045842905));
#13320=CARTESIAN_POINT('Ctrl Pts',(-0.146133770585873,6.2751561688711E-5,
0.0589344954157103));
#13321=CARTESIAN_POINT('Ctrl Pts',(-0.146026644150963,-0.0282514289199324,
0.0604687786045534));
#13322=CARTESIAN_POINT('Ctrl Pts',(-0.138100435392092,-0.0566215672018456,
0.0620030617933965));
#13323=CARTESIAN_POINT('Ctrl Pts',(-0.122745086057252,-0.0801407530065182,
0.0635373449822396));
#13324=CARTESIAN_POINT('Ctrl Pts',(-0.0962495935935968,-0.120722858737265,
0.0661847343564996));
#13325=CARTESIAN_POINT('Ctrl Pts',(-0.0476352194187008,-0.146862157398507,
0.0688321237307596));
#13326=CARTESIAN_POINT('Ctrl Pts',(0.00082938917649622,-0.146587691816784,
0.0714795131050196));
#13327=CARTESIAN_POINT('Ctrl Pts',(0.0492939977716932,-0.146313226235061,
0.0741269024792796));
#13328=CARTESIAN_POINT('Ctrl Pts',(0.0976088407871913,-0.119624996410372,
0.0767742918535397));
#13329=CARTESIAN_POINT('Ctrl Pts',(0.123643642180798,-0.0787464320231966,
0.0794216812277997));
#13330=CARTESIAN_POINT('Ctrl Pts',(0.149678443574405,-0.0378678676360213,
0.0820690706020596));
#13331=CARTESIAN_POINT('Ctrl Pts',(0.153433203346121,0.0172010313136401,
0.0847164599763195));
#13332=CARTESIAN_POINT('Ctrl Pts',(0.133187835944515,0.06123527443138,0.0873638493505795));
#13333=CARTESIAN_POINT('Ctrl Pts',(0.11294246854291,0.10526951754912,0.0900112387248395));
#13334=CARTESIAN_POINT('Ctrl Pts',(0.0686969739679828,0.138269104834938,
0.0926586280990997));
#13335=CARTESIAN_POINT('Ctrl Pts',(0.0207181735233275,0.145118849380084,
0.0953060174733597));
#13336=CARTESIAN_POINT('Ctrl Pts',(-0.027260626921328,0.151968593925229,
0.0979534068476197));
#13337=CARTESIAN_POINT('Ctrl Pts',(-0.0789727332357116,0.132668495729702,
0.10060079622188));
#13338=CARTESIAN_POINT('Ctrl Pts',(-0.110731403441959,0.0960588230543748,
0.10324818559614));
#13339=CARTESIAN_POINT('Ctrl Pts',(-0.133469481440122,0.0698475998711364,
0.105143622202663));
#13340=CARTESIAN_POINT('Ctrl Pts',(-0.145979327216774,0.0347634013028336,
0.107039058809187));
#13341=CARTESIAN_POINT('Ctrl Pts',(-0.146276374479508,-0.000129480650117819,
0.10893449541571));
#13342=CARTESIAN_POINT('Origin',(0.,0.,0.));
#13343=CARTESIAN_POINT('',(-0.146589818999335,-3.81787486967988E-6,0.166065504584291));
#13344=CARTESIAN_POINT('',(-0.146589453522336,1.04004190909306E-5,0.15893449541571));
#13345=CARTESIAN_POINT('',(-0.14635,-1.79227059055215E-17,0.));
#13346=CARTESIAN_POINT('Ctrl Pts',(-0.146589818999335,-3.81787486967988E-6,
0.166065504584291));
#13347=CARTESIAN_POINT('Ctrl Pts',(-0.146571339149733,0.0482382848470949,
0.163430332415738));
#13348=CARTESIAN_POINT('Ctrl Pts',(-0.120433071521034,0.0964975486977609,
0.160795160247185));
#13349=CARTESIAN_POINT('Ctrl Pts',(-0.0800107885095625,0.122828684230981,
0.158159988078632));
#13350=CARTESIAN_POINT('Ctrl Pts',(-0.0394173515450545,0.149271309704865,
0.15551365819953));
#13351=CARTESIAN_POINT('Ctrl Pts',(0.0155813181737399,0.153599719825856,
0.152867328320428));
#13352=CARTESIAN_POINT('Ctrl Pts',(0.0598114643267532,0.133832733731537,
0.150220998441327));
#13353=CARTESIAN_POINT('Ctrl Pts',(0.104041610479766,0.114065747637217,
0.147574668562225));
#13354=CARTESIAN_POINT('Ctrl Pts',(0.137503233066998,0.0702033653275883,
0.144928338683123));
#13355=CARTESIAN_POINT('Ctrl Pts',(0.144880420813362,0.0223220882221681,
0.142282008804021));
#13356=CARTESIAN_POINT('Ctrl Pts',(0.152257608559726,-0.0255591888832524,
0.139635678924919));
#13357=CARTESIAN_POINT('Ctrl Pts',(0.133550361465222,-0.077459360784464,
0.136989349045817));
#13358=CARTESIAN_POINT('Ctrl Pts',(0.0973212811704284,-0.109622900294719,
0.134343019166715));
#13359=CARTESIAN_POINT('Ctrl Pts',(0.0610922008756344,-0.141786439804975,
0.131696689287613));
#13360=CARTESIAN_POINT('Ctrl Pts',(0.00734128738055008,-0.154213346924274,
0.129050359408511));
#13361=CARTESIAN_POINT('Ctrl Pts',(-0.0393288211819405,-0.141215634503184,
0.126404029529409));
#13362=CARTESIAN_POINT('Ctrl Pts',(-0.0859989297444312,-0.128217922082094,
0.123757699650308));
#13363=CARTESIAN_POINT('Ctrl Pts',(-0.125588233374328,-0.0897955901206149,
0.121111369771206));
#13364=CARTESIAN_POINT('Ctrl Pts',(-0.139976083766172,-0.043535137330043,
0.118465039892104));
#13365=CARTESIAN_POINT('Ctrl Pts',(-0.144324767489921,-0.0295530571287048,
0.117665194789499));
#13366=CARTESIAN_POINT('Ctrl Pts',(-0.146371217526823,-0.0148549394177889,
0.116865349686895));
#13367=CARTESIAN_POINT('Ctrl Pts',(-0.146252097264499,-0.000124487410312429,
0.116065504584291));
#13368=CARTESIAN_POINT('Ctrl Pts',(-0.146276374479508,-0.000129480650117819,
0.10893449541571));
#13369=CARTESIAN_POINT('Ctrl Pts',(-0.14639421831063,-0.0139720956278579,
0.109686448183447));
#13370=CARTESIAN_POINT('Ctrl Pts',(-0.14458995413065,-0.0277846002915201,
0.110438400951183));
#13371=CARTESIAN_POINT('Ctrl Pts',(-0.140739671041232,-0.041001045008257,
0.11119035371892));
#13372=CARTESIAN_POINT('Ctrl Pts',(-0.127184034336146,-0.0875319932404337,
0.11383774309318));
#13373=CARTESIAN_POINT('Ctrl Pts',(-0.0882675268278623,-0.12667464254966,
0.11648513246744));
#13374=CARTESIAN_POINT('Ctrl Pts',(-0.0418159243469935,-0.140499695546946,
0.1191325218417));
#13375=CARTESIAN_POINT('Ctrl Pts',(0.00463567813387508,-0.154324748544231,
0.12177991121596));
#13376=CARTESIAN_POINT('Ctrl Pts',(0.0586223755873289,-0.142832205229577,
0.12442730059022));
#13377=CARTESIAN_POINT('Ctrl Pts',(0.0954154960694136,-0.111286216216264,
0.12707468996448));
#13378=CARTESIAN_POINT('Ctrl Pts',(0.132208616551499,-0.0797402272029501,
0.12972207933874));
#13379=CARTESIAN_POINT('Ctrl Pts',(0.151808160062214,-0.0281407924909768,
0.132369468712999));
#13380=CARTESIAN_POINT('Ctrl Pts',(0.145236524363737,0.0198768833792122,
0.135016858087259));
#13381=CARTESIAN_POINT('Ctrl Pts',(0.138664888665259,0.0678945592494009,
0.13766424746152));
#13382=CARTESIAN_POINT('Ctrl Pts',(0.105922073757589,0.112330476277805,
0.14031163683578));
#13383=CARTESIAN_POINT('Ctrl Pts',(0.062005973158836,0.132830708741579,
0.14295902621004));
#13384=CARTESIAN_POINT('Ctrl Pts',(0.0180898725600832,0.153330941205352,
0.1456064155843));
#13385=CARTESIAN_POINT('Ctrl Pts',(-0.0369995137297515,0.149895489104495,
0.14825380495856));
#13386=CARTESIAN_POINT('Ctrl Pts',(-0.0780284182758478,0.124097962381086,
0.15090119433282));
#13387=CARTESIAN_POINT('Ctrl Pts',(-0.119057322821944,0.0983004356576776,
0.153548583707079));
#13388=CARTESIAN_POINT('Ctrl Pts',(-0.146025745624302,0.0501408343117172,
0.15619597308134));
#13389=CARTESIAN_POINT('Ctrl Pts',(-0.14658076309025,0.00167873146180186,
0.1588433624556));
#13390=CARTESIAN_POINT('Ctrl Pts',(-0.146587131676737,0.00112264969450139,
0.15887374010897));
#13391=CARTESIAN_POINT('Ctrl Pts',(-0.146590022522527,0.000566528098114988,
0.15890411776234));
#13392=CARTESIAN_POINT('Ctrl Pts',(-0.146589453522336,1.04004190909306E-5,
0.15893449541571));
#13393=CARTESIAN_POINT('Origin',(0.,0.,0.));
#13394=CARTESIAN_POINT('',(-0.146263250741535,0.000126870157254357,0.21606550458429));
#13395=CARTESIAN_POINT('',(-0.146245769975643,0.000123264779366826,0.20893449541571));
#13396=CARTESIAN_POINT('',(-0.14635,-1.79227059055215E-17,0.));
#13397=CARTESIAN_POINT('Ctrl Pts',(-0.146263250741535,0.000126870157254357,
0.21606550458429));
#13398=CARTESIAN_POINT('Ctrl Pts',(-0.146381923100139,0.0144435832128767,
0.215287974902784));
#13399=CARTESIAN_POINT('Ctrl Pts',(-0.144450237714319,0.0287289633064517,
0.214510445221278));
#13400=CARTESIAN_POINT('Ctrl Pts',(-0.140337374518256,0.0423560295890773,
0.213732915539772));
#13401=CARTESIAN_POINT('Ctrl Pts',(-0.126339204386259,0.0887358830222778,
0.21108658566067));
#13402=CARTESIAN_POINT('Ctrl Pts',(-0.0870745347363382,0.127489909020004,
0.208440255781569));
#13403=CARTESIAN_POINT('Ctrl Pts',(-0.0405154226099946,0.140879780169064,
0.205793925902467));
#13404=CARTESIAN_POINT('Ctrl Pts',(0.00604368951634975,0.154269651318124,
0.203147596023365));
#13405=CARTESIAN_POINT('Ctrl Pts',(0.0598972441191175,0.142295367618517,
0.200501266144263));
#13406=CARTESIAN_POINT('Ctrl Pts',(0.0963956219934077,0.110437747119808,
0.197854936265161));
#13407=CARTESIAN_POINT('Ctrl Pts',(0.132893999867697,0.0785801266211,0.195208606386059));
#13408=CARTESIAN_POINT('Ctrl Pts',(0.15203720101351,0.0268391693232909,
0.192562276506957));
#13409=CARTESIAN_POINT('Ctrl Pts',(0.145063081087281,-0.0211024746124516,
0.189915946627855));
#13410=CARTESIAN_POINT('Ctrl Pts',(0.138088961161051,-0.0690441185481943,
0.187269616748753));
#13411=CARTESIAN_POINT('Ctrl Pts',(0.10499752016278,-0.11318644912187,0.184623286869651));
#13412=CARTESIAN_POINT('Ctrl Pts',(0.060935231264163,-0.133324827106958,
0.181976956990549));
#13413=CARTESIAN_POINT('Ctrl Pts',(0.0168729423655461,-0.153463205092045,
0.179330627111448));
#13414=CARTESIAN_POINT('Ctrl Pts',(-0.0381601944334158,-0.149597630488544,
0.176684297232346));
#13415=CARTESIAN_POINT('Ctrl Pts',(-0.0789746466099193,-0.123497437688695,
0.174037967353244));
#13416=CARTESIAN_POINT('Ctrl Pts',(-0.119961184605052,-0.0972871987457574,
0.171380479763593));
#13417=CARTESIAN_POINT('Ctrl Pts',(-0.146608455341797,-0.0486544490602708,
0.168722992173942));
#13418=CARTESIAN_POINT('Ctrl Pts',(-0.146589818999335,-3.81787486967988E-6,
0.166065504584291));
#13419=CARTESIAN_POINT('Ctrl Pts',(-0.146589453522336,1.04004190909306E-5,
0.15893449541571));
#13420=CARTESIAN_POINT('Ctrl Pts',(-0.146540434588914,-0.0478995759235739,
0.1615515071366));
#13421=CARTESIAN_POINT('Ctrl Pts',(-0.120813506558866,-0.0958546957256878,
0.16416851885749));
#13422=CARTESIAN_POINT('Ctrl Pts',(-0.0808500697395765,-0.122278388912248,
0.16678553057838));
#13423=CARTESIAN_POINT('Ctrl Pts',(-0.0404227467934142,-0.149008802082514,
0.16943291995264));
#13424=CARTESIAN_POINT('Ctrl Pts',(0.0145735112284506,-0.153705024069172,
0.1720803093269));
#13425=CARTESIAN_POINT('Ctrl Pts',(0.0589475933459444,-0.134215943447351,
0.17472769870116));
#13426=CARTESIAN_POINT('Ctrl Pts',(0.103321675463438,-0.11472686282553,
0.17737508807542));
#13427=CARTESIAN_POINT('Ctrl Pts',(0.137073581676561,-0.0710524795952304,
0.18002247744968));
#13428=CARTESIAN_POINT('Ctrl Pts',(0.144743205110219,-0.0231979049720499,
0.18266986682394));
#13429=CARTESIAN_POINT('Ctrl Pts',(0.152412828543877,0.024656669651131,
0.1853172561982));
#13430=CARTESIAN_POINT('Ctrl Pts',(0.13400016919807,0.0766914356671922,
0.18796464557246));
#13431=CARTESIAN_POINT('Ctrl Pts',(0.0979391709064228,0.109071797518936,
0.19061203494672));
#13432=CARTESIAN_POINT('Ctrl Pts',(0.0618781726147763,0.141452159370678,
0.19325942432098));
#13433=CARTESIAN_POINT('Ctrl Pts',(0.00816883537729064,0.154178117058104,
0.195906813695239));
#13434=CARTESIAN_POINT('Ctrl Pts',(-0.0385872054932313,0.1414205281901,
0.198554203069499));
#13435=CARTESIAN_POINT('Ctrl Pts',(-0.0853432463637543,0.128662939322095,
0.201201592443759));
#13436=CARTESIAN_POINT('Ctrl Pts',(-0.125145990867313,0.0904218038986596,
0.20384898181802));
#13437=CARTESIAN_POINT('Ctrl Pts',(-0.139763737461459,0.0442135263146365,
0.20649637119228));
#13438=CARTESIAN_POINT('Ctrl Pts',(-0.144251162244238,0.030028291356252,
0.207309079266757));
#13439=CARTESIAN_POINT('Ctrl Pts',(-0.146365162502875,0.0150922359825044,
0.208121787341234));
#13440=CARTESIAN_POINT('Ctrl Pts',(-0.146245769975643,0.000123264779366826,
0.20893449541571));
#13441=CARTESIAN_POINT('Origin',(0.,0.,0.));
#13442=CARTESIAN_POINT('',(-0.146142672279203,-7.01165389862951E-5,0.266065504584291));
#13443=CARTESIAN_POINT('',(-0.146150215784492,-7.74481165901552E-5,0.258934495415711));
#13444=CARTESIAN_POINT('',(-0.14635,-1.79227059055215E-17,0.));
#13445=CARTESIAN_POINT('Ctrl Pts',(-0.146142672279203,-7.01165389862951E-5,
0.266065504584291));
#13446=CARTESIAN_POINT('Ctrl Pts',(-0.146017527260215,0.028828671850369,
0.264499287510729));
#13447=CARTESIAN_POINT('Ctrl Pts',(-0.137733916992107,0.0577936173630845,
0.262933070437168));
#13448=CARTESIAN_POINT('Ctrl Pts',(-0.121770841384076,0.0816117278206753,
0.261366853363607));
#13449=CARTESIAN_POINT('Ctrl Pts',(-0.0947991242083451,0.121855560193383,
0.258720523484505));
#13450=CARTESIAN_POINT('Ctrl Pts',(-0.0459036471244643,0.147405924851771,
0.256074193605403));
#13451=CARTESIAN_POINT('Ctrl Pts',(0.0025353607453442,0.146568017913755,
0.253427863726301));
#13452=CARTESIAN_POINT('Ctrl Pts',(0.050974368615152,0.145730110975738,
0.250781533847199));
#13453=CARTESIAN_POINT('Ctrl Pts',(0.0989569072708876,0.118503932441319,
0.248135203968097));
#13454=CARTESIAN_POINT('Ctrl Pts',(0.124520613871998,0.0773513325689396,
0.245488874088995));
#13455=CARTESIAN_POINT('Ctrl Pts',(0.150084320473109,0.0361987326965595,
0.242842544209893));
#13456=CARTESIAN_POINT('Ctrl Pts',(0.153229195019594,-0.0188802885137813,
0.240196214330791));
#13457=CARTESIAN_POINT('Ctrl Pts',(0.132515778953886,-0.0626751965094481,
0.237549884451689));
#13458=CARTESIAN_POINT('Ctrl Pts',(0.111802362888177,-0.106470104505115,
0.234903554572587));
#13459=CARTESIAN_POINT('Ctrl Pts',(0.0672306562102751,-0.138980899286108,
0.232257224693486));
#13460=CARTESIAN_POINT('Ctrl Pts',(0.0192018303028616,-0.145326878595667,
0.229610894814384));
#13461=CARTESIAN_POINT('Ctrl Pts',(-0.0288269956045516,-0.151672857905225,
0.226964564935282));
#13462=CARTESIAN_POINT('Ctrl Pts',(-0.0803129407414762,-0.131854021743351,
0.22431823505618));
#13463=CARTESIAN_POINT('Ctrl Pts',(-0.111690078002902,-0.0949417632280756,
0.221671905177078));
#13464=CARTESIAN_POINT('Ctrl Pts',(-0.133848162215005,-0.0688748557907962,
0.219803104979482));
#13465=CARTESIAN_POINT('Ctrl Pts',(-0.145978020566425,-0.0342834897603843,
0.217934304781886));
#13466=CARTESIAN_POINT('Ctrl Pts',(-0.146263250741535,0.000126870157254357,
0.21606550458429));
#13467=CARTESIAN_POINT('Ctrl Pts',(-0.146245769975643,0.000123264779366826,
0.20893449541571));
#13468=CARTESIAN_POINT('Ctrl Pts',(-0.145976242399967,-0.03366905549635,
0.210769176715493));
#13469=CARTESIAN_POINT('Ctrl Pts',(-0.134324750276972,-0.067629123606452,
0.212603858015276));
#13470=CARTESIAN_POINT('Ctrl Pts',(-0.112902327433,-0.0934976078712483,
0.214438539315059));
#13471=CARTESIAN_POINT('Ctrl Pts',(-0.0819904221256615,-0.130825044728502,
0.217085928689319));
#13472=CARTESIAN_POINT('Ctrl Pts',(-0.0307338628262512,-0.151304498698398,
0.21973331806358));
#13473=CARTESIAN_POINT('Ctrl Pts',(0.0173892134168267,-0.145555327884408,
0.22238070743784));
#13474=CARTESIAN_POINT('Ctrl Pts',(0.0655122896599044,-0.139806157070418,
0.2250280968121));
#13475=CARTESIAN_POINT('Ctrl Pts',(0.11050188284665,-0.107828361472542,
0.22767548618636));
#13476=CARTESIAN_POINT('Ctrl Pts',(0.131750448317205,-0.0642694140823833,
0.23032287556062));
#13477=CARTESIAN_POINT('Ctrl Pts',(0.15299901378776,-0.020710466692225,
0.232970264934879));
#13478=CARTESIAN_POINT('Ctrl Pts',(0.150506551542124,0.0344296324902152,
0.23561765430914));
#13479=CARTESIAN_POINT('Ctrl Pts',(0.125414737320077,0.0758938856636754,
0.2382650436834));
#13480=CARTESIAN_POINT('Ctrl Pts',(0.10032292309803,0.117358138837136,0.24091243305766));
#13481=CARTESIAN_POINT('Ctrl Pts',(0.0526317568995709,0.145146546001616,
0.24355982243192));
#13482=CARTESIAN_POINT('Ctrl Pts',(0.00418624259284972,0.146530589268381,
0.24620721180618));
#13483=CARTESIAN_POINT('Ctrl Pts',(-0.0442592717138715,0.147914632535146,
0.24885460118044));
#13484=CARTESIAN_POINT('Ctrl Pts',(-0.0934591341288551,0.122894311904195,
0.2515019905547));
#13485=CARTESIAN_POINT('Ctrl Pts',(-0.120877280418781,0.082930219442967,
0.25414937992896));
#13486=CARTESIAN_POINT('Ctrl Pts',(-0.137396572682769,0.0588520590724165,
0.255744418424543));
#13487=CARTESIAN_POINT('Ctrl Pts',(-0.146009100715185,0.0293493086505574,
0.257339456920127));
#13488=CARTESIAN_POINT('Ctrl Pts',(-0.146150215784492,-7.74481165901552E-5,
0.258934495415711));
#13489=CARTESIAN_POINT('Origin',(0.,0.,0.));
#13490=CARTESIAN_POINT('',(-0.146519404976022,-8.97763884284003E-5,0.316065504584291));
#13491=CARTESIAN_POINT('',(-0.146528765763263,-8.45393868379275E-5,0.30893449541571));
#13492=CARTESIAN_POINT('',(-0.14635,-1.79227059055215E-17,0.));
#13493=CARTESIAN_POINT('Ctrl Pts',(-0.146519404976022,-8.97763884284003E-5,
0.316065504584291));
#13494=CARTESIAN_POINT('Ctrl Pts',(-0.146208092107557,0.043076445171776,
0.313710600118674));
#13495=CARTESIAN_POINT('Ctrl Pts',(-0.125958424314353,0.0864965766126209,
0.311355695653057));
#13496=CARTESIAN_POINT('Ctrl Pts',(-0.0925183485457987,0.1137056160074,
0.309000791187441));
#13497=CARTESIAN_POINT('Ctrl Pts',(-0.0549399784004991,0.144281843189175,
0.306354461308339));
#13498=CARTESIAN_POINT('Ctrl Pts',(-0.00070450021881692,0.154386382754941,
0.303708131429237));
#13499=CARTESIAN_POINT('Ctrl Pts',(0.0453636543616171,0.139394227973128,
0.301061801550135));
#13500=CARTESIAN_POINT('Ctrl Pts',(0.0914318089420511,0.124402073191315,
0.298415471671033));
#13501=CARTESIAN_POINT('Ctrl Pts',(0.129332639921237,0.0843132240619223,
0.295769141791931));
#13502=CARTESIAN_POINT('Ctrl Pts',(0.141718340675246,0.0374769775398043,
0.293122811912829));
#13503=CARTESIAN_POINT('Ctrl Pts',(0.154104041429255,-0.00935926898231351,
0.290476482033727));
#13504=CARTESIAN_POINT('Ctrl Pts',(0.140974611958088,-0.0629429128971569,
0.287830152154626));
#13505=CARTESIAN_POINT('Ctrl Pts',(0.108339598692885,-0.0987478773661917,
0.285183822275524));
#13506=CARTESIAN_POINT('Ctrl Pts',(0.0757045854276824,-0.134552841835227,
0.282537492396422));
#13507=CARTESIAN_POINT('Ctrl Pts',(0.0235639883684441,-0.152579126858453,
0.27989116251732));
#13508=CARTESIAN_POINT('Ctrl Pts',(-0.0242166208952047,-0.144575818177467,
0.277244832638218));
#13509=CARTESIAN_POINT('Ctrl Pts',(-0.0719972301588528,-0.136572509496481,
0.274598502759116));
#13510=CARTESIAN_POINT('Ctrl Pts',(-0.115417851626912,-0.102539607111283,
0.271952172880014));
#13511=CARTESIAN_POINT('Ctrl Pts',(-0.13460418372715,-0.0580545058751705,
0.269305843000912));
#13512=CARTESIAN_POINT('Ctrl Pts',(-0.142435181350113,-0.0398976888130428,
0.268225730195372));
#13513=CARTESIAN_POINT('Ctrl Pts',(-0.146228976240411,-0.0199996345674016,
0.267145617389831));
#13514=CARTESIAN_POINT('Ctrl Pts',(-0.146142672279203,-7.01165389862951E-5,
0.266065504584291));
#13515=CARTESIAN_POINT('Ctrl Pts',(-0.146150215784492,-7.74481165901552E-5,
0.258934495415711));
#13516=CARTESIAN_POINT('Ctrl Pts',(-0.146243318595233,-0.0194921979337541,
0.259986846294387));
#13517=CARTESIAN_POINT('Ctrl Pts',(-0.142648899141753,-0.0388738684647463,
0.261039197173063));
#13518=CARTESIAN_POINT('Ctrl Pts',(-0.135204796371803,-0.0566427511368837,
0.26209154805174));
#13519=CARTESIAN_POINT('Ctrl Pts',(-0.116477735870028,-0.101343764964001,
0.264738937426));
#13520=CARTESIAN_POINT('Ctrl Pts',(-0.0733871847016099,-0.135837928326728,
0.26738632680026));
#13521=CARTESIAN_POINT('Ctrl Pts',(-0.0256708287318585,-0.144325142544676,
0.27003371617452));
#13522=CARTESIAN_POINT('Ctrl Pts',(0.0220455272378925,-0.152812356762624,
0.27268110554878));
#13523=CARTESIAN_POINT('Ctrl Pts',(0.0743876880089763,-0.135292621835792,
0.27532849492304));
#13524=CARTESIAN_POINT('Ctrl Pts',(0.10738025529095,-0.0997908762961729,
0.2779758842973));
#13525=CARTESIAN_POINT('Ctrl Pts',(0.140372822572925,-0.0642891307565533,
0.280623273671559));
#13526=CARTESIAN_POINT('Ctrl Pts',(0.154015796365789,-0.010805374604146,
0.283270663045819));
#13527=CARTESIAN_POINT('Ctrl Pts',(0.142059993874458,0.0361620845457957,
0.285918052420079));
#13528=CARTESIAN_POINT('Ctrl Pts',(0.130104191383128,0.0831295436957373,
0.288565441794339));
#13529=CARTESIAN_POINT('Ctrl Pts',(0.0925496126076039,0.123580705843213,
0.291212831168599));
#13530=CARTESIAN_POINT('Ctrl Pts',(0.0465981836912963,0.138986860871753,
0.29386022054286));
#13531=CARTESIAN_POINT('Ctrl Pts',(0.000646754774988913,0.154393015900293,
0.296507609917119));
#13532=CARTESIAN_POINT('Ctrl Pts',(-0.0537015242821025,0.144754163809898,
0.29915499929138));
#13533=CARTESIAN_POINT('Ctrl Pts',(-0.0915523499663989,0.114485393976436,
0.30180238866564));
#13534=CARTESIAN_POINT('Ctrl Pts',(-0.125542580994678,0.0873038870745135,
0.30417975758233));
#13535=CARTESIAN_POINT('Ctrl Pts',(-0.146229051243382,0.0434861464246214,
0.30655712649902));
#13536=CARTESIAN_POINT('Ctrl Pts',(-0.146528765763263,-8.45393868379275E-5,
0.30893449541571));
#13537=CARTESIAN_POINT('Origin',(0.,0.,0.));
#13538=CARTESIAN_POINT('',(-0.146416087288192,0.000126442170093593,0.366065504584291));
#13539=CARTESIAN_POINT('',(-0.146408012399712,0.000128195943346294,0.358934495415711));
#13540=CARTESIAN_POINT('',(-0.14635,-1.79227059055215E-17,0.));
#13541=CARTESIAN_POINT('Ctrl Pts',(-0.146416087288192,0.000126442170093593,
0.366065504584291));
#13542=CARTESIAN_POINT('Ctrl Pts',(-0.146499294961499,0.00925816812376314,
0.365568242605721));
#13543=CARTESIAN_POINT('Ctrl Pts',(-0.145718277739785,0.0183757049974218,
0.365070980627151));
#13544=CARTESIAN_POINT('Ctrl Pts',(-0.144021710151773,0.0273195705351122,
0.364573718648581));
#13545=CARTESIAN_POINT('Ctrl Pts',(-0.134992913071845,0.0749170536065741,
0.361927388769479));
#13546=CARTESIAN_POINT('Ctrl Pts',(-0.100034284522917,0.117595890322328,
0.359281058890377));
#13547=CARTESIAN_POINT('Ctrl Pts',(-0.0551469387876206,0.135821305661589,
0.356634729011275));
#13548=CARTESIAN_POINT('Ctrl Pts',(-0.0102595930523245,0.15404672100085,
0.353988399132173));
#13549=CARTESIAN_POINT('Ctrl Pts',(0.0445564698693406,0.147818714963618,
0.351342069253072));
#13550=CARTESIAN_POINT('Ctrl Pts',(0.0842110755700531,0.119987943896873,
0.34869573937397));
#13551=CARTESIAN_POINT('Ctrl Pts',(0.123865681270766,0.0921571728301272,
0.346049409494868));
#13552=CARTESIAN_POINT('Ctrl Pts',(0.148358829750526,0.0427236367338667,
0.343403079615766));
#13553=CARTESIAN_POINT('Ctrl Pts',(0.146479621605269,-0.00568615719458776,
0.340756749736664));
#13554=CARTESIAN_POINT('Ctrl Pts',(0.144600413460012,-0.0540959511230416,
0.338110419857562));
#13555=CARTESIAN_POINT('Ctrl Pts',(0.116348848689739,-0.101482002883689,
0.33546408997846));
#13556=CARTESIAN_POINT('Ctrl Pts',(0.0746561129649502,-0.126154971072205,
0.332817760099358));
#13557=CARTESIAN_POINT('Ctrl Pts',(0.0329633772401616,-0.150827939260721,
0.330171430220256));
#13558=CARTESIAN_POINT('Ctrl Pts',(-0.0221705294391424,-0.152787823877104,
0.327525100341154));
#13559=CARTESIAN_POINT('Ctrl Pts',(-0.0655099505772086,-0.131137554898038,
0.324878770462052));
#13560=CARTESIAN_POINT('Ctrl Pts',(-0.108849371715275,-0.109487285918972,
0.322232440582951));
#13561=CARTESIAN_POINT('Ctrl Pts',(-0.140394307312104,-0.0642268633444555,
0.319586110703849));
#13562=CARTESIAN_POINT('Ctrl Pts',(-0.14570614405606,-0.0160726946583056,
0.316939780824747));
#13563=CARTESIAN_POINT('Ctrl Pts',(-0.146291106736525,-0.0107697471190636,
0.316648355411261));
#13564=CARTESIAN_POINT('Ctrl Pts',(-0.146557930734812,-0.0054317060295066,
0.316356929997776));
#13565=CARTESIAN_POINT('Ctrl Pts',(-0.146519404976022,-8.97763884284003E-5,
0.316065504584291));
#13566=CARTESIAN_POINT('Ctrl Pts',(-0.146528765763263,-8.45393868379275E-5,
0.30893449541571));
#13567=CARTESIAN_POINT('Ctrl Pts',(-0.146562807199252,-0.00503327764821679,
0.30920451587328));
#13568=CARTESIAN_POINT('Ctrl Pts',(-0.14633385314783,-0.00997882882536714,
0.30947453633085));
#13569=CARTESIAN_POINT('Ctrl Pts',(-0.145831525524598,-0.0148964553326841,
0.309744556788419));
#13570=CARTESIAN_POINT('Ctrl Pts',(-0.140906503086998,-0.0631108472318147,
0.312391946162679));
#13571=CARTESIAN_POINT('Ctrl Pts',(-0.109703085900295,-0.108640943453547,
0.31503933553694));
#13572=CARTESIAN_POINT('Ctrl Pts',(-0.0665140418604196,-0.13063162118607,
0.3176867249112));
#13573=CARTESIAN_POINT('Ctrl Pts',(-0.0233249978205455,-0.152622298918592,
0.32033411428546));
#13574=CARTESIAN_POINT('Ctrl Pts',(0.0318496730725009,-0.151073558161906,
0.322981503659719));
#13575=CARTESIAN_POINT('Ctrl Pts',(0.0737371373950496,-0.126694801736668,
0.325628893033979));
#13576=CARTESIAN_POINT('Ctrl Pts',(0.115624601717599,-0.10231604531143,
0.328276282408239));
#13577=CARTESIAN_POINT('Ctrl Pts',(0.144224859469651,-0.0551072732176397,
0.3309236717825));
#13578=CARTESIAN_POINT('Ctrl Pts',(0.146437523492708,-0.0066925280449658,
0.33357106115676));
#13579=CARTESIAN_POINT('Ctrl Pts',(0.148650187515766,0.0417222171277085,
0.33621845053102));
#13580=CARTESIAN_POINT('Ctrl Pts',(0.124475257809829,0.0913429353792657,
0.33886583990528));
#13581=CARTESIAN_POINT('Ctrl Pts',(0.0849860939726622,0.119440788885456,
0.34151322927954));
#13582=CARTESIAN_POINT('Ctrl Pts',(0.0454969301354961,0.147538642391646,
0.344160618653799));
#13583=CARTESIAN_POINT('Ctrl Pts',(-0.00930646783289898,0.154113631152469,
0.346808008028059));
#13584=CARTESIAN_POINT('Ctrl Pts',(-0.0543213285795041,0.136154072578339,
0.349455397402319));
#13585=CARTESIAN_POINT('Ctrl Pts',(-0.0993361893261098,0.11819451400421,
0.352102786776579));
#13586=CARTESIAN_POINT('Ctrl Pts',(-0.134562512850926,0.0757004080951257,
0.35475017615084));
#13587=CARTESIAN_POINT('Ctrl Pts',(-0.143864833510727,0.0281362381501331,
0.3573975655251));
#13588=CARTESIAN_POINT('Ctrl Pts',(-0.145664973529558,0.0189318504589563,
0.357909875488637));
#13589=CARTESIAN_POINT('Ctrl Pts',(-0.146494308508217,0.00953759842677947,
0.358422185452174));
#13590=CARTESIAN_POINT('Ctrl Pts',(-0.146408012399712,0.000128195943346294,
0.358934495415711));
#13591=CARTESIAN_POINT('Origin',(0.,0.,0.));
#13592=CARTESIAN_POINT('',(-0.146110491840834,1.12683595067248E-5,0.416065504584291));
#13593=CARTESIAN_POINT('',(-0.146109756335714,8.81622270207575E-6,0.40893449541571));
#13594=CARTESIAN_POINT('',(-0.14635,-1.79227059055215E-17,0.));
#13595=CARTESIAN_POINT('Ctrl Pts',(-0.146110491840834,1.12683595067248E-5,
0.416065504584291));
#13596=CARTESIAN_POINT('Ctrl Pts',(-0.146126798292857,0.0237518011834032,
0.414779555213666));
#13597=CARTESIAN_POINT('Ctrl Pts',(-0.140669750958991,0.0474852665485293,
0.413493605843041));
#13598=CARTESIAN_POINT('Ctrl Pts',(-0.129698698951591,0.0683144158983218,
0.412207656472415));
#13599=CARTESIAN_POINT('Ctrl Pts',(-0.107121587134001,0.111178312051432,
0.409561326593314));
#13600=CARTESIAN_POINT('Ctrl Pts',(-0.0611933749717542,0.141742803557285,
0.406914996714211));
#13601=CARTESIAN_POINT('Ctrl Pts',(-0.0129361277491455,0.146018041789781,
0.40426866683511));
#13602=CARTESIAN_POINT('Ctrl Pts',(0.0353211194734639,0.150293280022276,
0.401622336956008));
#13603=CARTESIAN_POINT('Ctrl Pts',(0.0859074017564354,0.128279264981412,
0.398976007076906));
#13604=CARTESIAN_POINT('Ctrl Pts',(0.115668581836909,0.0900521576926538,
0.396329677197804));
#13605=CARTESIAN_POINT('Ctrl Pts',(0.145429761917382,0.0518250504038959,
0.393683347318702));
#13606=CARTESIAN_POINT('Ctrl Pts',(0.154365839795359,-0.0026151491327561,
0.3910370174396));
#13607=CARTESIAN_POINT('Ctrl Pts',(0.138386632036901,-0.0483503050946702,
0.388390687560498));
#13608=CARTESIAN_POINT('Ctrl Pts',(0.122407424278443,-0.094085461056585,
0.385744357681396));
#13609=CARTESIAN_POINT('Ctrl Pts',(0.0815129308835505,-0.131115573443762,
0.383098027802294));
#13610=CARTESIAN_POINT('Ctrl Pts',(0.0344212048624006,-0.142491377230642,
0.380451697923192));
#13611=CARTESIAN_POINT('Ctrl Pts',(-0.0126705211587486,-0.153867181017521,
0.37780536804409));
#13612=CARTESIAN_POINT('Ctrl Pts',(-0.0659594798061549,-0.139588676204105,
0.375159038164988));
#13613=CARTESIAN_POINT('Ctrl Pts',(-0.101054476324393,-0.106191359083811,
0.372512708285887));
#13614=CARTESIAN_POINT('Ctrl Pts',(-0.129554902927378,-0.0790696072742943,
0.370363640385355));
#13615=CARTESIAN_POINT('Ctrl Pts',(-0.146056480184715,-0.0393390709180539,
0.368214572484823));
#13616=CARTESIAN_POINT('Ctrl Pts',(-0.146416087288192,0.000126442170093593,
0.366065504584291));
#13617=CARTESIAN_POINT('Ctrl Pts',(-0.146408012399712,0.000128195943346294,
0.358934495415711));
#13618=CARTESIAN_POINT('Ctrl Pts',(-0.146048368712081,-0.0390859965171687,
0.361069574826434));
#13619=CARTESIAN_POINT('Ctrl Pts',(-0.1297855810823,-0.0785633296797545,
0.363204654237157));
#13620=CARTESIAN_POINT('Ctrl Pts',(-0.101613371150224,-0.105657280969165,
0.36533973364788));
#13621=CARTESIAN_POINT('Ctrl Pts',(-0.066681270335132,-0.139252396162569,
0.36798712302214));
#13622=CARTESIAN_POINT('Ctrl Pts',(-0.0134387509101597,-0.153808392568477,
0.370634512396399));
#13623=CARTESIAN_POINT('Ctrl Pts',(0.0337263783221333,-0.142657876135818,
0.373281901770659));
#13624=CARTESIAN_POINT('Ctrl Pts',(0.0808915075544263,-0.13150735970316,
0.375929291144919));
#13625=CARTESIAN_POINT('Ctrl Pts',(0.12197924659404,-0.0946503304319347,
0.378576680519179));
#13626=CARTESIAN_POINT('Ctrl Pts',(0.138169300408926,-0.0489692009616054,
0.38122406989344));
#13627=CARTESIAN_POINT('Ctrl Pts',(0.154359354223812,-0.00328807149127619,
0.3838714592677));
#13628=CARTESIAN_POINT('Ctrl Pts',(0.14565172281397,0.0512171581781573,
0.38651884864196));
#13629=CARTESIAN_POINT('Ctrl Pts',(0.11603494864959,0.0895802930905963,
0.38916623801622));
#13630=CARTESIAN_POINT('Ctrl Pts',(0.0864181744852101,0.127943428003035,
0.39181362739048));
#13631=CARTESIAN_POINT('Ctrl Pts',(0.0358922575662923,0.15016446815848,
0.394461016764739));
#13632=CARTESIAN_POINT('Ctrl Pts',(-0.0123993367959677,0.146065035738641,
0.397108406138999));
#13633=CARTESIAN_POINT('Ctrl Pts',(-0.0606909311582276,0.141965603318802,
0.399755795513259));
#13634=CARTESIAN_POINT('Ctrl Pts',(-0.106748202963829,0.111545698323679,
0.40240318488752));
#13635=CARTESIAN_POINT('Ctrl Pts',(-0.129474555904152,0.0687391998188283,
0.40505057426178));
#13636=CARTESIAN_POINT('Ctrl Pts',(-0.140588317483115,0.0478057390183907,
0.406345214646423));
#13637=CARTESIAN_POINT('Ctrl Pts',(-0.146122589096428,0.0239100770892618,
0.407639855031067));
#13638=CARTESIAN_POINT('Ctrl Pts',(-0.146109756335714,8.81622270207575E-6,
0.40893449541571));
#13639=CARTESIAN_POINT('Origin',(0.,0.,0.));
#13640=CARTESIAN_POINT('',(-0.146374718215768,-0.000132229735885947,0.466065504584291));
#13641=CARTESIAN_POINT('',(-0.146375609273197,-0.000132432188538665,0.458934495415711));
#13642=CARTESIAN_POINT('',(-0.14635,-1.79227059055215E-17,0.));
#13643=CARTESIAN_POINT('Ctrl Pts',(-0.146374718215768,-0.000132229735885947,
0.466065504584291));
#13644=CARTESIAN_POINT('Ctrl Pts',(-0.146022504084922,0.0379941335185874,
0.46399086782161));
#13645=CARTESIAN_POINT('Ctrl Pts',(-0.130761950520226,0.0763703265456945,
0.46191623105893));
#13646=CARTESIAN_POINT('Ctrl Pts',(-0.103994021541854,0.103314352404769,
0.45984159429625));
#13647=CARTESIAN_POINT('Ctrl Pts',(-0.0698498419286355,0.137683154682254,
0.457195264417148));
#13648=CARTESIAN_POINT('Ctrl Pts',(-0.0169824611430249,0.153451124186949,
0.454548934538046));
#13649=CARTESIAN_POINT('Ctrl Pts',(0.030409888879481,0.143401013202843,
0.451902604658944));
#13650=CARTESIAN_POINT('Ctrl Pts',(0.0778022389019875,0.133350902218736,
0.449256274779842));
#13651=CARTESIAN_POINT('Ctrl Pts',(0.119719558161389,0.0974827107458278,
0.44660994490074));
#13652=CARTESIAN_POINT('Ctrl Pts',(0.136975630157447,0.0522138743269898,
0.443963615021638));
#13653=CARTESIAN_POINT('Ctrl Pts',(0.154231702153504,0.00694503790815254,
0.441317285142536));
#13654=CARTESIAN_POINT('Ctrl Pts',(0.146826526886218,-0.0477244434566137,
0.438670955263434));
#13655=CARTESIAN_POINT('Ctrl Pts',(0.118149569579287,-0.0867714880447125,
0.436024625384332));
#13656=CARTESIAN_POINT('Ctrl Pts',(0.0894726122723542,-0.125818532632812,
0.43337829550523));
#13657=CARTESIAN_POINT('Ctrl Pts',(0.0395238729257754,-0.149243140444243,
0.430731965626129));
#13658=CARTESIAN_POINT('Ctrl Pts',(-0.00883432462988853,-0.146323499949933,
0.428085635747027));
#13659=CARTESIAN_POINT('Ctrl Pts',(-0.0571925221855517,-0.143403859455623,
0.425439305867925));
#13660=CARTESIAN_POINT('Ctrl Pts',(-0.1039601779503,-0.114139970655572,
0.422792975988823));
#13661=CARTESIAN_POINT('Ctrl Pts',(-0.127731000096207,-0.0719263758553634,
0.420146646109721));
#13662=CARTESIAN_POINT('Ctrl Pts',(-0.139950702323481,-0.0502259249733931,
0.418786265601244));
#13663=CARTESIAN_POINT('Ctrl Pts',(-0.146093241566443,-0.0251033736724598,
0.417425885092767));
#13664=CARTESIAN_POINT('Ctrl Pts',(-0.146110491840834,1.12683595067248E-5,
0.416065504584291));
#13665=CARTESIAN_POINT('Ctrl Pts',(-0.146109756335714,8.81622270207575E-6,
0.40893449541571));
#13666=CARTESIAN_POINT('Ctrl Pts',(-0.146096347589706,-0.0249652282079418,
0.410287244405327));
#13667=CARTESIAN_POINT('Ctrl Pts',(-0.140026707259891,-0.049945385460595,
0.411639993394943));
#13668=CARTESIAN_POINT('Ctrl Pts',(-0.127937780377622,-0.0715588049813403,
0.412992742384559));
#13669=CARTESIAN_POINT('Ctrl Pts',(-0.104279217835726,-0.113857219262079,
0.415640131758819));
#13670=CARTESIAN_POINT('Ctrl Pts',(-0.0575666586768896,-0.14326095580898,
0.41828752113308));
#13671=CARTESIAN_POINT('Ctrl Pts',(-0.00919685447762893,-0.146301592903247,
0.42093491050734));
#13672=CARTESIAN_POINT('Ctrl Pts',(0.039172949721632,-0.149342229997515,
0.4235822998816));
#13673=CARTESIAN_POINT('Ctrl Pts',(0.089199998961318,-0.126019767639148,
0.426229689255859));
#13674=CARTESIAN_POINT('Ctrl Pts',(0.117969334952632,-0.0870170915920772,
0.428877078630119));
#13675=CARTESIAN_POINT('Ctrl Pts',(0.146738670943946,-0.0480144155450057,
0.431524468004379));
#13676=CARTESIAN_POINT('Ctrl Pts',(0.154250293686888,0.00666847419077017,
0.43417185737864));
#13677=CARTESIAN_POINT('Ctrl Pts',(0.137063494116028,0.051984005222912,
0.4368192467529));
#13678=CARTESIAN_POINT('Ctrl Pts',(0.119876694545168,0.0972995362550541,
0.43946663612716));
#13679=CARTESIAN_POINT('Ctrl Pts',(0.0779914726605056,0.133247708583562,
0.442114025501419));
#13680=CARTESIAN_POINT('Ctrl Pts',(0.0305934116013849,0.143362412733947,
0.444761414875679));
#13681=CARTESIAN_POINT('Ctrl Pts',(-0.0168046494577345,0.153477116884331,
0.447408804249939));
#13682=CARTESIAN_POINT('Ctrl Pts',(-0.0697155496913122,0.137758352856595,
0.4500561936242));
#13683=CARTESIAN_POINT('Ctrl Pts',(-0.103903378920715,0.103406122000434,
0.45270358299846));
#13684=CARTESIAN_POINT('Ctrl Pts',(-0.130724942802416,0.0764555792150183,
0.45478055380421));
#13685=CARTESIAN_POINT('Ctrl Pts',(-0.146022533856355,0.0380362146017157,
0.45685752460996));
#13686=CARTESIAN_POINT('Ctrl Pts',(-0.146375609273197,-0.000132432188538665,
0.458934495415711));
#13687=CARTESIAN_POINT('Origin',(0.,0.,0.));
#13688=CARTESIAN_POINT('',(-0.146548608312775,6.99729089778146E-5,0.516065504584291));
#13689=CARTESIAN_POINT('',(-0.146550766805835,6.86360251013434E-5,0.508934495415711));
#13690=CARTESIAN_POINT('',(-0.14635,-1.79227059055215E-17,0.));
#13691=CARTESIAN_POINT('Ctrl Pts',(-0.146548608312775,6.99729089778146E-5,
0.516065504584291));
#13692=CARTESIAN_POINT('Ctrl Pts',(-0.146572081366671,0.00404546554386884,
0.515848510308657));
#13693=CARTESIAN_POINT('Ctrl Pts',(-0.146424333269732,0.00801918670503405,
0.515631516033023));
#13694=CARTESIAN_POINT('Ctrl Pts',(-0.146099725131082,0.0119784074854107,
0.51541452175739));
#13695=CARTESIAN_POINT('Ctrl Pts',(-0.142141002193345,0.06026265009261,
0.512768191878288));
#13696=CARTESIAN_POINT('Ctrl Pts',(-0.111878319621163,0.106390286678145,
0.510121861999186));
#13697=CARTESIAN_POINT('Ctrl Pts',(-0.069163383343408,0.129247972261684,
0.507475532120084));
#13698=CARTESIAN_POINT('Ctrl Pts',(-0.0264484470656534,0.152105657845224,
0.504829202240982));
#13699=CARTESIAN_POINT('Ctrl Pts',(0.0287187429176733,0.151693392426768,
0.50218287236188));
#13700=CARTESIAN_POINT('Ctrl Pts',(0.07108729581893,0.128199876374419,0.499536542482778));
#13701=CARTESIAN_POINT('Ctrl Pts',(0.113455848720186,0.10470636032207,0.496890212603677));
#13702=CARTESIAN_POINT('Ctrl Pts',(0.143025764539373,0.0581315936358261,
0.494243882724575));
#13703=CARTESIAN_POINT('Ctrl Pts',(0.146262427589597,0.00979357977770552,
0.491597552845473));
#13704=CARTESIAN_POINT('Ctrl Pts',(0.149499090639821,-0.0385444340804161,
0.488951222966371));
#13705=CARTESIAN_POINT('Ctrl Pts',(0.126402500921083,-0.0886456951104151,
0.486304893087269));
#13706=CARTESIAN_POINT('Ctrl Pts',(0.087544330920799,-0.117578067907642,
0.483658563208167));
#13707=CARTESIAN_POINT('Ctrl Pts',(0.0486861609205161,-0.146510440704867,
0.481012233329065));
#13708=CARTESIAN_POINT('Ctrl Pts',(-0.00593358936131212,-0.154273925269321,
0.478365903449963));
#13709=CARTESIAN_POINT('Ctrl Pts',(-0.0513146009011563,-0.137315052574797,
0.475719573570861));
#13710=CARTESIAN_POINT('Ctrl Pts',(-0.0966956124410008,-0.120356179880273,
0.473073243691759));
#13711=CARTESIAN_POINT('Ctrl Pts',(-0.132837885238862,-0.078674949926771,
0.470426913812657));
#13712=CARTESIAN_POINT('Ctrl Pts',(-0.14319853241738,-0.0313495174248821,
0.467780583933555));
#13713=CARTESIAN_POINT('Ctrl Pts',(-0.145436768368387,-0.0211256884885646,
0.467208890817134));
#13714=CARTESIAN_POINT('Ctrl Pts',(-0.146471775395962,-0.0106384445195334,
0.466637197700712));
#13715=CARTESIAN_POINT('Ctrl Pts',(-0.146374718215768,-0.000132229735885947,
0.466065504584291));
#13716=CARTESIAN_POINT('Ctrl Pts',(-0.146375609273197,-0.000132432188538665,
0.458934495415711));
#13717=CARTESIAN_POINT('Ctrl Pts',(-0.146472577787773,-0.0106150565970108,
0.45950491398422));
#13718=CARTESIAN_POINT('Ctrl Pts',(-0.145442327125792,-0.021078770125739,
0.46007533255273));
#13719=CARTESIAN_POINT('Ctrl Pts',(-0.143213999951756,-0.0312807998000163,
0.460645751121239));
#13720=CARTESIAN_POINT('Ctrl Pts',(-0.132872033528166,-0.0786297930597184,
0.463293140495499));
#13721=CARTESIAN_POINT('Ctrl Pts',(-0.0967233424557573,-0.120342081894533,
0.465940529869759));
#13722=CARTESIAN_POINT('Ctrl Pts',(-0.0513258840937604,-0.13731129538499,
0.46858791924402));
#13723=CARTESIAN_POINT('Ctrl Pts',(-0.00592842573176499,-0.154280508875447,
0.47123530861828));
#13724=CARTESIAN_POINT('Ctrl Pts',(0.0487177999198187,-0.146506647021548,
0.47388269799254));
#13725=CARTESIAN_POINT('Ctrl Pts',(0.0875820145025328,-0.117550537871965,
0.476530087366799));
#13726=CARTESIAN_POINT('Ctrl Pts',(0.126446229085248,-0.0885944287223814,
0.47917747674106));
#13727=CARTESIAN_POINT('Ctrl Pts',(0.149528432599094,-0.0384560722771122,
0.481824866115319));
#13728=CARTESIAN_POINT('Ctrl Pts',(0.146255790172295,0.0098985887573764,
0.484472255489579));
#13729=CARTESIAN_POINT('Ctrl Pts',(0.142983147745498,0.0582532497918637,
0.487119644863839));
#13730=CARTESIAN_POINT('Ctrl Pts',(0.113355659378058,0.10482421541557,0.4897670342381));
#13731=CARTESIAN_POINT('Ctrl Pts',(0.0709442366160257,0.128279591164298,
0.49241442361236));
#13732=CARTESIAN_POINT('Ctrl Pts',(0.0285328138539934,0.151734966913027,
0.49506181298662));
#13733=CARTESIAN_POINT('Ctrl Pts',(-0.0266625433026316,0.152074752786777,
0.497709202360879));
#13734=CARTESIAN_POINT('Ctrl Pts',(-0.0693595260588707,0.129143309401606,
0.500356591735139));
#13735=CARTESIAN_POINT('Ctrl Pts',(-0.11205650881511,0.106211866016435,
0.503003981109399));
#13736=CARTESIAN_POINT('Ctrl Pts',(-0.142255117170964,0.060009193372344,
0.505651370483659));
#13737=CARTESIAN_POINT('Ctrl Pts',(-0.146122837288996,0.0116984888307781,
0.50829875985792));
#13738=CARTESIAN_POINT('Ctrl Pts',(-0.146432431239741,0.00783142983325791,
0.508510671710517));
#13739=CARTESIAN_POINT('Ctrl Pts',(-0.14657331536999,0.00395086404934249,
0.508722583563114));
#13740=CARTESIAN_POINT('Ctrl Pts',(-0.146550766805835,6.86360251013434E-5,
0.508934495415711));
#13741=CARTESIAN_POINT('Origin',(0.,0.,0.));
#13742=CARTESIAN_POINT('',(-0.146165204287215,8.83645032875094E-5,0.566065504584291));
#13743=CARTESIAN_POINT('',(-0.146168951232552,9.12430751481418E-5,0.558934495415711));
#13744=CARTESIAN_POINT('',(-0.14635,-1.79227059055215E-17,0.));
#13745=CARTESIAN_POINT('Ctrl Pts',(-0.146165204287215,8.83645032875094E-5,
0.566065504584291));
#13746=CARTESIAN_POINT('Ctrl Pts',(-0.146267412293664,0.0186373661349918,
0.565059822916602));
#13747=CARTESIAN_POINT('Ctrl Pts',(-0.142994166834961,0.0371516370495788,
0.564054141248913));
#13748=CARTESIAN_POINT('Ctrl Pts',(-0.136179985035193,0.0542551712289143,
0.563048459581224));
#13749=CARTESIAN_POINT('Ctrl Pts',(-0.118249288396568,0.0992610562830057,
0.560402129702122));
#13750=CARTESIAN_POINT('Ctrl Pts',(-0.0758005933416487,0.134498778989873,
0.55775579982302));
#13751=CARTESIAN_POINT('Ctrl Pts',(-0.0282633354322908,0.143839479279877,
0.555109469943918));
#13752=CARTESIAN_POINT('Ctrl Pts',(0.0192739224770691,0.153180179569881,
0.552463140064816));
#13753=CARTESIAN_POINT('Ctrl Pts',(0.0718997432408687,0.136623857443018,
0.549816810185715));
#13754=CARTESIAN_POINT('Ctrl Pts',(0.105526460745998,0.101748602013432,
0.547170480306613));
#13755=CARTESIAN_POINT('Ctrl Pts',(0.139153178251127,0.0668733465838454,
0.544524150427511));
#13756=CARTESIAN_POINT('Ctrl Pts',(0.153780792497586,0.0136791578515372,
0.541877820548409));
#13757=CARTESIAN_POINT('Ctrl Pts',(0.142714014311998,-0.0334861471092027,
0.539231490669307));
#13758=CARTESIAN_POINT('Ctrl Pts',(0.13164723612641,-0.0806514520699426,
0.536585160790205));
#13759=CARTESIAN_POINT('Ctrl Pts',(0.0948860655087725,-0.121787873259113,
0.533938830911103));
#13760=CARTESIAN_POINT('Ctrl Pts',(0.0492566686055307,-0.138066623508903,
0.531292501032001));
#13761=CARTESIAN_POINT('Ctrl Pts',(0.00362727170228945,-0.154345373758693,
0.528646171152899));
#13762=CARTESIAN_POINT('Ctrl Pts',(-0.050870351486557,-0.145766453069103,
0.525999841273797));
#13763=CARTESIAN_POINT('Ctrl Pts',(-0.089291781429334,-0.116256568409877,
0.523353511394695));
#13764=CARTESIAN_POINT('Ctrl Pts',(-0.124562723435938,-0.0891664410515947,
0.520924175791227));
#13765=CARTESIAN_POINT('Ctrl Pts',(-0.146285818313441,-0.0444372186796531,
0.518494840187759));
#13766=CARTESIAN_POINT('Ctrl Pts',(-0.146548608312775,6.99729089778146E-5,
0.516065504584291));
#13767=CARTESIAN_POINT('Ctrl Pts',(-0.146550766805835,6.86360251013434E-5,
0.508934495415711));
#13768=CARTESIAN_POINT('Ctrl Pts',(-0.146291618860727,-0.0445493453248537,
0.511369972937373));
#13769=CARTESIAN_POINT('Ctrl Pts',(-0.124445252016267,-0.0893868858389474,
0.513805450459036));
#13770=CARTESIAN_POINT('Ctrl Pts',(-0.0890226177929609,-0.116463349340462,
0.516240927980699));
#13771=CARTESIAN_POINT('Ctrl Pts',(-0.0505178462986829,-0.145895746531099,
0.518888317354959));
#13772=CARTESIAN_POINT('Ctrl Pts',(0.00402852857008221,-0.154341804473332,
0.52153570672922));
#13773=CARTESIAN_POINT('Ctrl Pts',(0.0496314652424392,-0.137932794781367,
0.52418309610348));
#13774=CARTESIAN_POINT('Ctrl Pts',(0.0952344019147948,-0.121523785089403,
0.52683048547774));
#13775=CARTESIAN_POINT('Ctrl Pts',(0.131893900390741,-0.0802597077632436,
0.529477874851999));
#13776=CARTESIAN_POINT('Ctrl Pts',(0.14281802728161,-0.0330416298281342,
0.532125264226259));
#13777=CARTESIAN_POINT('Ctrl Pts',(0.153742154172479,0.0141764481069759,
0.53477265360052));
#13778=CARTESIAN_POINT('Ctrl Pts',(0.138930909478268,0.0673485266510362,
0.53742004297478));
#13779=CARTESIAN_POINT('Ctrl Pts',(0.105168604077417,0.102119062543277,
0.54006743234904));
#13780=CARTESIAN_POINT('Ctrl Pts',(0.0714062986765666,0.136889598435517,
0.5427148217233));
#13781=CARTESIAN_POINT('Ctrl Pts',(0.018692932569077,0.153258591675938,
0.545362211097559));
#13782=CARTESIAN_POINT('Ctrl Pts',(-0.0288260648428939,0.143728202535144,
0.548009600471819));
#13783=CARTESIAN_POINT('Ctrl Pts',(-0.0763450622548654,0.13419781339435,
0.550656989846079));
#13784=CARTESIAN_POINT('Ctrl Pts',(-0.118669690971318,0.0987680418723385,
0.55330437922034));
#13785=CARTESIAN_POINT('Ctrl Pts',(-0.136413096952957,0.0536675432455532,
0.5559517685946));
#13786=CARTESIAN_POINT('Ctrl Pts',(-0.143076734904351,0.036729792140314,
0.556946010868304));
#13787=CARTESIAN_POINT('Ctrl Pts',(-0.146273385252938,0.0184280612467595,
0.557940253142007));
#13788=CARTESIAN_POINT('Ctrl Pts',(-0.146168951232552,9.12430751481418E-5,
0.558934495415711));
#13789=CARTESIAN_POINT('Origin',(0.,0.,0.));
#13790=CARTESIAN_POINT('',(-0.146227179098081,-0.000117664897458569,0.616065504584291));
#13791=CARTESIAN_POINT('',(-0.146218520919543,-0.000115076211918358,0.608934495415711));
#13792=CARTESIAN_POINT('',(-0.14635,-1.79227059055215E-17,0.));
#13793=CARTESIAN_POINT('Ctrl Pts',(-0.146227179098081,-0.000117664897458569,
0.616065504584291));
#13794=CARTESIAN_POINT('Ctrl Pts',(-0.145977603365176,0.0329427899635141,
0.614271135524546));
#13795=CARTESIAN_POINT('Ctrl Pts',(-0.134874795495675,0.0661550248562671,
0.612476766464802));
#13796=CARTESIAN_POINT('Ctrl Pts',(-0.114309815624116,0.091770790457776,
0.610682397405058));
#13797=CARTESIAN_POINT('Ctrl Pts',(-0.0839806476072558,0.129548841477563,
0.608036067525956));
#13798=CARTESIAN_POINT('Ctrl Pts',(-0.0330710111925292,0.150804375664025,
0.605389737646855));
#13799=CARTESIAN_POINT('Ctrl Pts',(0.0151169520838501,0.145808400611758,
0.602743407767753));
#13800=CARTESIAN_POINT('Ctrl Pts',(0.0633049153602295,0.140812425559491,
0.600097077888651));
#13801=CARTESIAN_POINT('Ctrl Pts',(0.108771205498262,0.109564941268491,
0.597450748009549));
#13802=CARTESIAN_POINT('Ctrl Pts',(0.130705186191441,0.0663684129079872,
0.594804418130447));
#13803=CARTESIAN_POINT('Ctrl Pts',(0.152639166884621,0.023171884547483,
0.592158088251345));
#13804=CARTESIAN_POINT('Ctrl Pts',(0.151040838132949,-0.0319736878825246,
0.589511758372243));
#13805=CARTESIAN_POINT('Ctrl Pts',(0.126641780152193,-0.0738273082886534,
0.586865428493141));
#13806=CARTESIAN_POINT('Ctrl Pts',(0.102242722171437,-0.115680928694782,
0.584219098614039));
#13807=CARTESIAN_POINT('Ctrl Pts',(0.0550429349615966,-0.14424259707703,
0.581572768734937));
#13808=CARTESIAN_POINT('Ctrl Pts',(0.00664650371163741,-0.14643918846291,
0.578926438855836));
#13809=CARTESIAN_POINT('Ctrl Pts',(-0.0417499275383225,-0.148635779848789,
0.576280108976733));
#13810=CARTESIAN_POINT('Ctrl Pts',(-0.0913430028284016,-0.1244672942383,
0.573633779097631));
#13811=CARTESIAN_POINT('Ctrl Pts',(-0.119433191362276,-0.0849960277323969,
0.570987449218529));
#13812=CARTESIAN_POINT('Ctrl Pts',(-0.136848298201485,-0.0605249807527623,
0.569346801007117));
#13813=CARTESIAN_POINT('Ctrl Pts',(-0.145998464265635,-0.0301720919893573,
0.567706152795704));
#13814=CARTESIAN_POINT('Ctrl Pts',(-0.146165204287215,8.83645032875094E-5,
0.566065504584291));
#13815=CARTESIAN_POINT('Ctrl Pts',(-0.146168951232552,9.12430751481418E-5,
0.558934495415711));
#13816=CARTESIAN_POINT('Ctrl Pts',(-0.145995306636495,-0.0303977620653178,
0.560587642516267));
#13817=CARTESIAN_POINT('Ctrl Pts',(-0.136695352934655,-0.0609837708898569,
0.562240789616823));
#13818=CARTESIAN_POINT('Ctrl Pts',(-0.119031718004195,-0.0855580991331628,
0.563893936717379));
#13819=CARTESIAN_POINT('Ctrl Pts',(-0.090744749826965,-0.124912017153538,
0.566541326091639));
#13820=CARTESIAN_POINT('Ctrl Pts',(-0.0410086302256792,-0.148848627462727,
0.5691887154659));
#13821=CARTESIAN_POINT('Ctrl Pts',(0.00739494322942312,-0.146403732988417,
0.57183610484016));
#13822=CARTESIAN_POINT('Ctrl Pts',(0.0557985166845234,-0.143958838514108,
0.57448349421442));
#13823=CARTESIAN_POINT('Ctrl Pts',(0.10286954399344,-0.1151324392563,0.57713088358868));
#13824=CARTESIAN_POINT('Ctrl Pts',(0.127047076753504,-0.0731285067993286,
0.579778272962939));
#13825=CARTESIAN_POINT('Ctrl Pts',(0.151224609513568,-0.031124574342357,
0.5824256623372));
#13826=CARTESIAN_POINT('Ctrl Pts',(0.15250864772478,0.0240568913137802,
0.58507305171146));
#13827=CARTESIAN_POINT('Ctrl Pts',(0.130311035929276,0.0671399443948921,
0.58772044108572));
#13828=CARTESIAN_POINT('Ctrl Pts',(0.108113424133771,0.110222997476006,
0.59036783045998));
#13829=CARTESIAN_POINT('Ctrl Pts',(0.0624341623315493,0.141207637982093,
0.593015219834239));
#13830=CARTESIAN_POINT('Ctrl Pts',(0.0141966988324609,0.145901308974836,
0.595662609208499));
#13831=CARTESIAN_POINT('Ctrl Pts',(-0.0340407646666261,0.150594979967579,
0.598309998582759));
#13832=CARTESIAN_POINT('Ctrl Pts',(-0.0848364298625779,0.128997681446978,
0.60095738795702));
#13833=CARTESIAN_POINT('Ctrl Pts',(-0.114923272877171,0.091002085522857,
0.60360477733128));
#13834=CARTESIAN_POINT('Ctrl Pts',(-0.135113526827902,0.0655045372973676,
0.60538135002609));
#13835=CARTESIAN_POINT('Ctrl Pts',(-0.14597798884013,0.0326223532682757,
0.6071579227209));
#13836=CARTESIAN_POINT('Ctrl Pts',(-0.146218520919543,-0.000115076211918358,
0.608934495415711));
#13837=CARTESIAN_POINT('Origin',(0.,0.,0.));
#13838=CARTESIAN_POINT('',(-0.146586033401767,-2.15382961294558E-5,0.66606550458429));
#13839=CARTESIAN_POINT('',(-0.146582846697157,-3.00215943766004E-5,0.65893449541571));
#13840=CARTESIAN_POINT('',(-0.14635,-1.79227059055215E-17,0.));
#13841=CARTESIAN_POINT('Ctrl Pts',(-0.146586033401767,-2.15382961294558E-5,
0.66606550458429));
#13842=CARTESIAN_POINT('Ctrl Pts',(-0.146488810225965,0.0472697707580183,
0.663482448132491));
#13843=CARTESIAN_POINT('Ctrl Pts',(-0.121516563758978,0.0946492637554097,
0.660899391680692));
#13844=CARTESIAN_POINT('Ctrl Pts',(-0.0824084263440199,0.121233094478226,
0.658316335228893));
#13845=CARTESIAN_POINT('Ctrl Pts',(-0.0423423130056393,0.148468111155377,
0.655670005349791));
#13846=CARTESIAN_POINT('Ctrl Pts',(0.0125607065496858,0.153876184485078,
0.653023675470689));
#13847=CARTESIAN_POINT('Ctrl Pts',(0.0571706564953393,0.134981954220393,
0.650377345591587));
#13848=CARTESIAN_POINT('Ctrl Pts',(0.101780606440992,0.116087723955709,
0.647731015712485));
#13849=CARTESIAN_POINT('Ctrl Pts',(0.136097486776972,0.0728911900966409,
0.645084685833384));
#13850=CARTESIAN_POINT('Ctrl Pts',(0.144413921474191,0.0251640857912735,
0.642438355954282));
#13851=CARTESIAN_POINT('Ctrl Pts',(0.152730356171409,-0.0225630185140953,
0.63979202607518));
#13852=CARTESIAN_POINT('Ctrl Pts',(0.135046345229863,-0.0748206932657649,
0.637145696196077));
#13853=CARTESIAN_POINT('Ctrl Pts',(0.0994561386758346,-0.10768977857233,
0.634499366316975));
#13854=CARTESIAN_POINT('Ctrl Pts',(0.0638659321218069,-0.140558863878895,
0.631853036437873));
#13855=CARTESIAN_POINT('Ctrl Pts',(0.0103695299552984,-0.154039359740357,
0.629206706558772));
#13856=CARTESIAN_POINT('Ctrl Pts',(-0.0365469229059137,-0.141961031115491,
0.62656037667967));
#13857=CARTESIAN_POINT('Ctrl Pts',(-0.0834633757671259,-0.129882702490626,
0.623914046800568));
#13858=CARTESIAN_POINT('Ctrl Pts',(-0.123799879323041,-0.0922455493794331,
0.621267716921466));
#13859=CARTESIAN_POINT('Ctrl Pts',(-0.139093781291504,-0.0462766888972804,
0.618621387042364));
#13860=CARTESIAN_POINT('Ctrl Pts',(-0.14401750805555,-0.0314774500153124,
0.617769426223006));
#13861=CARTESIAN_POINT('Ctrl Pts',(-0.14634567687575,-0.0158146654998378,
0.616917465403648));
#13862=CARTESIAN_POINT('Ctrl Pts',(-0.146227179098081,-0.000117664897458569,
0.616065504584291));
#13863=CARTESIAN_POINT('Ctrl Pts',(-0.146218520919543,-0.000115076211918358,
0.608934495415711));
#13864=CARTESIAN_POINT('Ctrl Pts',(-0.1463364217222,-0.0161618722236638,
0.60980531209516));
#13865=CARTESIAN_POINT('Ctrl Pts',(-0.143901781624712,-0.032173889023867,
0.61067612877461));
#13866=CARTESIAN_POINT('Ctrl Pts',(-0.138761720114909,-0.0472643972675185,
0.611546945454059));
#13867=CARTESIAN_POINT('Ctrl Pts',(-0.123135303504819,-0.0931413908061287,
0.614194334828319));
#13868=CARTESIAN_POINT('Ctrl Pts',(-0.0825044494514074,-0.130501484555709,
0.616841724202579));
#13869=CARTESIAN_POINT('Ctrl Pts',(-0.0354801761942514,-0.142231836504824,
0.619489113576839));
#13870=CARTESIAN_POINT('Ctrl Pts',(0.0115440970629072,-0.15396218845394,
0.6221365029511));
#13871=CARTESIAN_POINT('Ctrl Pts',(0.0649617895238099,-0.140062798602586,
0.624783892325359));
#13872=CARTESIAN_POINT('Ctrl Pts',(0.100304854137336,-0.106900301471969,
0.627431281699619));
#13873=CARTESIAN_POINT('Ctrl Pts',(0.135647918750861,-0.0737378043413545,
0.630078671073879));
#13874=CARTESIAN_POINT('Ctrl Pts',(0.15291635551701,-0.0213121999314781,
0.63272606044814));
#13875=CARTESIAN_POINT('Ctrl Pts',(0.144200333369931,0.026362891994447,
0.6353734498224));
#13876=CARTESIAN_POINT('Ctrl Pts',(0.135484311222852,0.0740379839203748,
0.63802083919666));
#13877=CARTESIAN_POINT('Ctrl Pts',(0.100783830162543,0.11696256336235,0.640668228570919));
#13878=CARTESIAN_POINT('Ctrl Pts',(0.055993492972559,0.135474968031154,
0.643315617945179));
#13879=CARTESIAN_POINT('Ctrl Pts',(0.0112031557825773,0.153987372699956,
0.64596300731944));
#13880=CARTESIAN_POINT('Ctrl Pts',(-0.04367703753708,0.148087602595587,
0.6486103966937));
#13881=CARTESIAN_POINT('Ctrl Pts',(-0.0835091394177698,0.120478055479053,
0.65125778606796));
#13882=CARTESIAN_POINT('Ctrl Pts',(-0.122009894390588,0.0937913289882395,
0.653816689183877));
#13883=CARTESIAN_POINT('Ctrl Pts',(-0.146451680634158,0.0468218259492564,
0.656375592299793));
#13884=CARTESIAN_POINT('Ctrl Pts',(-0.146582846697157,-3.00215943766004E-5,
0.65893449541571));
#13885=CARTESIAN_POINT('Origin',(0.,0.,0.));
#13886=CARTESIAN_POINT('',(-0.146290249280603,0.000131112932912382,0.716065504584291));
#13887=CARTESIAN_POINT('',(-0.146307221518699,0.000133045872591754,0.708934495415711));
#13888=CARTESIAN_POINT('',(-0.14635,-1.79227059055215E-17,0.));
#13889=CARTESIAN_POINT('Ctrl Pts',(-0.146290249280603,0.000131112932912382,
0.716065504584291));
#13890=CARTESIAN_POINT('Ctrl Pts',(-0.146406294125046,0.0134819654399978,
0.715340090619538));
#13891=CARTESIAN_POINT('Ctrl Pts',(-0.144729088574721,0.0268041890186768,
0.714614676654786));
#13892=CARTESIAN_POINT('Ctrl Pts',(-0.141142411757643,0.0395908011096033,
0.713889262690033));
#13893=CARTESIAN_POINT('Ctrl Pts',(-0.128058117149462,0.0862367098911347,
0.711242932810931));
#13894=CARTESIAN_POINT('Ctrl Pts',(-0.0895623832093418,0.125754646095387,
0.708596602931829));
#13895=CARTESIAN_POINT('Ctrl Pts',(-0.0432753130058998,0.140056628595385,
0.705950273052727));
#13896=CARTESIAN_POINT('Ctrl Pts',(0.00301175719754219,0.154358611095384,
0.703303943173625));
#13897=CARTESIAN_POINT('Ctrl Pts',(0.0570901636643063,0.143444639891129,
0.700657613294523));
#13898=CARTESIAN_POINT('Ctrl Pts',(0.0942073689518517,0.11231021130972,
0.698011283415421));
#13899=CARTESIAN_POINT('Ctrl Pts',(0.131324574239397,0.0811757827283121,
0.695364953536319));
#13900=CARTESIAN_POINT('Ctrl Pts',(0.151480578347723,0.0298208967697505,
0.692718623657217));
#13901=CARTESIAN_POINT('Ctrl Pts',(0.145449661086834,-0.0182485073085286,
0.690072293778115));
#13902=CARTESIAN_POINT('Ctrl Pts',(0.139418743825945,-0.0663179113868083,
0.687425963899014));
#13903=CARTESIAN_POINT('Ctrl Pts',(0.107200905195838,-0.111101833584806,
0.684779634019911));
#13904=CARTESIAN_POINT('Ctrl Pts',(0.0635427568131047,-0.132101968137704,
0.68213330414081));
#13905=CARTESIAN_POINT('Ctrl Pts',(0.0198846084303716,-0.153102102690602,
0.679486974261708));
#13906=CARTESIAN_POINT('Ctrl Pts',(-0.0352138497049885,-0.150318449598402,
0.676840644382606));
#13907=CARTESIAN_POINT('Ctrl Pts',(-0.0765331864534889,-0.125025130675956,
0.674194314503504));
#13908=CARTESIAN_POINT('Ctrl Pts',(-0.117852523201989,-0.0997318117535095,
0.671547984624402));
#13909=CARTESIAN_POINT('Ctrl Pts',(-0.14539273856363,-0.0519288270008166,
0.6689016547453));
#13910=CARTESIAN_POINT('Ctrl Pts',(-0.146548242683733,-0.00349635461217019,
0.666255324866198));
#13911=CARTESIAN_POINT('Ctrl Pts',(-0.146575870647472,-0.00233834005587287,
0.666192051438896));
#13912=CARTESIAN_POINT('Ctrl Pts',(-0.146588414938392,-0.00117996563262623,
0.666128778011593));
#13913=CARTESIAN_POINT('Ctrl Pts',(-0.146586033401767,-2.15382961294558E-5,
0.66606550458429));
#13914=CARTESIAN_POINT('Ctrl Pts',(-0.146582846697157,-3.00215943766004E-5,
0.65893449541571));
#13915=CARTESIAN_POINT('Ctrl Pts',(-0.146587382388275,-0.00165014728799839,
0.659022981674053));
#13916=CARTESIAN_POINT('Ctrl Pts',(-0.146562848415234,-0.00327013229389975,
0.659111467932396));
#13917=CARTESIAN_POINT('Ctrl Pts',(-0.146508820881567,-0.00488913307276392,
0.659199954190739));
#13918=CARTESIAN_POINT('Ctrl Pts',(-0.144892390022949,-0.0533274503793473,
0.661847343564999));
#13919=CARTESIAN_POINT('Ctrl Pts',(-0.116875517863988,-0.100884760863813,
0.66449473293926));
#13920=CARTESIAN_POINT('Ctrl Pts',(-0.0752913709948059,-0.125777373450206,
0.66714212231352));
#13921=CARTESIAN_POINT('Ctrl Pts',(-0.0337072241256252,-0.150669986036599,
0.66978951168778));
#13922=CARTESIAN_POINT('Ctrl Pts',(0.021444197453776,-0.15289790072492,
0.672436901062039));
#13923=CARTESIAN_POINT('Ctrl Pts',(0.0649007096996251,-0.131440618146733,
0.675084290436299));
#13924=CARTESIAN_POINT('Ctrl Pts',(0.108357221945475,-0.109983335568545,
0.677731679810559));
#13925=CARTESIAN_POINT('Ctrl Pts',(0.140118824857774,-0.0648408557238465,
0.68037906918482));
#13926=CARTESIAN_POINT('Ctrl Pts',(0.145637072805965,-0.0166907532130915,
0.68302645855908));
#13927=CARTESIAN_POINT('Ctrl Pts',(0.151155320754156,0.031459349297663,
0.68567384793334));
#13928=CARTESIAN_POINT('Ctrl Pts',(0.130430213738242,0.0826170744744734,
0.688321237307599));
#13929=CARTESIAN_POINT('Ctrl Pts',(0.0929549153570804,0.113349556369966,
0.690968626681859));
#13930=CARTESIAN_POINT('Ctrl Pts',(0.0554796169759186,0.14408203826546,
0.693616016056119));
#13931=CARTESIAN_POINT('Ctrl Pts',(0.00125412722950909,0.154389276879634,
0.69626340543038));
#13932=CARTESIAN_POINT('Ctrl Pts',(-0.0448834941801804,0.139550027475769,
0.69891079480464));
#13933=CARTESIAN_POINT('Ctrl Pts',(-0.0910211155898686,0.124710778071904,
0.7015581841789));
#13934=CARTESIAN_POINT('Ctrl Pts',(-0.129070868662838,0.0847250406500019,
0.704205573553159));
#13935=CARTESIAN_POINT('Ctrl Pts',(-0.141604011991841,0.0379083368947344,
0.706852962927419));
#13936=CARTESIAN_POINT('Ctrl Pts',(-0.144888775625201,0.0256383259412015,
0.707546807090183));
#13937=CARTESIAN_POINT('Ctrl Pts',(-0.146420824649375,0.0128991016161637,
0.708240651252947));
#13938=CARTESIAN_POINT('Ctrl Pts',(-0.146307221518699,0.000133045872591754,
0.708934495415711));
#13939=CARTESIAN_POINT('Origin',(0.,0.,0.));
#13940=CARTESIAN_POINT('',(-0.1461301977291,-5.61458017395017E-5,0.766065504584291));
#13941=CARTESIAN_POINT('',(-0.14612241379348,-4.54149644099216E-5,0.758934495415711));
#13942=CARTESIAN_POINT('',(-0.14635,-1.79227059055215E-17,0.));
#13943=CARTESIAN_POINT('Ctrl Pts',(-0.1461301977291,-5.61458017395017E-5,
0.766065504584291));
#13944=CARTESIAN_POINT('Ctrl Pts',(-0.14603380141711,0.0278870014676159,
0.764551403227483));
#13945=CARTESIAN_POINT('Ctrl Pts',(-0.138327245009168,0.0558793842949389,
0.763037301870675));
#13946=CARTESIAN_POINT('Ctrl Pts',(-0.123350675409043,0.079203679241543,
0.761523200513867));
#13947=CARTESIAN_POINT('Ctrl Pts',(-0.0971747899961838,0.119969628197767,
0.758876870634766));
#13948=CARTESIAN_POINT('Ctrl Pts',(-0.048790709571801,0.146475657227381,
0.756230540755664));
#13949=CARTESIAN_POINT('Ctrl Pts',(-0.000344588961360588,0.146589539830481,
0.753584210876561));
#13950=CARTESIAN_POINT('Ctrl Pts',(0.0481015316490792,0.14670342243358,
0.750937880997459));
#13951=CARTESIAN_POINT('Ctrl Pts',(0.0966096924455767,0.120425158610167,
0.748291551118357));
#13952=CARTESIAN_POINT('Ctrl Pts',(0.122976945064223,0.0797827231418903,
0.745645221239255));
#13953=CARTESIAN_POINT('Ctrl Pts',(0.149344197682869,0.0391402876736125,
0.742998891360154));
#13954=CARTESIAN_POINT('Ctrl Pts',(0.153570542123663,-0.01586631943953,
0.740352561481052));
#13955=CARTESIAN_POINT('Ctrl Pts',(0.133721514043982,-0.0600597087159893,
0.73770623160195));
#13956=CARTESIAN_POINT('Ctrl Pts',(0.113872485964301,-0.104253097992448,
0.735059901722848));
#13957=CARTESIAN_POINT('Ctrl Pts',(0.0699480853641458,-0.137633269432224,
0.732413571843746));
#13958=CARTESIAN_POINT('Ctrl Pts',(0.0220532014503509,-0.144921593405036,
0.729767241964644));
#13959=CARTESIAN_POINT('Ctrl Pts',(-0.0258416824634434,-0.152209917377848,
0.727120912085542));
#13960=CARTESIAN_POINT('Ctrl Pts',(-0.0777070496908773,-0.133406393883698,
0.724474582206441));
#13961=CARTESIAN_POINT('Ctrl Pts',(-0.109803305666473,-0.0971176914572187,
0.721828252327339));
#13962=CARTESIAN_POINT('Ctrl Pts',(-0.133101311474982,-0.0707764758164216,
0.71990733641299));
#13963=CARTESIAN_POINT('Ctrl Pts',(-0.14598295937539,-0.0352223077304616,
0.71798642049864));
#13964=CARTESIAN_POINT('Ctrl Pts',(-0.146290249280603,0.000131112932912382,
0.716065504584291));
#13965=CARTESIAN_POINT('Ctrl Pts',(-0.146307221518699,0.000133045872591754,
0.708934495415711));
#13966=CARTESIAN_POINT('Ctrl Pts',(-0.145987367488279,-0.0358102803178394,
0.710888040627207));
#13967=CARTESIAN_POINT('Ctrl Pts',(-0.132622002370819,-0.0719663061161047,
0.712841585838703));
#13968=CARTESIAN_POINT('Ctrl Pts',(-0.1086007072861,-0.0984612847532928,
0.7147951310502));
#13969=CARTESIAN_POINT('Ctrl Pts',(-0.0760477256663158,-0.134366532557423,
0.71744252042446));
#13970=CARTESIAN_POINT('Ctrl Pts',(-0.0239252288417074,-0.152529358077047,
0.720089909798719));
#13971=CARTESIAN_POINT('Ctrl Pts',(0.0238920022682765,-0.144630254255197,
0.722737299172979));
#13972=CARTESIAN_POINT('Ctrl Pts',(0.071709233378259,-0.136731150433346,
0.725384688547239));
#13973=CARTESIAN_POINT('Ctrl Pts',(0.115221198773618,-0.102770117270024,
0.7280320779215));
#13974=CARTESIAN_POINT('Ctrl Pts',(0.134497183226257,-0.058303052428779,
0.730679467295759));
#13975=CARTESIAN_POINT('Ctrl Pts',(0.153773167678896,-0.0138359875875333,
0.733326856670019));
#13976=CARTESIAN_POINT('Ctrl Pts',(0.148813171188813,0.0411371089316358,
0.735974246044279));
#13977=CARTESIAN_POINT('Ctrl Pts',(0.121889126928366,0.0814357351225549,
0.738621635418539));
#13978=CARTESIAN_POINT('Ctrl Pts',(0.0949650826679194,0.121734361313473,
0.741269024792799));
#13979=CARTESIAN_POINT('Ctrl Pts',(0.0460769906371109,0.147358517176143,
0.74391641416706));
#13980=CARTESIAN_POINT('Ctrl Pts',(-0.00238189178169058,0.146571023090686,
0.74656380354132));
#13981=CARTESIAN_POINT('Ctrl Pts',(-0.0508407742004934,0.14578352900523,
0.74921119291558));
#13982=CARTESIAN_POINT('Ctrl Pts',(-0.0988704470072894,0.118584384971644,
0.751858582289839));
#13983=CARTESIAN_POINT('Ctrl Pts',(-0.124470852918682,0.0774321960944291,
0.754505971664099));
#13984=CARTESIAN_POINT('Ctrl Pts',(-0.138745545153454,0.0544858868428234,
0.75598214624797));
#13985=CARTESIAN_POINT('Ctrl Pts',(-0.146046671909043,0.027201385339783,
0.757458320831841));
#13986=CARTESIAN_POINT('Ctrl Pts',(-0.14612241379348,-4.54149644099216E-5,
0.758934495415711));
#13987=CARTESIAN_POINT('Origin',(0.,0.,0.));
#13988=CARTESIAN_POINT('',(-0.146495788566881,-0.000101744904923998,0.816065504584291));
#13989=CARTESIAN_POINT('',(-0.146473871348434,-0.000110945968026819,0.808934495415711));
#13990=CARTESIAN_POINT('',(-0.14635,-1.79227059055215E-17,0.));
#13991=CARTESIAN_POINT('Ctrl Pts',(-0.146495788566881,-0.000101744904923998,
0.816065504584291));
#13992=CARTESIAN_POINT('Ctrl Pts',(-0.14616118452328,0.0421270051992108,
0.813762715835428));
#13993=CARTESIAN_POINT('Ctrl Pts',(-0.126905337350145,0.0846218946815527,
0.811459927086565));
#13994=CARTESIAN_POINT('Ctrl Pts',(-0.0947343415465314,0.111866064832055,
0.809157138337701));
#13995=CARTESIAN_POINT('Ctrl Pts',(-0.0577639214515077,0.143174651664521,
0.806510808458599));
#13996=CARTESIAN_POINT('Ctrl Pts',(-0.00373742343573488,0.154342745753647,
0.803864478579497));
#13997=CARTESIAN_POINT('Ctrl Pts',(0.0426163743729279,0.140258534729872,
0.801218148700395));
#13998=CARTESIAN_POINT('Ctrl Pts',(0.0889701721815907,0.126174323706097,
0.798571818821294));
#13999=CARTESIAN_POINT('Ctrl Pts',(0.127651269783143,0.0868378075694234,
0.795925488942192));
#14000=CARTESIAN_POINT('Ctrl Pts',(0.140954720244851,0.040253928627653,
0.79327915906309));
#14001=CARTESIAN_POINT('Ctrl Pts',(0.154258170706558,-0.00632995031411615,
0.790632829183988));
#14002=CARTESIAN_POINT('Ctrl Pts',(0.14218397402842,-0.060161192060982,
0.787986499304886));
#14003=CARTESIAN_POINT('Ctrl Pts',(0.110258679990485,-0.0966003903512828,
0.785340169425784));
#14004=CARTESIAN_POINT('Ctrl Pts',(0.0783333859525485,-0.133039588641585,
0.782693839546682));
#14005=CARTESIAN_POINT('Ctrl Pts',(0.0265569945548152,-0.152086743475322,
0.780047509667581));
#14006=CARTESIAN_POINT('Ctrl Pts',(-0.021371625274328,-0.14502367242074,
0.777401179788479));
#14007=CARTESIAN_POINT('Ctrl Pts',(-0.0693002451034712,-0.137960601366157,
0.774754849909377));
#14008=CARTESIAN_POINT('Ctrl Pts',(-0.113381093364023,-0.104787304423254,
0.772108520030274));
#14009=CARTESIAN_POINT('Ctrl Pts',(-0.133437672293631,-0.0606877215103841,
0.769462190151172));
#14010=CARTESIAN_POINT('Ctrl Pts',(-0.1420188514214,-0.0418197768941368,
0.768329961628878));
#14011=CARTESIAN_POINT('Ctrl Pts',(-0.146202281842484,-0.0209517273285418,
0.767197733106584));
#14012=CARTESIAN_POINT('Ctrl Pts',(-0.1461301977291,-5.61458017395017E-5,
0.766065504584291));
#14013=CARTESIAN_POINT('Ctrl Pts',(-0.14612241379348,-4.54149644099216E-5,
0.758934495415711));
#14014=CARTESIAN_POINT('Ctrl Pts',(-0.146182508321779,-0.0216633562673834,
0.760105710206101));
#14015=CARTESIAN_POINT('Ctrl Pts',(-0.141694203021096,-0.0432575645610501,
0.76127692499649));
#14016=CARTESIAN_POINT('Ctrl Pts',(-0.132531725405586,-0.0626424774360703,
0.76244813978688));
#14017=CARTESIAN_POINT('Ctrl Pts',(-0.111821052965107,-0.106459728368519,
0.76509552916114));
#14018=CARTESIAN_POINT('Ctrl Pts',(-0.067228569068158,-0.138988996512573,
0.767742918535399));
#14019=CARTESIAN_POINT('Ctrl Pts',(-0.0191799219195066,-0.145330206128911,
0.770390307909659));
#14020=CARTESIAN_POINT('Ctrl Pts',(0.0288687252291434,-0.151671415745249,
0.773037697283919));
#14021=CARTESIAN_POINT('Ctrl Pts',(0.080373535629496,-0.131824566833873,
0.77568508665818));
#14022=CARTESIAN_POINT('Ctrl Pts',(0.111742660473083,-0.0948805356683208,
0.77833247603244));
#14023=CARTESIAN_POINT('Ctrl Pts',(0.14311178531667,-0.0579365045027684,
0.7809798654067));
#14024=CARTESIAN_POINT('Ctrl Pts',(0.154345224603492,-0.00389529108304171,
0.783627254780959));
#14025=CARTESIAN_POINT('Ctrl Pts',(0.140297486112651,0.0424894529122293,
0.786274644155219));
#14026=CARTESIAN_POINT('Ctrl Pts',(0.126249747621811,0.0888741969075009,
0.788922033529479));
#14027=CARTESIAN_POINT('Ctrl Pts',(0.0869208313533056,0.127602471478316,
0.79156942290374));
#14028=CARTESIAN_POINT('Ctrl Pts',(0.0403254011646538,0.140934737517831,
0.794216812278));
#14029=CARTESIAN_POINT('Ctrl Pts',(-0.00627002902399674,0.154267003557346,
0.79686420165226));
#14030=CARTESIAN_POINT('Ctrl Pts',(-0.0601319731327944,0.142203261065564,
0.799511591026519));
#14031=CARTESIAN_POINT('Ctrl Pts',(-0.0965888940360299,0.110269323781398,
0.802158980400779));
#14032=CARTESIAN_POINT('Ctrl Pts',(-0.127690529151203,0.0830262752573849,
0.804417485405756));
#14033=CARTESIAN_POINT('Ctrl Pts',(-0.146124951115714,0.0413218847513699,
0.806675990410734));
#14034=CARTESIAN_POINT('Ctrl Pts',(-0.146473871348434,-0.000110945968026819,
0.808934495415711));
#14035=CARTESIAN_POINT('Origin',(0.,0.,0.));
#14036=CARTESIAN_POINT('',(-0.146444331750498,0.000119944961782359,0.866065504584291));
#14037=CARTESIAN_POINT('',(-0.146471560192382,0.00011177640072981,0.858934495415711));
#14038=CARTESIAN_POINT('',(-0.14635,-1.79227059055215E-17,0.));
#14039=CARTESIAN_POINT('Ctrl Pts',(-0.146444331750498,0.000119944961782359,
0.866065504584291));
#14040=CARTESIAN_POINT('Ctrl Pts',(-0.146516681599632,0.00829054204730037,
0.865620358322474));
#14041=CARTESIAN_POINT('Ctrl Pts',(-0.145891801779796,0.0164500693154795,
0.865175212060658));
#14042=CARTESIAN_POINT('Ctrl Pts',(-0.14453063157077,0.0244848619971339,
0.864730065798841));
#14043=CARTESIAN_POINT('Ctrl Pts',(-0.136438672357208,0.0722505376181754,
0.862083735919739));
#14044=CARTESIAN_POINT('Ctrl Pts',(-0.102325254887189,0.115607931012472,
0.859437406040638));
#14045=CARTESIAN_POINT('Ctrl Pts',(-0.0578046270350215,0.134711681091902,
0.856791076161536));
#14046=CARTESIAN_POINT('Ctrl Pts',(-0.0132839991828526,0.153815431171333,
0.854144746282434));
#14047=CARTESIAN_POINT('Ctrl Pts',(0.0416438390514653,0.148665537935894,
0.851498416403331));
#14048=CARTESIAN_POINT('Ctrl Pts',(0.081837551941475,0.121619188541491,
0.848852086524229));
#14049=CARTESIAN_POINT('Ctrl Pts',(0.122031264831484,0.0945728391470885,
0.846205756645128));
#14050=CARTESIAN_POINT('Ctrl Pts',(0.147490852377186,0.0456300335937214,
0.843559426766026));
#14051=CARTESIAN_POINT('Ctrl Pts',(0.146563060809277,-0.0028073360113171,
0.840913096886925));
#14052=CARTESIAN_POINT('Ctrl Pts',(0.145635269241369,-0.0512447056163556,
0.838266767007823));
#14053=CARTESIAN_POINT('Ctrl Pts',(0.118320098559852,-0.0991766392730661,
0.835620437128721));
#14054=CARTESIAN_POINT('Ctrl Pts',(0.0771201321287374,-0.124663936845065,
0.832974107249619));
#14055=CARTESIAN_POINT('Ctrl Pts',(0.035920165697623,-0.150151234417064,
0.830327777370517));
#14056=CARTESIAN_POINT('Ctrl Pts',(-0.0191645964830881,-0.153193895904352,
0.827681447491415));
#14057=CARTESIAN_POINT('Ctrl Pts',(-0.0629209921278279,-0.132399247274726,
0.825035117612313));
#14058=CARTESIAN_POINT('Ctrl Pts',(-0.106677387772568,-0.111604598645101,
0.822388787733211));
#14059=CARTESIAN_POINT('Ctrl Pts',(-0.139105416881337,-0.0669726398985626,
0.819742457854109));
#14060=CARTESIAN_POINT('Ctrl Pts',(-0.145362260348583,-0.0189321207373897,
0.817096127975007));
#14061=CARTESIAN_POINT('Ctrl Pts',(-0.146174510965348,-0.0126955988357878,
0.816752586844768));
#14062=CARTESIAN_POINT('Ctrl Pts',(-0.146545706411658,-0.00640163348415362,
0.81640904571453));
#14063=CARTESIAN_POINT('Ctrl Pts',(-0.146495788566881,-0.000101744904923998,
0.816065504584291));
#14064=CARTESIAN_POINT('Ctrl Pts',(-0.146473871348434,-0.000110945968026819,
0.808934495415711));
#14065=CARTESIAN_POINT('Ctrl Pts',(-0.146533950748007,-0.00724512552769256,
0.809323379784994));
#14066=CARTESIAN_POINT('Ctrl Pts',(-0.146057826922151,-0.0143712538186879,
0.809712264154277));
#14067=CARTESIAN_POINT('Ctrl Pts',(-0.145017839345608,-0.0214141189368497,
0.81010114852356));
#14068=CARTESIAN_POINT('Ctrl Pts',(-0.137937966054276,-0.0693594922943736,
0.81274853789782));
#14069=CARTESIAN_POINT('Ctrl Pts',(-0.104726321773939,-0.113446106932874,
0.81539592727208));
#14070=CARTESIAN_POINT('Ctrl Pts',(-0.0605955455659204,-0.133480028752914,
0.818043316646339));
#14071=CARTESIAN_POINT('Ctrl Pts',(-0.0164647693578984,-0.153513950572954,
0.820690706020599));
#14072=CARTESIAN_POINT('Ctrl Pts',(0.0385851387778066,-0.149495179574532,
0.823338095394859));
#14073=CARTESIAN_POINT('Ctrl Pts',(0.0793384931690736,-0.12326451930694,
0.825985484769119));
#14074=CARTESIAN_POINT('Ctrl Pts',(0.120091847560339,-0.0970338590393495,
0.828632874143379));
#14075=CARTESIAN_POINT('Ctrl Pts',(0.146548648207165,-0.0485913095025905,
0.83128026351764));
#14076=CARTESIAN_POINT('Ctrl Pts',(0.146590321408106,-0.000126046730599388,
0.833927652891899));
#14077=CARTESIAN_POINT('Ctrl Pts',(0.146631994609047,0.0483392160413931,
0.836575042266159));
#14078=CARTESIAN_POINT('Ctrl Pts',(0.120258540364101,0.0968271920486179,
0.839222431640419));
#14079=CARTESIAN_POINT('Ctrl Pts',(0.0795503554414038,0.123127897600245,
0.841869821014679));
#14080=CARTESIAN_POINT('Ctrl Pts',(0.0388421705187073,0.149428603151872,
0.844517210388939));
#14081=CARTESIAN_POINT('Ctrl Pts',(-0.0162007450817403,0.153542038247903,
0.8471645997632));
#14082=CARTESIAN_POINT('Ctrl Pts',(-0.0603659086281491,0.133584038319734,
0.84981198913746));
#14083=CARTESIAN_POINT('Ctrl Pts',(-0.104531072174558,0.113626038391565,
0.85245937851172));
#14084=CARTESIAN_POINT('Ctrl Pts',(-0.137818483666928,0.0695966034391962,
0.855106767885979));
#14085=CARTESIAN_POINT('Ctrl Pts',(-0.144980798768897,0.0216634763286692,
0.857754157260239));
#14086=CARTESIAN_POINT('Ctrl Pts',(-0.146045237806912,0.0145398171508471,
0.858147603312063));
#14087=CARTESIAN_POINT('Ctrl Pts',(-0.146532654486068,0.00732993751956911,
0.858541049363887));
#14088=CARTESIAN_POINT('Ctrl Pts',(-0.146471560192382,0.00011177640072981,
0.858934495415711));
#14089=CARTESIAN_POINT('Origin',(0.,0.,0.));
#14090=CARTESIAN_POINT('',(-0.146114231148477,2.69008449349656E-5,0.916065504584291));
#14091=CARTESIAN_POINT('',(-0.146121644853617,4.41067432152685E-5,0.908934495415711));
#14092=CARTESIAN_POINT('',(-0.14635,-1.79227059055215E-17,0.));
#14093=CARTESIAN_POINT('Ctrl Pts',(-0.146114231148477,2.69008449349656E-5,
0.916065504584291));
#14094=CARTESIAN_POINT('Ctrl Pts',(-0.146151635159142,0.0228038459942234,
0.914831670930419));
#14095=CARTESIAN_POINT('Ctrl Pts',(-0.141147538069067,0.0455652341090756,
0.913597837276548));
#14096=CARTESIAN_POINT('Ctrl Pts',(-0.131015765267123,0.0657531838068269,
0.912364003622676));
#14097=CARTESIAN_POINT('Ctrl Pts',(-0.109285110563454,0.109052354902802,
0.909717673743574));
#14098=CARTESIAN_POINT('Ctrl Pts',(-0.0639662294071284,0.140513248471977,
0.907071343864472));
#14099=CARTESIAN_POINT('Ctrl Pts',(-0.015802286694576,0.145735718560985,
0.90442501398537));
#14100=CARTESIAN_POINT('Ctrl Pts',(0.0323616560179757,0.150958188649994,
0.901778684106268));
#14101=CARTESIAN_POINT('Ctrl Pts',(0.0833706602867547,0.129942235258839,
0.899132354227166));
#14102=CARTESIAN_POINT('Ctrl Pts',(0.113877102345416,0.0923071908936453,
0.896486024348064));
#14103=CARTESIAN_POINT('Ctrl Pts',(0.144383544404078,0.0546721465284523,
0.893839694468962));
#14104=CARTESIAN_POINT('Ctrl Pts',(0.15438742425262,0.000418011189221586,
0.891193364589861));
#14105=CARTESIAN_POINT('Ctrl Pts',(0.139309808695705,-0.0456222438118789,
0.888547034710759));
#14106=CARTESIAN_POINT('Ctrl Pts',(0.124232193138789,-0.0916624988129813,
0.885900704831657));
#14107=CARTESIAN_POINT('Ctrl Pts',(0.0840730821764119,-0.129488873475953,
0.883254374952555));
#14108=CARTESIAN_POINT('Ctrl Pts',(0.0372139327097935,-0.141787641004198,
0.880608045073453));
#14109=CARTESIAN_POINT('Ctrl Pts',(-0.00964521675682358,-0.154086408532443,
0.877961715194351));
#14110=CARTESIAN_POINT('Ctrl Pts',(-0.0632044047276821,-0.140857568925962,
0.875315385315249));
#14111=CARTESIAN_POINT('Ctrl Pts',(-0.0989487482345592,-0.108156170198829,
0.872669055436147));
#14112=CARTESIAN_POINT('Ctrl Pts',(-0.128680439645858,-0.0809555616469925,
0.870467871818862));
#14113=CARTESIAN_POINT('Ctrl Pts',(-0.146086572253705,-0.0402824710322022,
0.868266688201576));
#14114=CARTESIAN_POINT('Ctrl Pts',(-0.146444331750498,0.000119944961782359,
0.866065504584291));
#14115=CARTESIAN_POINT('Ctrl Pts',(-0.146471560192382,0.00011177640072981,
0.858934495415711));
#14116=CARTESIAN_POINT('Ctrl Pts',(-0.146121567926216,-0.0412390669452651,
0.861188438738147));
#14117=CARTESIAN_POINT('Ctrl Pts',(-0.127770397964496,-0.0828616943330661,
0.863442382060584));
#14118=CARTESIAN_POINT('Ctrl Pts',(-0.096778382793969,-0.110103055552942,
0.86569632538302));
#14119=CARTESIAN_POINT('Ctrl Pts',(-0.0603764330055066,-0.142099641055337,
0.86834371475728));
#14120=CARTESIAN_POINT('Ctrl Pts',(-0.00653531471701479,-0.154255992791443,
0.870991104131539));
#14121=CARTESIAN_POINT('Ctrl Pts',(0.040082974241256,-0.14100387723139,
0.873638493505799));
#14122=CARTESIAN_POINT('Ctrl Pts',(0.0867012631995282,-0.127751761671338,
0.876285882880059));
#14123=CARTESIAN_POINT('Ctrl Pts',(0.12609672282758,-0.0890911788151255,
0.878933272254319));
#14124=CARTESIAN_POINT('Ctrl Pts',(0.140224208991091,-0.042730661487191,
0.88158066162858));
#14125=CARTESIAN_POINT('Ctrl Pts',(0.154351695154603,0.00362985584074295,
0.88422805100284));
#14126=CARTESIAN_POINT('Ctrl Pts',(0.143211207853577,0.057690307640398,
0.886875440377099));
#14127=CARTESIAN_POINT('Ctrl Pts',(0.111905662524754,0.09468823006692,0.889522829751359));
#14128=CARTESIAN_POINT('Ctrl Pts',(0.0806001171959318,0.131686152493442,
0.892170219125619));
#14129=CARTESIAN_POINT('Ctrl Pts',(0.0291295138393125,0.15162154554683,
0.894817608499879));
#14130=CARTESIAN_POINT('Ctrl Pts',(-0.0189299673197759,0.145362975188259,
0.897464997874139));
#14131=CARTESIAN_POINT('Ctrl Pts',(-0.0669894484788628,0.139104404829688,
0.9001123872484));
#14132=CARTESIAN_POINT('Ctrl Pts',(-0.11163780744042,0.10665187105916,0.902759776622659));
#14133=CARTESIAN_POINT('Ctrl Pts',(-0.132423802349956,0.0628703013313112,
0.905407165996919));
#14134=CARTESIAN_POINT('Ctrl Pts',(-0.141655418982822,0.043425734493323,
0.90658294246985));
#14135=CARTESIAN_POINT('Ctrl Pts',(-0.146180218154578,0.0217465313827003,
0.907758718942781));
#14136=CARTESIAN_POINT('Ctrl Pts',(-0.146121644853617,4.41067432152685E-5,
0.908934495415711));
#14137=CARTESIAN_POINT('Origin',(0.,0.,0.));
#14138=CARTESIAN_POINT('',(-0.146345621585321,-0.000133809880645736,0.966065504584291));
#14139=CARTESIAN_POINT('',(-0.146309694201085,-0.000133223314395004,0.958934495415711));
#14140=CARTESIAN_POINT('',(-0.14635,-1.79227059055215E-17,0.));
#14141=CARTESIAN_POINT('Ctrl Pts',(-0.146345621585321,-0.000133809880645736,
0.966065504584291));
#14142=CARTESIAN_POINT('Ctrl Pts',(-0.146004672532387,0.0370537288701324,
0.964042983538364));
#14143=CARTESIAN_POINT('Ctrl Pts',(-0.131578083002406,0.0744765756810296,
0.962020462492437));
#14144=CARTESIAN_POINT('Ctrl Pts',(-0.106003654037246,0.101251356830495,
0.959997941446511));
#14145=CARTESIAN_POINT('Ctrl Pts',(-0.0725412702228666,0.136284319036219,
0.957351611567409));
#14146=CARTESIAN_POINT('Ctrl Pts',(-0.0199938687303381,0.153087872523943,
0.954705281688306));
#14147=CARTESIAN_POINT('Ctrl Pts',(0.0275867780614433,0.143970766496025,
0.952058951809204));
#14148=CARTESIAN_POINT('Ctrl Pts',(0.0751674248532248,0.134853660468108,
0.949412621930102));
#14149=CARTESIAN_POINT('Ctrl Pts',(0.11778131694426,0.0998158949245492,
0.946766292051));
#14150=CARTESIAN_POINT('Ctrl Pts',(0.135923405490256,0.0548948063954655,
0.944119962171899));
#14151=CARTESIAN_POINT('Ctrl Pts',(0.154065494036253,0.0099737178663825,
0.941473632292797));
#14152=CARTESIAN_POINT('Ctrl Pts',(0.147735779037212,-0.0448306936482241,
0.938827302413695));
#14153=CARTESIAN_POINT('Ctrl Pts',(0.119831470632095,-0.0844335867733556,
0.936180972534593));
#14154=CARTESIAN_POINT('Ctrl Pts',(0.0919271622269763,-0.124036479898489,
0.933534642655491));
#14155=CARTESIAN_POINT('Ctrl Pts',(0.0424482604157787,-0.148437854634144,
0.93088831277639));
#14156=CARTESIAN_POINT('Ctrl Pts',(-0.00595796300272124,-0.146468817862788,
0.928241982897288));
#14157=CARTESIAN_POINT('Ctrl Pts',(-0.0543641864212212,-0.144499781091432,
0.925595653018186));
#14158=CARTESIAN_POINT('Ctrl Pts',(-0.101697731447024,-0.116160332813065,
0.922949323139084));
#14159=CARTESIAN_POINT('Ctrl Pts',(-0.126293289834417,-0.0744218843624929,
0.920302993259982));
#14160=CARTESIAN_POINT('Ctrl Pts',(-0.139421333187579,-0.052143709087005,
0.918890497034752));
#14161=CARTESIAN_POINT('Ctrl Pts',(-0.146071410932229,-0.0260482098028304,
0.917478000809521));
#14162=CARTESIAN_POINT('Ctrl Pts',(-0.146114231148477,2.69008449349656E-5,
0.916065504584291));
#14163=CARTESIAN_POINT('Ctrl Pts',(-0.146121644853617,4.41067432152685E-5,
0.908934495415711));
#14164=CARTESIAN_POINT('Ctrl Pts',(-0.146048333958771,-0.027118852224649,
0.910406108317041));
#14165=CARTESIAN_POINT('Ctrl Pts',(-0.138795050353101,-0.0543181883240968,
0.91187772121837));
#14166=CARTESIAN_POINT('Ctrl Pts',(-0.124603830013468,-0.0772180274565794,
0.9133493341197));
#14167=CARTESIAN_POINT('Ctrl Pts',(-0.0990742319099257,-0.118414180831446,
0.91599672349396));
#14168=CARTESIAN_POINT('Ctrl Pts',(-0.0510914048453256,-0.145695881896007,
0.91864411286822));
#14169=CARTESIAN_POINT('Ctrl Pts',(-0.00263394834681351,-0.146566710184873,
0.92129150224248));
#14170=CARTESIAN_POINT('Ctrl Pts',(0.0458235081516972,-0.147437538473739,
0.92393889161674));
#14171=CARTESIAN_POINT('Ctrl Pts',(0.0947555940841207,-0.121897493986912,
0.926586280990999));
#14172=CARTESIAN_POINT('Ctrl Pts',(0.121748900601314,-0.0816452290135895,
0.929233670365259));
#14173=CARTESIAN_POINT('Ctrl Pts',(0.148742207118509,-0.0413929640402651,
0.931881059739519));
#14174=CARTESIAN_POINT('Ctrl Pts',(0.153796734220472,0.0135715214195569,
0.93452844911378));
#14175=CARTESIAN_POINT('Ctrl Pts',(0.134597248858856,0.0580716696672091,
0.93717583848804));
#14176=CARTESIAN_POINT('Ctrl Pts',(0.115397763497239,0.102571817914861,
0.9398232278623));
#14177=CARTESIAN_POINT('Ctrl Pts',(0.0719442656720451,0.136607628950342,
0.942470617236559));
#14178=CARTESIAN_POINT('Ctrl Pts',(0.0241406894609324,0.144588953003544,
0.945118006610819));
#14179=CARTESIAN_POINT('Ctrl Pts',(-0.023662886750181,0.152570277056746,
0.947765395985079));
#14180=CARTESIAN_POINT('Ctrl Pts',(-0.0758165413472122,0.134497114127667,
0.950412785359339));
#14181=CARTESIAN_POINT('Ctrl Pts',(-0.108431221550465,0.0986479012011113,
0.953060174733599));
#14182=CARTESIAN_POINT('Ctrl Pts',(-0.132554242808212,0.0721325001574252,
0.955018281627637));
#14183=CARTESIAN_POINT('Ctrl Pts',(-0.145988218858404,0.0358924841874147,
0.956976388521674));
#14184=CARTESIAN_POINT('Ctrl Pts',(-0.146309694201085,-0.000133223314395004,
0.958934495415711));
#14185=CARTESIAN_POINT('Origin',(0.,0.,0.));
#14186=CARTESIAN_POINT('',(-0.146565171121453,5.44893591410845E-5,1.01606550458429));
#14187=CARTESIAN_POINT('',(-0.146582076026177,3.15354312248815E-5,1.00893449541571));
#14188=CARTESIAN_POINT('',(-0.14635,-1.79227059055215E-17,0.));
#14189=CARTESIAN_POINT('Ctrl Pts',(-0.146565171121453,5.44893591410845E-5,
1.01606550458429));
#14190=CARTESIAN_POINT('Ctrl Pts',(-0.146579596851449,0.00307427920823236,
1.01590062602541));
#14191=CARTESIAN_POINT('Ctrl Pts',(-0.146494352296349,0.00609323927190738,
1.01573574746653));
#14192=CARTESIAN_POINT('Ctrl Pts',(-0.146306854564556,0.00910583530985269,
1.01557086890765));
#14193=CARTESIAN_POINT('Ctrl Pts',(-0.143297482980539,0.0574585317612167,
1.01292453902855));
#14194=CARTESIAN_POINT('Ctrl Pts',(-0.11394685994478,0.104171803331984,
1.01027820914945));
#14195=CARTESIAN_POINT('Ctrl Pts',(-0.0716892273871119,0.127864250695428,
1.00763187927034));
#14196=CARTESIAN_POINT('Ctrl Pts',(-0.0294315948294418,0.151556698058874,
1.00498554939124));
#14197=CARTESIAN_POINT('Ctrl Pts',(0.0257330472501378,0.152228321214993,
1.00233921951214));
#14198=CARTESIAN_POINT('Ctrl Pts',(0.0685549742796134,0.129571707678744,
0.999692889633039));
#14199=CARTESIAN_POINT('Ctrl Pts',(0.111376901309088,0.106915094142495,
0.997046559753937));
#14200=CARTESIAN_POINT('Ctrl Pts',(0.141856113288459,0.0609302439138786,
0.994400229874835));
#14201=CARTESIAN_POINT('Ctrl Pts',(0.146041795372579,0.0126651464112397,
0.991753899995733));
#14202=CARTESIAN_POINT('Ctrl Pts',(0.150227477456699,-0.0355999510913994,
0.989107570116631));
#14203=CARTESIAN_POINT('Ctrl Pts',(0.128119629645567,-0.0861452958680607,
0.986461240237529));
#14204=CARTESIAN_POINT('Ctrl Pts',(0.0898373616998479,-0.115835488396583,
0.983814910358427));
#14205=CARTESIAN_POINT('Ctrl Pts',(0.051555093754129,-0.145525680925106,
0.981168580479325));
#14206=CARTESIAN_POINT('Ctrl Pts',(-0.00290159432617693,-0.154360721205491,
0.978522250600224));
#14207=CARTESIAN_POINT('Ctrl Pts',(-0.0486070196525971,-0.138296672301818,
0.975875920721122));
#14208=CARTESIAN_POINT('Ctrl Pts',(-0.0943124449790173,-0.122232623398145,
0.97322959084202));
#14209=CARTESIAN_POINT('Ctrl Pts',(-0.131266607551552,-0.081269485310415,
0.970583260962917));
#14210=CARTESIAN_POINT('Ctrl Pts',(-0.142555005769704,-0.0341567308046872,
0.967936931083816));
#14211=CARTESIAN_POINT('Ctrl Pts',(-0.145215975052668,-0.0230510282813687,
0.967313122250641));
#14212=CARTESIAN_POINT('Ctrl Pts',(-0.146450780951306,-0.0116036114945705,
0.966689313417466));
#14213=CARTESIAN_POINT('Ctrl Pts',(-0.146345621585321,-0.000133809880645736,
0.966065504584291));
#14214=CARTESIAN_POINT('Ctrl Pts',(-0.146309694201085,-0.000133223314395004,
0.958934495415711));
#14215=CARTESIAN_POINT('Ctrl Pts',(-0.146422858258782,-0.0128148032088542,
0.959623777895933));
#14216=CARTESIAN_POINT('Ctrl Pts',(-0.14491119500038,-0.0254698272036438,
0.960313060376156));
#14217=CARTESIAN_POINT('Ctrl Pts',(-0.141668994059001,-0.037664762585484,
0.961002342856379));
#14218=CARTESIAN_POINT('Ctrl Pts',(-0.129216380554811,-0.0845029505214961,
0.963649732230639));
#14219=CARTESIAN_POINT('Ctrl Pts',(-0.0912354477369537,-0.12455406346949,
0.966297121604899));
#14220=CARTESIAN_POINT('Ctrl Pts',(-0.0451234138007503,-0.1394726343957,
0.968944510979159));
#14221=CARTESIAN_POINT('Ctrl Pts',(0.00098862013545236,-0.154391205321909,
0.97159190035342));
#14222=CARTESIAN_POINT('Ctrl Pts',(0.055231755190001,-0.144177234226336,
0.974239289727679));
#14223=CARTESIAN_POINT('Ctrl Pts',(0.0927598492034174,-0.113509244531313,
0.976886679101939));
#14224=CARTESIAN_POINT('Ctrl Pts',(0.130287943216833,-0.0828412548362905,
0.979534068476199));
#14225=CARTESIAN_POINT('Ctrl Pts',(0.151100996189117,-0.0317192465418168,
0.982181457850459));
#14226=CARTESIAN_POINT('Ctrl Pts',(0.145665560755875,0.0164402745715088,
0.984828847224719));
#14227=CARTESIAN_POINT('Ctrl Pts',(0.140230125322634,0.0645997956848379,
0.987476236598979));
#14228=CARTESIAN_POINT('Ctrl Pts',(0.108546201483865,0.109796829617019,
0.990123625973239));
#14229=CARTESIAN_POINT('Ctrl Pts',(0.0651266538643092,0.131328813193254,
0.992771015347499));
#14230=CARTESIAN_POINT('Ctrl Pts',(0.0217071062447581,0.152860796769488,
0.995418404721759));
#14231=CARTESIAN_POINT('Ctrl Pts',(-0.0334480651555777,0.15072772998978,
0.998065794096019));
#14232=CARTESIAN_POINT('Ctrl Pts',(-0.0750749586823209,0.125906667008376,
1.00071318347028));
#14233=CARTESIAN_POINT('Ctrl Pts',(-0.116701852209067,0.101085604026969,
1.00336057284454));
#14234=CARTESIAN_POINT('Ctrl Pts',(-0.144800467862219,0.053576544843864,
1.0060079622188));
#14235=CARTESIAN_POINT('Ctrl Pts',(-0.146500196332402,0.00514107896046776,
1.00865535159306));
#14236=CARTESIAN_POINT('Ctrl Pts',(-0.146559936783033,0.00343871495990628,
1.00874839953394));
#14237=CARTESIAN_POINT('Ctrl Pts',(-0.146587066279139,0.00173520655478852,
1.00884144747483));
#14238=CARTESIAN_POINT('Ctrl Pts',(-0.146582076026177,3.15354312248815E-5,
1.00893449541571));
#14239=CARTESIAN_POINT('Origin',(0.,0.,0.));
#14240=CARTESIAN_POINT('',(-0.146184049129756,9.96948043307314E-5,1.06606550458429));
#14241=CARTESIAN_POINT('',(-0.146216477546812,0.000114345603752017,1.05893449541571));
#14242=CARTESIAN_POINT('',(-0.14635,-1.79227059055215E-17,0.));
#14243=CARTESIAN_POINT('Ctrl Pts',(-0.146184049129756,9.96948043307314E-5,
1.06606550458429));
#14244=CARTESIAN_POINT('Ctrl Pts',(-0.146294264763128,0.0176817746259609,
1.06511193863336));
#14245=CARTESIAN_POINT('Ctrl Pts',(-0.143360807533043,0.0352283113603788,
1.06415837268242));
#14246=CARTESIAN_POINT('Ctrl Pts',(-0.13721959397524,0.0515693218739058,
1.06320480673148));
#14247=CARTESIAN_POINT('Ctrl Pts',(-0.120176538991979,0.0969187854681546,
1.06055847685238));
#14248=CARTESIAN_POINT('Ctrl Pts',(-0.0784283132238915,0.132983650068601,
1.05791214697328));
#14249=CARTESIAN_POINT('Ctrl Pts',(-0.0310837364199337,0.143256459747686,
1.05526581709418));
#14250=CARTESIAN_POINT('Ctrl Pts',(0.0162608403840241,0.153529269426771,
1.05261948721508));
#14251=CARTESIAN_POINT('Ctrl Pts',(0.0692017682238519,0.138010024184496,
1.04997315733597));
#14252=CARTESIAN_POINT('Ctrl Pts',(0.103507151520239,0.103802126728842,
1.04732682745687));
#14253=CARTESIAN_POINT('Ctrl Pts',(0.137812534816628,0.0695942292731864,
1.04468049757777));
#14254=CARTESIAN_POINT('Ctrl Pts',(0.153482373569574,0.01669767960415,1.04203416769867));
#14255=CARTESIAN_POINT('Ctrl Pts',(0.143344336052008,-0.0306759392859165,
1.03938783781957));
#14256=CARTESIAN_POINT('Ctrl Pts',(0.133206298534443,-0.0780495581759789,
1.03674150794047));
#14257=CARTESIAN_POINT('Ctrl Pts',(0.0972603847463712,-0.119900246287072,
1.03409517806136));
#14258=CARTESIAN_POINT('Ctrl Pts',(0.0519596049571008,-0.137072285243832,
1.03144884818226));
#14259=CARTESIAN_POINT('Ctrl Pts',(0.00665882516783032,-0.154244324200591,
1.02880251830316));
#14260=CARTESIAN_POINT('Ctrl Pts',(-0.0479968206226384,-0.146737714003016,
1.02615618842406));
#14261=CARTESIAN_POINT('Ctrl Pts',(-0.0869905834517384,-0.11798834823825,
1.02350985854496));
#14262=CARTESIAN_POINT('Ctrl Pts',(-0.123554854979944,-0.0910302005802824,
1.02102840722473));
#14263=CARTESIAN_POINT('Ctrl Pts',(-0.146348061346918,-0.0453938791777224,
1.01854695590451));
#14264=CARTESIAN_POINT('Ctrl Pts',(-0.146565171121453,5.44893591410845E-5,
1.01606550458429));
#14265=CARTESIAN_POINT('Ctrl Pts',(-0.146582076026177,3.15354312248815E-5,
1.00893449541571));
#14266=CARTESIAN_POINT('Ctrl Pts',(-0.146445084172466,-0.0467374494427972,
1.01148883684909));
#14267=CARTESIAN_POINT('Ctrl Pts',(-0.122102455869861,-0.0936290599181376,
1.01404317828246));
#14268=CARTESIAN_POINT('Ctrl Pts',(-0.0837162036049941,-0.120334265578335,
1.01659751971584));
#14269=CARTESIAN_POINT('Ctrl Pts',(-0.0439316411201867,-0.14801227165006,
1.0192449090901));
#14270=CARTESIAN_POINT('Ctrl Pts',(0.0109383251366414,-0.154006411209824,
1.02189229846436));
#14271=CARTESIAN_POINT('Ctrl Pts',(0.0557604321169594,-0.135571060438576,
1.02453968783862));
#14272=CARTESIAN_POINT('Ctrl Pts',(0.100582539097277,-0.11713570966733,
1.02718707721288));
#14273=CARTESIAN_POINT('Ctrl Pts',(0.135356786801084,-0.0742708685650716,
1.02983446658714));
#14274=CARTESIAN_POINT('Ctrl Pts',(0.144154783532934,-0.0266108361928598,
1.0324818559614));
#14275=CARTESIAN_POINT('Ctrl Pts',(0.152952780264784,0.0210491961793507,
1.03512924533566));
#14276=CARTESIAN_POINT('Ctrl Pts',(0.135774526024679,0.0735044198215165,
1.03777663470992));
#14277=CARTESIAN_POINT('Ctrl Pts',(0.100488543649143,0.106727647840587,
1.04042402408418));
#14278=CARTESIAN_POINT('Ctrl Pts',(0.0652025612736062,0.139950875859659,
1.04307141345844));
#14279=CARTESIAN_POINT('Ctrl Pts',(0.0118088507626404,0.153942108255635,
1.0457188028327));
#14280=CARTESIAN_POINT('Ctrl Pts',(-0.0352355257975899,0.142292641904202,
1.04836619220696));
#14281=CARTESIAN_POINT('Ctrl Pts',(-0.0822799023578202,0.130643175552769,
1.05101358158122));
#14282=CARTESIAN_POINT('Ctrl Pts',(-0.122974944967313,0.0933530104539243,
1.05366097095548));
#14283=CARTESIAN_POINT('Ctrl Pts',(-0.138680233730631,0.0475029577050484,
1.05630836032974));
#14284=CARTESIAN_POINT('Ctrl Pts',(-0.143873300563147,0.0323423075707214,
1.05718373869173));
#14285=CARTESIAN_POINT('Ctrl Pts',(-0.146334133026589,0.0162457690968458,
1.05805911705372));
#14286=CARTESIAN_POINT('Ctrl Pts',(-0.146216477546812,0.000114345603752017,
1.05893449541571));
#14287=CARTESIAN_POINT('Origin',(0.,0.,0.));
#14288=CARTESIAN_POINT('',(-0.146204073634541,-0.000109175101205505,1.11606550458429));
#14289=CARTESIAN_POINT('',(-0.146170555016798,-9.22629125885076E-5,1.10893449541571));
#14290=CARTESIAN_POINT('',(-0.14635,-1.79227059055215E-17,0.));
#14291=CARTESIAN_POINT('Ctrl Pts',(-0.146204073634541,-0.000109175101205505,
1.11606550458429));
#14292=CARTESIAN_POINT('Ctrl Pts',(-0.145981599624502,0.032003853555373,
1.1143232512413));
#14293=CARTESIAN_POINT('Ctrl Pts',(-0.135565881201595,0.0642480963468658,
1.11258099789831));
#14294=CARTESIAN_POINT('Ctrl Pts',(-0.11609067353381,0.0895073597405865,
1.11083874455532));
#14295=CARTESIAN_POINT('Ctrl Pts',(-0.0865095427755784,0.127873963375947,
1.10819241467622));
#14296=CARTESIAN_POINT('Ctrl Pts',(-0.0360273159486943,0.150125560802435,
1.10554608479712));
#14297=CARTESIAN_POINT('Ctrl Pts',(0.0122494975033169,0.14607724579886,
1.10289975491801));
#14298=CARTESIAN_POINT('Ctrl Pts',(0.0605263109553308,0.142028930795284,
1.10025342503891));
#14299=CARTESIAN_POINT('Ctrl Pts',(0.10659771103247,0.111680703361642,1.09760709515981));
#14300=CARTESIAN_POINT('Ctrl Pts',(0.129376093089052,0.0689234246557527,
1.09496076528071));
#14301=CARTESIAN_POINT('Ctrl Pts',(0.152154475145634,0.0261661459498645,
1.09231443540161));
#14302=CARTESIAN_POINT('Ctrl Pts',(0.151639839181659,-0.0290001840282729,
1.0896681055225));
#14303=CARTESIAN_POINT('Ctrl Pts',(0.128067742174483,-0.0713250681289163,
1.0870217756434));
#14304=CARTESIAN_POINT('Ctrl Pts',(0.104495645167307,-0.11364995222956,
1.0843754457643));
#14305=CARTESIAN_POINT('Ctrl Pts',(0.0578660871169326,-0.143133390452712,
1.0817291158852));
#14306=CARTESIAN_POINT('Ctrl Pts',(0.00952215035475689,-0.146280349267719,
1.0790827860061));
#14307=CARTESIAN_POINT('Ctrl Pts',(-0.0388217864074202,-0.149427308082725,
1.07643645612699));
#14308=CARTESIAN_POINT('Ctrl Pts',(-0.0888801018813974,-0.126237787489585,
1.07379012624789));
#14309=CARTESIAN_POINT('Ctrl Pts',(-0.117740317519168,-0.0873259958989869,
1.07114379636879));
#14310=CARTESIAN_POINT('Ctrl Pts',(-0.136201180005177,-0.0624354946409797,
1.06945103244062));
#14311=CARTESIAN_POINT('Ctrl Pts',(-0.145988395071105,-0.0311118962502767,
1.06775826851246));
#14312=CARTESIAN_POINT('Ctrl Pts',(-0.146184049129756,9.96948043307314E-5,
1.06606550458429));
#14313=CARTESIAN_POINT('Ctrl Pts',(-0.146216477546812,0.000114345603752017,
1.05893449541571));
#14314=CARTESIAN_POINT('Ctrl Pts',(-0.145978309898544,-0.0325401742182177,
1.06070650642798));
#14315=CARTESIAN_POINT('Ctrl Pts',(-0.135174246449945,-0.06533764273189,
1.06247851744025));
#14316=CARTESIAN_POINT('Ctrl Pts',(-0.115079600404687,-0.0908043159161929,
1.06425052845252));
#14317=CARTESIAN_POINT('Ctrl Pts',(-0.0850581433982766,-0.128851596389654,
1.06689791782678));
#14318=CARTESIAN_POINT('Ctrl Pts',(-0.0342996944683099,-0.150536216937668,
1.06954530720104));
#14319=CARTESIAN_POINT('Ctrl Pts',(0.0139457694684962,-0.145925507476389,
1.0721926965753));
#14320=CARTESIAN_POINT('Ctrl Pts',(0.0621912334052997,-0.14131479801511,
1.07484008594956));
#14321=CARTESIAN_POINT('Ctrl Pts',(0.107923712348941,-0.110408758544542,
1.07748747532382));
#14322=CARTESIAN_POINT('Ctrl Pts',(0.1301953818052,-0.0673639426912374,
1.08013486469808));
#14323=CARTESIAN_POINT('Ctrl Pts',(0.15246705126146,-0.024319126837932,
1.08278225407234));
#14324=CARTESIAN_POINT('Ctrl Pts',(0.151277911230334,0.0308644653981125,
1.0854296434466));
#14325=CARTESIAN_POINT('Ctrl Pts',(0.127172648928576,0.0729099141598672,
1.08807703282086));
#14326=CARTESIAN_POINT('Ctrl Pts',(0.103067386626818,0.114955362921624,
1.09072442219512));
#14327=CARTESIAN_POINT('Ctrl Pts',(0.0560460020544268,0.143862668209093,
1.09337181156938));
#14328=CARTESIAN_POINT('Ctrl Pts',(0.00764670469074742,0.146390799320458,
1.09601920094364));
#14329=CARTESIAN_POINT('Ctrl Pts',(-0.0407525926729279,0.148918930431823,
1.0986665903179));
#14330=CARTESIAN_POINT('Ctrl Pts',(-0.0905298028278899,0.125067887367091,
1.10131397969216));
#14331=CARTESIAN_POINT('Ctrl Pts',(-0.11888440661962,0.0857626730052823,
1.10396136906642));
#14332=CARTESIAN_POINT('Ctrl Pts',(-0.136639133674055,0.0611510311732957,
1.10561907784952));
#14333=CARTESIAN_POINT('Ctrl Pts',(-0.145994366384503,0.0304800321277272,
1.10727678663261));
#14334=CARTESIAN_POINT('Ctrl Pts',(-0.146170555016798,-9.22629125885076E-5,
1.10893449541571));
#14335=CARTESIAN_POINT('Origin',(0.,0.,0.));
#14336=CARTESIAN_POINT('',(-0.146577386142569,-3.88073511912723E-5,1.16606550458429));
#14337=CARTESIAN_POINT('',(-0.146552328192774,-6.73160170860698E-5,1.15893449541571));
#14338=CARTESIAN_POINT('',(-0.14635,-1.79227059055215E-17,0.));
#14339=CARTESIAN_POINT('Ctrl Pts',(-0.146577386142569,-3.88073511912723E-5,
1.16606550458429));
#14340=CARTESIAN_POINT('Ctrl Pts',(-0.146413350709018,0.0463056768050285,
1.16353456384924));
#14341=CARTESIAN_POINT('Ctrl Pts',(-0.122574225104448,0.0927954474992645,
1.1610036231142));
#14342=CARTESIAN_POINT('Ctrl Pts',(-0.0847742546295189,0.119590709008994,
1.15847268237915));
#14343=CARTESIAN_POINT('Ctrl Pts',(-0.0452509303920754,0.147607604138013,
1.15582635250005));
#14344=CARTESIAN_POINT('Ctrl Pts',(0.00953524646069181,0.154093252855687,
1.15318002262095));
#14345=CARTESIAN_POINT('Ctrl Pts',(0.0545077808453859,0.136079071706768,
1.15053369274185));
#14346=CARTESIAN_POINT('Ctrl Pts',(0.0994803152300801,0.118064890557849,
1.14788736286275));
#14347=CARTESIAN_POINT('Ctrl Pts',(0.134639207146701,0.0755508795423365,
1.14524103298364));
#14348=CARTESIAN_POINT('Ctrl Pts',(0.14389167861853,0.027996370364851,1.14259470310454));
#14349=CARTESIAN_POINT('Ctrl Pts',(0.15314415009036,-0.0195581388126345,
1.13994837322544));
#14350=CARTESIAN_POINT('Ctrl Pts',(0.136490201117397,-0.0721531461520931,
1.13730204334634));
#14351=CARTESIAN_POINT('Ctrl Pts',(0.101552606157185,-0.105715089329518,
1.13465571346724));
#14352=CARTESIAN_POINT('Ctrl Pts',(0.0666150111969725,-0.139277032506943,
1.13200938358813));
#14353=CARTESIAN_POINT('Ctrl Pts',(0.0133937702495101,-0.153805911522335,
1.12936305370903));
#14354=CARTESIAN_POINT('Ctrl Pts',(-0.033750917386428,-0.142651629870951,
1.12671672382993));
#14355=CARTESIAN_POINT('Ctrl Pts',(-0.0808956050223675,-0.131497348219567,
1.12407039395083));
#14356=CARTESIAN_POINT('Ctrl Pts',(-0.121963739346782,-0.094659905901407,
1.12142406407173));
#14357=CARTESIAN_POINT('Ctrl Pts',(-0.1381577891642,-0.0490003798202082,
1.11877773419262));
#14358=CARTESIAN_POINT('Ctrl Pts',(-0.143690228857438,-0.0334015285560649,
1.11787365765651));
#14359=CARTESIAN_POINT('Ctrl Pts',(-0.146319518115206,-0.0167730178360648,
1.1169695811204));
#14360=CARTESIAN_POINT('Ctrl Pts',(-0.146204073634541,-0.000109175101205505,
1.11606550458429));
#14361=CARTESIAN_POINT('Ctrl Pts',(-0.146170555016798,-9.22629125885076E-5,
1.10893449541571));
#14362=CARTESIAN_POINT('Ctrl Pts',(-0.146275742653821,-0.0183444476975235,
1.10992417600687));
#14363=CARTESIAN_POINT('Ctrl Pts',(-0.143109248288425,-0.0365614514641733,
1.11091385659804));
#14364=CARTESIAN_POINT('Ctrl Pts',(-0.136505188007283,-0.0534328725168923,
1.1119035371892));
#14365=CARTESIAN_POINT('Ctrl Pts',(-0.118839368174718,-0.0985638180183679,
1.11455092656346));
#14366=CARTESIAN_POINT('Ctrl Pts',(-0.0765757310810901,-0.134066323362434,
1.11719831593772));
#14367=CARTESIAN_POINT('Ctrl Pts',(-0.0290731934694857,-0.143678417446031,
1.11984570531198));
#14368=CARTESIAN_POINT('Ctrl Pts',(0.01842934414212,-0.153290511529629,
1.12249309468624));
#14369=CARTESIAN_POINT('Ctrl Pts',(0.071170782271703,-0.137012194352758,
1.1251404840605));
#14370=CARTESIAN_POINT('Ctrl Pts',(0.10499283308901,-0.102299771349957,
1.12778787343476));
#14371=CARTESIAN_POINT('Ctrl Pts',(0.138814883906317,-0.0675873483471558,
1.13043526280902));
#14372=CARTESIAN_POINT('Ctrl Pts',(0.153717547411349,-0.0144408195184256,
1.13308265218328));
#14373=CARTESIAN_POINT('Ctrl Pts',(0.142874638214406,0.0327959749574983,
1.13573004155754));
#14374=CARTESIAN_POINT('Ctrl Pts',(0.132031729017462,0.0800327694334235,
1.1383774309318));
#14375=CARTESIAN_POINT('Ctrl Pts',(0.0954432471185425,0.121359829556542,
1.14102482030606));
#14376=CARTESIAN_POINT('Ctrl Pts',(0.0498685966661331,0.137847238945365,
1.14367220968032));
#14377=CARTESIAN_POINT('Ctrl Pts',(0.00429394621372511,0.154334648334189,
1.14631959905458));
#14378=CARTESIAN_POINT('Ctrl Pts',(-0.0502668727921719,0.145982406988718,
1.14896698842884));
#14379=CARTESIAN_POINT('Ctrl Pts',(-0.0888222026239048,0.116616270474356,
1.1516143778031));
#14380=CARTESIAN_POINT('Ctrl Pts',(-0.124357782404925,0.0895501633622979,
1.1540544170073));
#14381=CARTESIAN_POINT('Ctrl Pts',(-0.146296868742479,0.0446329749882746,
1.15649445621151));
#14382=CARTESIAN_POINT('Ctrl Pts',(-0.146552328192774,-6.73160170860698E-5,
1.15893449541571));
#14383=CARTESIAN_POINT('Origin',(0.,0.,0.));
#14384=CARTESIAN_POINT('',(-0.146318311025392,0.000133437649768732,1.21606550458429));
#14385=CARTESIAN_POINT('',(-0.146373054956946,0.000132657382717961,1.20893449541571));
#14386=CARTESIAN_POINT('',(-0.14635,-1.79227059055215E-17,0.));
#14387=CARTESIAN_POINT('Ctrl Pts',(-0.146318311025392,0.000133437649768732,
1.21606550458429));
#14388=CARTESIAN_POINT('Ctrl Pts',(-0.146429658069886,0.0125190846592594,
1.21539220633629));
#14389=CARTESIAN_POINT('Ctrl Pts',(-0.144988168643405,0.0248791929292086,
1.21471890808829));
#14390=CARTESIAN_POINT('Ctrl Pts',(-0.141892968227885,0.0368102906365087,
1.21404560984029));
#14391=CARTESIAN_POINT('Ctrl Pts',(-0.129727599662405,0.083704249513052,
1.21139927996119));
#14392=CARTESIAN_POINT('Ctrl Pts',(-0.0920156607298113,0.123970842060419,
1.20875295008209));
#14393=CARTESIAN_POINT('Ctrl Pts',(-0.0460184991925076,0.139179415364965,
1.20610662020299));
#14394=CARTESIAN_POINT('Ctrl Pts',(-2.13376552038805E-5,0.15438798866951,
1.20346029032389));
#14395=CARTESIAN_POINT('Ctrl Pts',(0.0542610464868107,0.144538542731236,
1.20081396044478));
#14396=CARTESIAN_POINT('Ctrl Pts',(0.091982751999895,0.114139323915075,
1.19816763056568));
#14397=CARTESIAN_POINT('Ctrl Pts',(0.129704457512977,0.0837401050989159,
1.19552130068658));
#14398=CARTESIAN_POINT('Ctrl Pts',(0.150865484397133,0.0327911134048729,
1.19287497080748));
#14399=CARTESIAN_POINT('Ctrl Pts',(0.145780097726084,-0.0153874961003253,
1.19022864092838));
#14400=CARTESIAN_POINT('Ctrl Pts',(0.140694711055036,-0.063566105605525,
1.18758231104927));
#14401=CARTESIAN_POINT('Ctrl Pts',(0.109362910828785,-0.108974332921877,
1.18493598117017));
#14402=CARTESIAN_POINT('Ctrl Pts',(0.0661257549466402,-0.130828118009858,
1.18228965129107));
#14403=CARTESIAN_POINT('Ctrl Pts',(0.0228885990644955,-0.152681903097838,
1.17964332141197));
#14404=CARTESIAN_POINT('Ctrl Pts',(-0.0322539124735426,-0.150981245957443,
1.17699699153287));
#14405=CARTESIAN_POINT('Ctrl Pts',(-0.0740621845924981,-0.126504564117865,
1.17435066165376));
#14406=CARTESIAN_POINT('Ctrl Pts',(-0.115870456711455,-0.102027882278287,
1.17170433177466));
#14407=CARTESIAN_POINT('Ctrl Pts',(-0.144344489411329,-0.0547751757395235,
1.16905800189556));
#14408=CARTESIAN_POINT('Ctrl Pts',(-0.146451269950206,-0.00637475169995868,
1.16641167201646));
#14409=CARTESIAN_POINT('Ctrl Pts',(-0.146543132875163,-0.00426432565444621,
1.1662962828724));
#14410=CARTESIAN_POINT('Ctrl Pts',(-0.146584864748453,-0.00215171749738942,
1.16618089372835));
#14411=CARTESIAN_POINT('Ctrl Pts',(-0.146577386142569,-3.88073511912723E-5,
1.16606550458429));
#14412=CARTESIAN_POINT('Ctrl Pts',(-0.146552328192774,-6.73160170860698E-5,
1.15893449541571));
#14413=CARTESIAN_POINT('Ctrl Pts',(-0.146574036680232,-0.00386586684592084,
1.15914184558577));
#14414=CARTESIAN_POINT('Ctrl Pts',(-0.1464391612665,-0.00766285139452399,
1.15934919575582));
#14415=CARTESIAN_POINT('Ctrl Pts',(-0.146142739258869,-0.0114471821958193,
1.15955654592588));
#14416=CARTESIAN_POINT('Ctrl Pts',(-0.142358105404532,-0.0597644666683822,
1.16220393530014));
#14417=CARTESIAN_POINT('Ctrl Pts',(-0.112238997038288,-0.106019003930254,
1.1648513246744));
#14418=CARTESIAN_POINT('Ctrl Pts',(-0.0695815129186611,-0.129023839960917,
1.16749871404866));
#14419=CARTESIAN_POINT('Ctrl Pts',(-0.026924028799035,-0.15202867599158,
1.17014610342292));
#14420=CARTESIAN_POINT('Ctrl Pts',(0.0282718310739737,-0.151783810791035,
1.17279349279718));
#14421=CARTESIAN_POINT('Ctrl Pts',(0.0707235276354612,-0.128401405199111,
1.17544088217144));
#14422=CARTESIAN_POINT('Ctrl Pts',(0.11317522419695,-0.105018999607187,
1.1780882715457));
#14423=CARTESIAN_POINT('Ctrl Pts',(0.142882757446916,-0.0584990536238821,
1.18073566091996));
#14424=CARTESIAN_POINT('Ctrl Pts',(0.146238551171451,-0.0101500920973681,
1.18338305029422));
#14425=CARTESIAN_POINT('Ctrl Pts',(0.149594344895986,0.0381988694291446,
1.18603043966848));
#14426=CARTESIAN_POINT('Ctrl Pts',(0.12659839909509,0.0883768464988665,
1.18867782904274));
#14427=CARTESIAN_POINT('Ctrl Pts',(0.0877840381772113,0.117399748124142,
1.191325218417));
#14428=CARTESIAN_POINT('Ctrl Pts',(0.0489696772593311,0.146422649749419,
1.19397260779126));
#14429=CARTESIAN_POINT('Ctrl Pts',(-0.00566309877553352,0.154290475930249,
1.19661999716552));
#14430=CARTESIAN_POINT('Ctrl Pts',(-0.0510896721842483,0.137399358129564,
1.19926738653978));
#14431=CARTESIAN_POINT('Ctrl Pts',(-0.0965162455929618,0.12050824032888,
1.20191477591404));
#14432=CARTESIAN_POINT('Ctrl Pts',(-0.132736616375526,0.0788581785466829,
1.2045621652883));
#14433=CARTESIAN_POINT('Ctrl Pts',(-0.143159994183491,0.0315270405159292,
1.20720955466256));
#14434=CARTESIAN_POINT('Ctrl Pts',(-0.145423823013163,0.021247302336111,
1.20778453491361));
#14435=CARTESIAN_POINT('Ctrl Pts',(-0.146470795531708,0.0106995851133921,
1.20835951516466));
#14436=CARTESIAN_POINT('Ctrl Pts',(-0.146373054956946,0.000132657382717961,
1.20893449541571));
#14437=CARTESIAN_POINT('Origin',(0.,0.,0.));
#14438=CARTESIAN_POINT('',(-0.146120596765396,-4.14129048147555E-5,1.26606550458429));
#14439=CARTESIAN_POINT('',(-0.146109918970638,-1.0198006988139E-5,1.25893449541571));
#14440=CARTESIAN_POINT('',(-0.14635,-1.79227059055215E-17,0.));
#14441=CARTESIAN_POINT('Ctrl Pts',(-0.146120596765396,-4.14129048147555E-5,
1.26606550458429));
#14442=CARTESIAN_POINT('Ctrl Pts',(-0.14605219935785,0.0269443530192317,
1.26460351894424));
#14443=CARTESIAN_POINT('Ctrl Pts',(-0.138898723445843,0.053963836666407,
1.26314153330418));
#14444=CARTESIAN_POINT('Ctrl Pts',(-0.124882896249422,0.0767650581554474,
1.26167954766413));
#14445=CARTESIAN_POINT('Ctrl Pts',(-0.0995129464537159,0.118037388097231,
1.25903321778503));
#14446=CARTESIAN_POINT('Ctrl Pts',(-0.051658938874944,0.145488850208621,
1.25638688790592));
#14447=CARTESIAN_POINT('Ctrl Pts',(-0.00322440565727106,0.146554478394238,
1.25374055802682));
#14448=CARTESIAN_POINT('Ctrl Pts',(0.0452101275604033,0.147620106579856,
1.25109422814772));
#14449=CARTESIAN_POINT('Ctrl Pts',(0.0942251864169787,0.122299900839699,
1.24844789826862));
#14450=CARTESIAN_POINT('Ctrl Pts',(0.121385807331354,0.0821833176976391,
1.24580156838952));
#14451=CARTESIAN_POINT('Ctrl Pts',(0.148546428245729,0.0420667345555804,
1.24315523851041));
#14452=CARTESIAN_POINT('Ctrl Pts',(0.153852611217905,-0.0128462259883804,
1.24050890863131));
#14453=CARTESIAN_POINT('Ctrl Pts',(0.134875632820701,-0.0574210379606392,
1.23786257875221));
#14454=CARTESIAN_POINT('Ctrl Pts',(0.115898654423498,-0.101995849932898,
1.23521624887311));
#14455=CARTESIAN_POINT('Ctrl Pts',(0.0726385146569148,-0.136232513333455,
1.23256991899401));
#14456=CARTESIAN_POINT('Ctrl Pts',(0.0248960600935515,-0.144460368686643,
1.2299235891149));
#14457=CARTESIAN_POINT('Ctrl Pts',(-0.0228463944698117,-0.152688224039831,
1.2272772592358));
#14458=CARTESIAN_POINT('Ctrl Pts',(-0.0750711638299551,-0.134907271345651,
1.2246309293567));
#14459=CARTESIAN_POINT('Ctrl Pts',(-0.107874149410843,-0.0992561323957017,
1.2219845994776));
#14460=CARTESIAN_POINT('Ctrl Pts',(-0.132331163880887,-0.072675612185966,
1.2200115678465));
#14461=CARTESIAN_POINT('Ctrl Pts',(-0.145992019903337,-0.0361614337449312,
1.21803853621539));
#14462=CARTESIAN_POINT('Ctrl Pts',(-0.146318311025392,0.000133437649768732,
1.21606550458429));
#14463=CARTESIAN_POINT('Ctrl Pts',(-0.146373054956946,0.000132657382717961,
1.20893449541571));
#14464=CARTESIAN_POINT('Ctrl Pts',(-0.146020767276673,-0.0379538636644633,
1.21100690453892));
#14465=CARTESIAN_POINT('Ctrl Pts',(-0.130797424420382,-0.0762899498869128,
1.21307931366213));
#14466=CARTESIAN_POINT('Ctrl Pts',(-0.104081054125652,-0.103227285106232,
1.21515172278534));
#14467=CARTESIAN_POINT('Ctrl Pts',(-0.0699523514264828,-0.137638258418326,
1.2177991121596));
#14468=CARTESIAN_POINT('Ctrl Pts',(-0.0170685611947798,-0.153447990763203,
1.22044650153386));
#14469=CARTESIAN_POINT('Ctrl Pts',(0.0303468241642401,-0.143414812629152,
1.22309389090812));
#14470=CARTESIAN_POINT('Ctrl Pts',(0.0777622095232573,-0.133381634495101,
1.22574128028238));
#14471=CARTESIAN_POINT('Ctrl Pts',(0.119709190009594,-0.0975055458821257,
1.22838866965664));
#14472=CARTESIAN_POINT('Ctrl Pts',(0.136973893871985,-0.052219638220276,
1.2310360590309));
#14473=CARTESIAN_POINT('Ctrl Pts',(0.154238597734379,-0.00693373055842239,
1.23368344840516));
#14474=CARTESIAN_POINT('Ctrl Pts',(0.146821024972825,0.0477619961523044,
1.23633083777942));
#14475=CARTESIAN_POINT('Ctrl Pts',(0.118118804930222,0.0868140895256425,
1.23897822715368));
#14476=CARTESIAN_POINT('Ctrl Pts',(0.0894165848876198,0.125866182898978,
1.24162561652794));
#14477=CARTESIAN_POINT('Ctrl Pts',(0.0394297175639698,0.149274642934924,
1.2442730059022));
#14478=CARTESIAN_POINT('Ctrl Pts',(-0.00894524413350711,0.146317192515786,
1.24692039527646));
#14479=CARTESIAN_POINT('Ctrl Pts',(-0.0573202058309854,0.143359742096648,
1.24956778465072));
#14480=CARTESIAN_POINT('Ctrl Pts',(-0.104083261902292,0.114036381222425,
1.25221517402498));
#14481=CARTESIAN_POINT('Ctrl Pts',(-0.127814530591109,0.0717787154251623,
1.25486256339924));
#14482=CARTESIAN_POINT('Ctrl Pts',(-0.139981499518435,0.0501133037087236,
1.2562198740714));
#14483=CARTESIAN_POINT('Ctrl Pts',(-0.146094355379323,0.0250479932723348,
1.25757718474355));
#14484=CARTESIAN_POINT('Ctrl Pts',(-0.146109918970638,-1.0198006988139E-5,
1.25893449541571));
#14485=CARTESIAN_POINT('Origin',(0.,0.,0.));
#14486=CARTESIAN_POINT('',(-0.146470135615938,-0.000111966546850736,1.31606550458429));
#14487=CARTESIAN_POINT('',(-0.146410535958061,-0.000127756381200432,1.30893449541571));
#14488=CARTESIAN_POINT('',(-0.14635,-1.79227059055215E-17,0.));
#14489=CARTESIAN_POINT('Ctrl Pts',(-0.146470135615938,-0.000111966546850736,
1.31606550458429));
#14490=CARTESIAN_POINT('Ctrl Pts',(-0.146120207411574,0.0411799307449602,
1.31381483155218));
#14491=CARTESIAN_POINT('Ctrl Pts',(-0.127827491572984,0.0827431563937987,
1.31156415852007));
#14492=CARTESIAN_POINT('Ctrl Pts',(-0.0969137672218927,0.10998333351997,
1.30931348548796));
#14493=CARTESIAN_POINT('Ctrl Pts',(-0.0605655677022408,0.142012194937238,
1.30666715560886));
#14494=CARTESIAN_POINT('Ctrl Pts',(-0.00676890401288169,0.154239532672684,
1.30402082572976));
#14495=CARTESIAN_POINT('Ctrl Pts',(0.0398526445220406,0.14106870189023,
1.30137449585066));
#14496=CARTESIAN_POINT('Ctrl Pts',(0.0864741930569617,0.127897871107775,
1.29872816597155));
#14497=CARTESIAN_POINT('Ctrl Pts',(0.125920626437448,0.0893288718074177,
1.29608183609245));
#14498=CARTESIAN_POINT('Ctrl Pts',(0.14013669149516,0.0430153417578024,
1.29343550621335));
#14499=CARTESIAN_POINT('Ctrl Pts',(0.154352756552873,-0.00329818829181684,
1.29078917633425));
#14500=CARTESIAN_POINT('Ctrl Pts',(0.143338453287813,-0.0573562490906975,
1.28814284645515));
#14501=CARTESIAN_POINT('Ctrl Pts',(0.112135201594409,-0.0944156157243562,
1.28549651657604));
#14502=CARTESIAN_POINT('Ctrl Pts',(0.0809319499010078,-0.131474982358013,
1.28285018669694));
#14503=CARTESIAN_POINT('Ctrl Pts',(0.0295397497792676,-0.151535654826449,
1.28020385681784));
#14504=CARTESIAN_POINT('Ctrl Pts',(-0.0185183802362589,-0.1454155477333,
1.27755752693874));
#14505=CARTESIAN_POINT('Ctrl Pts',(-0.066576510251784,-0.139295440640151,
1.27491119705964));
#14506=CARTESIAN_POINT('Ctrl Pts',(-0.111300570161094,-0.106994553985419,
1.27226486718053));
#14507=CARTESIAN_POINT('Ctrl Pts',(-0.13221965410943,-0.0632975117719662,
1.26961853730143));
#14508=CARTESIAN_POINT('Ctrl Pts',(-0.141581826511298,-0.0437412423069929,
1.26843419306239));
#14509=CARTESIAN_POINT('Ctrl Pts',(-0.146176005022067,-0.0219023912433209,
1.26724984882334));
#14510=CARTESIAN_POINT('Ctrl Pts',(-0.146120596765396,-4.14129048147555E-5,
1.26606550458429));
#14511=CARTESIAN_POINT('Ctrl Pts',(-0.146109918970638,-1.0198006988139E-5,
1.25893449541571));
#14512=CARTESIAN_POINT('Ctrl Pts',(-0.146124711647138,-0.0238271763493914,
1.26022457411781));
#14513=CARTESIAN_POINT('Ctrl Pts',(-0.140631289159497,-0.0476377233371588,
1.26151465281992));
#14514=CARTESIAN_POINT('Ctrl Pts',(-0.129592576141605,-0.0685164391025303,
1.26280473152202));
#14515=CARTESIAN_POINT('Ctrl Pts',(-0.106939871696956,-0.111361957112663,
1.26545212089628));
#14516=CARTESIAN_POINT('Ctrl Pts',(-0.0609349815013302,-0.141861022412626,
1.26809951027054));
#14517=CARTESIAN_POINT('Ctrl Pts',(-0.0126505083952331,-0.146043496451057,
1.2707468996448));
#14518=CARTESIAN_POINT('Ctrl Pts',(0.0356339647108625,-0.150225970489488,
1.27339428901906));
#14519=CARTESIAN_POINT('Ctrl Pts',(0.0861980207274291,-0.128091853266388,
1.27604167839332));
#14520=CARTESIAN_POINT('Ctrl Pts',(0.11588072467734,-0.0897797074320025,
1.27868906776758));
#14521=CARTESIAN_POINT('Ctrl Pts',(0.145563428627253,-0.0514675615976161,
1.28133645714184));
#14522=CARTESIAN_POINT('Ctrl Pts',(0.154364780510509,0.00302261284805656,
1.2839838465161));
#14523=CARTESIAN_POINT('Ctrl Pts',(0.138253309066183,0.0487315170146188,
1.28663123589036));
#14524=CARTESIAN_POINT('Ctrl Pts',(0.122141837621857,0.0944404211811797,
1.28927862526462));
#14525=CARTESIAN_POINT('Ctrl Pts',(0.0811175428499519,0.131368055068631,
1.29192601463888));
#14526=CARTESIAN_POINT('Ctrl Pts',(0.0339716590485425,0.142599665496764,
1.29457340401314));
#14527=CARTESIAN_POINT('Ctrl Pts',(-0.013174224752867,0.153831275924897,
1.2972207933874));
#14528=CARTESIAN_POINT('Ctrl Pts',(-0.0664416975837803,0.139366862893713,
1.29986818276166));
#14529=CARTESIAN_POINT('Ctrl Pts',(-0.101431520699135,0.105831870563862,
1.30251557213592));
#14530=CARTESIAN_POINT('Ctrl Pts',(-0.129710573305276,0.0787286237393239,
1.30465521322918));
#14531=CARTESIAN_POINT('Ctrl Pts',(-0.146050663974784,0.0391684733249047,
1.30679485432245));
#14532=CARTESIAN_POINT('Ctrl Pts',(-0.146410535958061,-0.000127756381200432,
1.30893449541571));
#14533=CARTESIAN_POINT('Origin',(0.,0.,0.));
#14534=CARTESIAN_POINT('',(-0.146471469669193,0.000111495080380188,1.36606550458429));
#14535=CARTESIAN_POINT('',(-0.146526884620975,8.5711493927648E-5,1.35893449541571));
#14536=CARTESIAN_POINT('',(-0.14635,-1.79227059055215E-17,0.));
#14537=CARTESIAN_POINT('Ctrl Pts',(-0.146471469669193,0.000111495080380188,
1.36606550458429));
#14538=CARTESIAN_POINT('Ctrl Pts',(-0.146532402405025,0.0073220458586883,
1.36567247403923));
#14539=CARTESIAN_POINT('Ctrl Pts',(-0.146045973070864,0.0145243451116175,
1.36527944349416));
#14540=CARTESIAN_POINT('Ctrl Pts',(-0.144983764805735,0.0216407019395156,
1.3648864129491));
#14541=CARTESIAN_POINT('Ctrl Pts',(-0.137831767320671,0.0695561322809842,
1.36224008307));
#14542=CARTESIAN_POINT('Ctrl Pts',(-0.104576727819841,0.113575347233418,
1.3595937531909));
#14543=CARTESIAN_POINT('Ctrl Pts',(-0.060440002550743,0.133550058215342,
1.3569474233118));
#14544=CARTESIAN_POINT('Ctrl Pts',(-0.0163032772816473,0.153524769197265,
1.35430109343269));
#14545=CARTESIAN_POINT('Ctrl Pts',(0.0387151337557165,0.149454976208681,
1.35165476355359));
#14546=CARTESIAN_POINT('Ctrl Pts',(0.0794324390145508,0.123203488242689,
1.34900843367449));
#14547=CARTESIAN_POINT('Ctrl Pts',(0.120149744273387,0.0969520002766962,
1.34636210379539));
#14548=CARTESIAN_POINT('Ctrl Pts',(0.146565943753694,0.048518817333291,
1.34371577391629));
#14549=CARTESIAN_POINT('Ctrl Pts',(0.14658992694451,7.25688577880009E-5,
1.34106944403718));
#14550=CARTESIAN_POINT('Ctrl Pts',(0.146613910135327,-0.0483736796177136,
1.33842311415808));
#14551=CARTESIAN_POINT('Ctrl Pts',(0.120245677036657,-0.0968329936253116,
1.33577678427898));
#14552=CARTESIAN_POINT('Ctrl Pts',(0.0795543829983497,-0.123124782547022,
1.33313045439988));
#14553=CARTESIAN_POINT('Ctrl Pts',(0.0388630889600415,-0.149416571468734,
1.33048412452078));
#14554=CARTESIAN_POINT('Ctrl Pts',(-0.0161512660179049,-0.153540835304554,
1.32783779464168));
#14555=CARTESIAN_POINT('Ctrl Pts',(-0.0603077462478081,-0.133609833714981,
1.32519146476257));
#14556=CARTESIAN_POINT('Ctrl Pts',(-0.10446422647771,-0.113678832125408,
1.32254513488347));
#14557=CARTESIAN_POINT('Ctrl Pts',(-0.137762831959571,-0.0696925651104417,
1.31989880500437));
#14558=CARTESIAN_POINT('Ctrl Pts',(-0.144962267025529,-0.0217842390534145,
1.31725247512527));
#14559=CARTESIAN_POINT('Ctrl Pts',(-0.146038665626028,-0.0146213916011371,
1.31685681827827));
#14560=CARTESIAN_POINT('Ctrl Pts',(-0.146531651210624,-0.00737087161912708,
1.31646116143128));
#14561=CARTESIAN_POINT('Ctrl Pts',(-0.146470135615938,-0.000111966546850736,
1.31606550458429));
#14562=CARTESIAN_POINT('Ctrl Pts',(-0.146410535958061,-0.000127756381200432,
1.30893449541571));
#14563=CARTESIAN_POINT('Ctrl Pts',(-0.146495935505426,-0.00945296197092968,
1.30944224369671));
#14564=CARTESIAN_POINT('Ctrl Pts',(-0.145681427739287,-0.018763305174839,
1.3099499919777));
#14565=CARTESIAN_POINT('Ctrl Pts',(-0.143913007029536,-0.0278887903271487,
1.3104577402587));
#14566=CARTESIAN_POINT('Ctrl Pts',(-0.134692496844786,-0.0754688872597875,
1.31310512963296));
#14567=CARTESIAN_POINT('Ctrl Pts',(-0.0995393030754929,-0.118023509496548,
1.31575251900722));
#14568=CARTESIAN_POINT('Ctrl Pts',(-0.0545553941775042,-0.136060454153345,
1.31839990838148));
#14569=CARTESIAN_POINT('Ctrl Pts',(-0.00957148527951295,-0.154097398810142,
1.32104729775574));
#14570=CARTESIAN_POINT('Ctrl Pts',(0.0452431387471776,-0.14761666588697,
1.32369468713));
#14571=CARTESIAN_POINT('Ctrl Pts',(0.0847805644327026,-0.119586763955155,
1.32634207650426));
#14572=CARTESIAN_POINT('Ctrl Pts',(0.124317990118227,-0.09155686202334,
1.32898946587852));
#14573=CARTESIAN_POINT('Ctrl Pts',(0.148578217462589,-0.041977791082884,
1.33163685525278));
#14574=CARTESIAN_POINT('Ctrl Pts',(0.146448816178573,0.00644068764408242,
1.33428424462704));
#14575=CARTESIAN_POINT('Ctrl Pts',(0.144319414894557,0.0548591663710502,
1.3369316340013));
#14576=CARTESIAN_POINT('Ctrl Pts',(0.115800384982161,0.102117052884526,
1.33957902337556));
#14577=CARTESIAN_POINT('Ctrl Pts',(0.0739549070570988,0.126567807678519,
1.34222641274982));
#14578=CARTESIAN_POINT('Ctrl Pts',(0.0321094291320376,0.151018562472512,
1.34487380212408));
#14579=CARTESIAN_POINT('Ctrl Pts',(-0.0230624968056921,0.152662185547021,
1.34752119149834));
#14580=CARTESIAN_POINT('Ctrl Pts',(-0.0662892946253695,0.1307458130856,
1.3501685808726));
#14581=CARTESIAN_POINT('Ctrl Pts',(-0.109516092445046,0.10882944062418,
1.35281597024686));
#14582=CARTESIAN_POINT('Ctrl Pts',(-0.140797762146673,0.0633530726268328,
1.35546335962112));
#14583=CARTESIAN_POINT('Ctrl Pts',(-0.145805692234247,0.0151472216574969,
1.35811074899538));
#14584=CARTESIAN_POINT('Ctrl Pts',(-0.146325105122407,0.0101474034011793,
1.35838533113549));
#14585=CARTESIAN_POINT('Ctrl Pts',(-0.146561879835735,0.00511822289583405,
1.3586599132756));
#14586=CARTESIAN_POINT('Ctrl Pts',(-0.146526884620975,8.5711493927648E-5,
1.35893449541571));
#14587=CARTESIAN_POINT('Origin',(0.,0.,0.));
#14588=CARTESIAN_POINT('',(-0.146120987371435,4.2191387702159E-5,1.41606550458429));
#14589=CARTESIAN_POINT('',(-0.146148882937928,7.6306569664006E-5,1.40893449541571));
#14590=CARTESIAN_POINT('',(-0.14635,-1.79227059055215E-17,0.));
#14591=CARTESIAN_POINT('Ctrl Pts',(-0.146120987371435,4.2191387702159E-5,
1.41606550458429));
#14592=CARTESIAN_POINT('Ctrl Pts',(-0.146177309023295,0.021854523983563,
1.41488378664717));
#14593=CARTESIAN_POINT('Ctrl Pts',(-0.141604359564088,0.0436444172696427,
1.41370206871005));
#14594=CARTESIAN_POINT('Ctrl Pts',(-0.132282279973341,0.0631665524487371,
1.41252035077294));
#14595=CARTESIAN_POINT('Ctrl Pts',(-0.1114064880593,0.106884268839086,1.40987402089383));
#14596=CARTESIAN_POINT('Ctrl Pts',(-0.0667143915920224,0.139229456738304,
1.40722769101473));
#14597=CARTESIAN_POINT('Ctrl Pts',(-0.0186623352932378,0.145397151366753,
1.40458136113563));
#14598=CARTESIAN_POINT('Ctrl Pts',(0.0293897210055454,0.151564845995202,
1.40193503125653));
#14599=CARTESIAN_POINT('Ctrl Pts',(0.0808017371358351,0.131555047352884,
1.39928870137743));
#14600=CARTESIAN_POINT('Ctrl Pts',(0.112041660826149,0.0945265884816804,
1.39664237149832));
#14601=CARTESIAN_POINT('Ctrl Pts',(0.143281584516463,0.0574981296104763,
1.39399604161922));
#14602=CARTESIAN_POINT('Ctrl Pts',(0.154349415766802,0.00345101051038574,
1.39134971174012));
#14603=CARTESIAN_POINT('Ctrl Pts',(0.140179214932283,-0.0428765696854336,
1.38870338186102));
#14604=CARTESIAN_POINT('Ctrl Pts',(0.126009014097764,-0.089204149881253,
1.38605705198192));
#14605=CARTESIAN_POINT('Ctrl Pts',(0.0866007811783877,-0.127812191172801,
1.38341072210282));
#14606=CARTESIAN_POINT('Ctrl Pts',(0.0399922944706322,-0.14102917638501,
1.38076439222371));
#14607=CARTESIAN_POINT('Ctrl Pts',(-0.00661619223712474,-0.15424616159722,
1.37811806234461));
#14608=CARTESIAN_POINT('Ctrl Pts',(-0.060424932733261,-0.142072090730089,
1.37547173246551));
#14609=CARTESIAN_POINT('Ctrl Pts',(-0.0968048252466797,-0.110079232431271,
1.37282540258641));
#14610=CARTESIAN_POINT('Ctrl Pts',(-0.127781608685608,-0.08283792481198,
1.37057210325237));
#14611=CARTESIAN_POINT('Ctrl Pts',(-0.146122133733866,-0.0412276055847571,
1.36831880391833));
#14612=CARTESIAN_POINT('Ctrl Pts',(-0.146471469669193,0.000111495080380188,
1.36606550458429));
#14613=CARTESIAN_POINT('Ctrl Pts',(-0.146526884620975,8.5711493927648E-5,
1.35893449541571));
#14614=CARTESIAN_POINT('Ctrl Pts',(-0.146224472749943,-0.0434028397118431,
1.36130730264986));
#14615=CARTESIAN_POINT('Ctrl Pts',(-0.125627402569456,-0.0871401285467012,
1.36368010988401));
#14616=CARTESIAN_POINT('Ctrl Pts',(-0.0917490966422633,-0.114327780902106,
1.36605291711816));
#14617=CARTESIAN_POINT('Ctrl Pts',(-0.0539503804891888,-0.144661598551044,
1.36870030649242));
#14618=CARTESIAN_POINT('Ctrl Pts',(0.00038124229047478,-0.154393899907594,
1.37134769586668));
#14619=CARTESIAN_POINT('Ctrl Pts',(0.0463590973565905,-0.139066790892088,
1.37399508524094));
#14620=CARTESIAN_POINT('Ctrl Pts',(0.0923369524227062,-0.123739681876581,
1.3766424746152));
#14621=CARTESIAN_POINT('Ctrl Pts',(0.129961039775272,-0.083353162489017,
1.37928986398946));
#14622=CARTESIAN_POINT('Ctrl Pts',(0.141997595260484,-0.0364063334065561,
1.38193725336372));
#14623=CARTESIAN_POINT('Ctrl Pts',(0.154034150745695,0.0105404956759021,
1.38458464273798));
#14624=CARTESIAN_POINT('Ctrl Pts',(0.140483174363557,0.0640476344532581,
1.38723203211224));
#14625=CARTESIAN_POINT('Ctrl Pts',(0.10755170844225,0.0996060653705087,
1.3898794214865));
#14626=CARTESIAN_POINT('Ctrl Pts',(0.0746202425209409,0.135164496287762,
1.39252681086076));
#14627=CARTESIAN_POINT('Ctrl Pts',(0.0223082870604623,0.152774219344908,
1.39517420023502));
#14628=CARTESIAN_POINT('Ctrl Pts',(-0.025422593472234,0.144369075867769,
1.39782158960928));
#14629=CARTESIAN_POINT('Ctrl Pts',(-0.073153474004929,0.135963932390631,
1.40046897898354));
#14630=CARTESIAN_POINT('Ctrl Pts',(-0.11630327960984,0.101543922379208,
1.4031163683578));
#14631=CARTESIAN_POINT('Ctrl Pts',(-0.135107186188192,0.0568751802851974,
1.40576375773206));
#14632=CARTESIAN_POINT('Ctrl Pts',(-0.142614236437708,0.0390421576584788,
1.40682067029328));
#14633=CARTESIAN_POINT('Ctrl Pts',(-0.14624095998336,0.0195756595648056,
1.40787758285449));
#14634=CARTESIAN_POINT('Ctrl Pts',(-0.146148882937928,7.6306569664006E-5,
1.40893449541571));
#14635=CARTESIAN_POINT('Origin',(0.,0.,0.));
#14636=CARTESIAN_POINT('',(-0.14631473222987,-0.000131398079681141,1.46606550458429));
#14637=CARTESIAN_POINT('',(-0.146248097568756,-0.000123763188177425,1.45893449541571));
#14638=CARTESIAN_POINT('',(-0.14635,-1.79227059055215E-17,0.));
#14639=CARTESIAN_POINT('Ctrl Pts',(-0.14631473222987,-0.000131398079681141,
1.46606550458429));
#14640=CARTESIAN_POINT('Ctrl Pts',(-0.145989697979493,0.0361157155227289,
1.46409509925512));
#14641=CARTESIAN_POINT('Ctrl Pts',(-0.132370868650209,0.0725796635271419,
1.46212469392594));
#14642=CARTESIAN_POINT('Ctrl Pts',(-0.107973319296019,0.0991484059484618,
1.46015428859677));
#14643=CARTESIAN_POINT('Ctrl Pts',(-0.0752064754000165,0.134831245351468,
1.45750795871767));
#14644=CARTESIAN_POINT('Ctrl Pts',(-0.0229974942306327,0.152665588379184,
1.45486162883857));
#14645=CARTESIAN_POINT('Ctrl Pts',(0.0247535192036911,0.144485406820094,
1.45221529895946));
#14646=CARTESIAN_POINT('Ctrl Pts',(0.0725045326380122,0.136305225261004,
1.44956896908036));
#14647=CARTESIAN_POINT('Ctrl Pts',(0.115797578337275,0.102110519115111,
1.44692263920126));
#14648=CARTESIAN_POINT('Ctrl Pts',(0.134818450998255,0.0575543070937695,
1.44427630932216));
#14649=CARTESIAN_POINT('Ctrl Pts',(0.153839323659235,0.0129980950724284,
1.44162997944306));
#14650=CARTESIAN_POINT('Ctrl Pts',(0.148588023281934,-0.0419196228243577,
1.43898364956396));
#14651=CARTESIAN_POINT('Ctrl Pts',(0.121467255745355,-0.082062966762292,
1.43633731968485));
#14652=CARTESIAN_POINT('Ctrl Pts',(0.0943464882087764,-0.122206310700226,
1.43369098980575));
#14653=CARTESIAN_POINT('Ctrl Pts',(0.0453562535129183,-0.147575280679306,
1.43104465992665));
#14654=CARTESIAN_POINT('Ctrl Pts',(-0.00307937473935208,-0.146557666176543,
1.42839833004755));
#14655=CARTESIAN_POINT('Ctrl Pts',(-0.0515150029916225,-0.14554005167378,
1.42575200016845));
#14656=CARTESIAN_POINT('Ctrl Pts',(-0.0993960248003067,-0.118135852689175,
1.42310567028934));
#14657=CARTESIAN_POINT('Ctrl Pts',(-0.124806792024246,-0.0768886307561326,
1.42045934041024));
#14658=CARTESIAN_POINT('Ctrl Pts',(-0.138870387581649,-0.0540603453281256,
1.41899472846826));
#14659=CARTESIAN_POINT('Ctrl Pts',(-0.146051182757901,-0.0269918425378075,
1.41753011652627));
#14660=CARTESIAN_POINT('Ctrl Pts',(-0.146120987371435,4.2191387702159E-5,
1.41606550458429));
#14661=CARTESIAN_POINT('Ctrl Pts',(-0.146148882937928,7.6306569664006E-5,
1.40893449541571));
#14662=CARTESIAN_POINT('Ctrl Pts',(-0.146010322369016,-0.0292669616874671,
1.41052497222875));
#14663=CARTESIAN_POINT('Ctrl Pts',(-0.137450455640384,-0.0586846305953837,
1.4121154490418));
#14664=CARTESIAN_POINT('Ctrl Pts',(-0.121019719714466,-0.0827222215753489,
1.41370592585484));
#14665=CARTESIAN_POINT('Ctrl Pts',(-0.0936703391105966,-0.122733407165291,
1.4163533152291));
#14666=CARTESIAN_POINT('Ctrl Pts',(-0.0445135703510636,-0.147838304168576,
1.41900070460336));
#14667=CARTESIAN_POINT('Ctrl Pts',(0.00393424939099551,-0.146537573651384,
1.42164809397762));
#14668=CARTESIAN_POINT('Ctrl Pts',(0.0523820691330518,-0.145236843134192,
1.42429548335188));
#14669=CARTESIAN_POINT('Ctrl Pts',(0.100120939857634,-0.117530485096527,
1.42694287272614));
#14670=CARTESIAN_POINT('Ctrl Pts',(0.125284029446909,-0.0761094471358441,
1.4295902621004));
#14671=CARTESIAN_POINT('Ctrl Pts',(0.150447119036187,-0.0346884091751576,
1.43223765147466));
#14672=CARTESIAN_POINT('Ctrl Pts',(0.153034427490153,0.020447308708549,
1.43488504084892));
#14673=CARTESIAN_POINT('Ctrl Pts',(0.13186079120536,0.0640427391611241,
1.43753243022318));
#14674=CARTESIAN_POINT('Ctrl Pts',(0.110687154920568,0.107638169613697,
1.44017981959744));
#14675=CARTESIAN_POINT('Ctrl Pts',(0.0657525738970213,0.139693312635139,
1.4428272089717));
#14676=CARTESIAN_POINT('Ctrl Pts',(0.0176394768514684,0.145525221357757,
1.44547459834596));
#14677=CARTESIAN_POINT('Ctrl Pts',(-0.0304736201940859,0.151357130080375,
1.44812198772022));
#14678=CARTESIAN_POINT('Ctrl Pts',(-0.0817652332616461,0.130965804504167,
1.45076937709448));
#14679=CARTESIAN_POINT('Ctrl Pts',(-0.112741325423428,0.0936916042199666,
1.45341676646874));
#14680=CARTESIAN_POINT('Ctrl Pts',(-0.134261605244105,0.0677957870194472,
1.45525600945106));
#14681=CARTESIAN_POINT('Ctrl Pts',(-0.145976367207401,0.0337512577971725,
1.45709525243339));
#14682=CARTESIAN_POINT('Ctrl Pts',(-0.146248097568756,-0.000123763188177425,
1.45893449541571));
#14683=CARTESIAN_POINT('Origin',(0.,0.,-0.0924367114736175));
#14684=CARTESIAN_POINT('',(-0.117746618301147,-0.000105742458702955,1.48256328852638));
#14685=CARTESIAN_POINT('',(-0.117971241274414,-5.28325160115065E-6,1.49243671147361));
#14686=CARTESIAN_POINT('',(-0.117775,2.85464118895969E-14,-0.0924367114736175));
#14687=CARTESIAN_POINT('',(-0.117668597464313,0.00500517689812599,1.532225));
#14688=CARTESIAN_POINT('Ctrl Pts',(-0.117746618301147,-0.000105742458702949,
1.48256328852638));
#14689=CARTESIAN_POINT('Ctrl Pts',(-0.117836347163251,-0.0101121102621826,
1.48323921307631));
#14690=CARTESIAN_POINT('Ctrl Pts',(-0.112089674709738,-0.0591937430214443,
1.48656146750534));
#14691=CARTESIAN_POINT('Ctrl Pts',(-0.0435804807853106,-0.132222740314769,
1.49253005181348));
#14692=CARTESIAN_POINT('Ctrl Pts',(0.0874774386997331,-0.108286040948335,
1.50046904145078));
#14693=CARTESIAN_POINT('Ctrl Pts',(0.138385550162814,0.0147146982980264,
1.50840803108809));
#14694=CARTESIAN_POINT('Ctrl Pts',(0.0627460642121078,0.124368470664037,
1.51634702072539));
#14695=CARTESIAN_POINT('Ctrl Pts',(-0.0706026869052757,0.119928391791904,
1.5242860103627));
#14696=CARTESIAN_POINT('Ctrl Pts',(-0.116004137797729,0.0441355889673283,
1.5295786701209));
#14697=CARTESIAN_POINT('Ctrl Pts',(-0.117668597464313,0.00500517689812487,
1.532225));
#14698=CARTESIAN_POINT('',(-0.0334019664627544,0.1129391839063,1.53222500000001));
#14699=CARTESIAN_POINT('Origin',(0.,0.,1.532225));
#14700=CARTESIAN_POINT('Ctrl Pts',(-0.117971276761593,-5.28420699491729E-6,
1.49243671147361));
#14701=CARTESIAN_POINT('Ctrl Pts',(-0.117971582784674,-0.000385634193345565,
1.49246252744444));
#14702=CARTESIAN_POINT('Ctrl Pts',(-0.117794795258817,-0.0397700451254522,
1.49513573278954));
#14703=CARTESIAN_POINT('Ctrl Pts',(-0.0742871760264013,-0.117748889605885,
1.50045632750888));
#14704=CARTESIAN_POINT('Ctrl Pts',(0.0586284551779338,-0.126233948370975,
1.50839849563167));
#14705=CARTESIAN_POINT('Ctrl Pts',(0.137995068118234,-0.019163470063063,
1.51634066375444));
#14706=CARTESIAN_POINT('Ctrl Pts',(0.0906261803825392,0.105639137646141,
1.52428283187723));
#14707=CARTESIAN_POINT('Ctrl Pts',(0.00417072711528833,0.124051375507138,
1.52957761062575));
#14708=CARTESIAN_POINT('Ctrl Pts',(-0.0334019664627544,0.1129391839063,
1.53222500000001));
#14709=CARTESIAN_POINT('Origin',(0.,0.,-0.0924367114736175));
#14710=CARTESIAN_POINT('',(-0.117590702341447,3.3953472435133E-5,1.43256328852638));
#14711=CARTESIAN_POINT('',(-0.117692994131604,-9.95982882293356E-5,1.44243671147361));
#14712=CARTESIAN_POINT('',(-0.117775,2.85464118895969E-14,-0.0924367114736175));
#14713=CARTESIAN_POINT('Ctrl Pts',(-0.117590702341447,3.39534724351446E-5,
1.43256328852638));
#14714=CARTESIAN_POINT('Ctrl Pts',(-0.117534527156218,-0.0217216553118358,
1.43402790046837));
#14715=CARTESIAN_POINT('Ctrl Pts',(-0.101314495966545,-0.0828641818343832,
1.43813884228945));
#14716=CARTESIAN_POINT('Ctrl Pts',(-0.00292444232197888,-0.139176693688359,
1.44489611398964));
#14717=CARTESIAN_POINT('Ctrl Pts',(0.115350068603298,-0.0779297424218237,
1.45283510362695));
#14718=CARTESIAN_POINT('Ctrl Pts',(0.128028003046829,0.0546551750765237,
1.46077409326425));
#14719=CARTESIAN_POINT('Ctrl Pts',(0.0235079116789307,0.137209630484779,
1.46871308290156));
#14720=CARTESIAN_POINT('Ctrl Pts',(-0.0918059616614023,0.0978189523496558,
1.47597614798894));
#14721=CARTESIAN_POINT('Ctrl Pts',(-0.117485047349053,0.0290640819657798,
1.48059288319721));
#14722=CARTESIAN_POINT('Ctrl Pts',(-0.117746618301147,-0.000105742458702949,
1.48256328852638));
#14723=CARTESIAN_POINT('Ctrl Pts',(-0.117692994131604,-9.9598288229346E-5,
1.44243671147361));
#14724=CARTESIAN_POINT('Ctrl Pts',(-0.117789077779518,-0.0120777797952868,
1.44324485786555));
#14725=CARTESIAN_POINT('Ctrl Pts',(-0.110597905189529,-0.0631824179582176,
1.44670039363175));
#14726=CARTESIAN_POINT('Ctrl Pts',(-0.0368790902657646,-0.134252921254984,
1.45280331877221));
#14727=CARTESIAN_POINT('Ctrl Pts',(0.0928396680879532,-0.103751556080299,
1.46074548689499));
#14728=CARTESIAN_POINT('Ctrl Pts',(0.137511141307062,0.0217950526079239,
1.46868765501776));
#14729=CARTESIAN_POINT('Ctrl Pts',(0.0562018483347667,0.127378648737854,
1.47662982314055));
#14730=CARTESIAN_POINT('Ctrl Pts',(-0.0761502833827582,0.1162998103107,
1.48454617529249));
#14731=CARTESIAN_POINT('Ctrl Pts',(-0.117940200573233,0.0386186906477724,
1.48981513807018));
#14732=CARTESIAN_POINT('Ctrl Pts',(-0.117971276761593,-5.28420699491729E-6,
1.49243671147361));
#14733=CARTESIAN_POINT('Origin',(0.,0.,-0.0924367114736175));
#14734=CARTESIAN_POINT('',(-0.117872752581409,8.97255421561373E-5,1.38256328852638));
#14735=CARTESIAN_POINT('',(-0.117613151267609,6.14076272390171E-5,1.39243671147361));
#14736=CARTESIAN_POINT('',(-0.117775,2.85464118895969E-14,-0.0924367114736175));
#14737=CARTESIAN_POINT('Ctrl Pts',(-0.117872752581409,8.97255421561322E-5,
1.38256328852638));
#14738=CARTESIAN_POINT('Ctrl Pts',(-0.117591624875346,-0.0331778698171688,
1.38481658786042));
#14739=CARTESIAN_POINT('Ctrl Pts',(-0.0854981695600773,-0.105990339321694,
1.38971621707357));
#14740=CARTESIAN_POINT('Ctrl Pts',(0.0379781508110965,-0.133926497290667,
1.39726217616581));
#14741=CARTESIAN_POINT('Ctrl Pts',(0.133119345865688,-0.0407171622080862,
1.40520116580311));
#14742=CARTESIAN_POINT('Ctrl Pts',(0.106398871137127,0.0897659150453452,
1.41314015544042));
#14743=CARTESIAN_POINT('Ctrl Pts',(-0.0177224175491345,0.138074504763813,
1.42107914507772));
#14744=CARTESIAN_POINT('Ctrl Pts',(-0.105714817800915,0.0743914165933911,
1.42755352277305));
#14745=CARTESIAN_POINT('Ctrl Pts',(-0.11763602712824,0.0175874039095825,
1.43138157058926));
#14746=CARTESIAN_POINT('Ctrl Pts',(-0.117590702341447,3.39534724351446E-5,
1.43256328852638));
#14747=CARTESIAN_POINT('Ctrl Pts',(-0.117613151267609,6.1407627239024E-5,
1.39243671147361));
#14748=CARTESIAN_POINT('Ctrl Pts',(-0.117501644803633,-0.0235525549213426,
1.39402718828666));
#14749=CARTESIAN_POINT('Ctrl Pts',(-0.0991469449676741,-0.0866320980727062,
1.39826505447396));
#14750=CARTESIAN_POINT('Ctrl Pts',(0.00373660876362508,-0.139175849115243,
1.40515031003553));
#14751=CARTESIAN_POINT('Ctrl Pts',(0.118990018389619,-0.0722858665142316,
1.41309247815831));
#14752=CARTESIAN_POINT('Ctrl Pts',(0.125236419206141,0.0608253567263532,
1.42103464628109));
#14753=CARTESIAN_POINT('Ctrl Pts',(0.0167532566496359,0.13821437898841,
1.42897681440387));
#14754=CARTESIAN_POINT('Ctrl Pts',(-0.0944771051913143,0.0939940009069027,
1.43611083613471));
#14755=CARTESIAN_POINT('Ctrl Pts',(-0.117474319425011,0.0271612872365273,
1.44059746849129));
#14756=CARTESIAN_POINT('Ctrl Pts',(-0.117692994131604,-9.9598288229346E-5,
1.44243671147361));
#14757=CARTESIAN_POINT('Origin',(0.,0.,-0.0924367114736175));
#14758=CARTESIAN_POINT('',(-0.117871679003533,-9.01049542302267E-5,1.33256328852638));
#14759=CARTESIAN_POINT('',(-0.117917347702326,6.89762296073142E-5,1.34243671147361));
#14760=CARTESIAN_POINT('',(-0.117775,2.85464118895969E-14,-0.0924367114736175));
#14761=CARTESIAN_POINT('Ctrl Pts',(-0.117871679003533,-9.01049542302501E-5,
1.33256328852638));
#14762=CARTESIAN_POINT('Ctrl Pts',(-0.117921183610054,-0.00593170075121234,
1.33295894537338));
#14763=CARTESIAN_POINT('Ctrl Pts',(-0.114870949065289,-0.0507926200311143,
1.33600093209947));
#14764=CARTESIAN_POINT('Ctrl Pts',(-0.0572704544775333,-0.126880813469472,
1.34168924870467));
#14765=CARTESIAN_POINT('Ctrl Pts',(0.0755477687720905,-0.116923823242002,
1.34962823834197));
#14766=CARTESIAN_POINT('Ctrl Pts',(0.13920718769651,6.89141801743488E-5,
1.35756722797928));
#14767=CARTESIAN_POINT('Ctrl Pts',(0.0754319660950179,0.116998564767658,
1.36550621761658));
#14768=CARTESIAN_POINT('Ctrl Pts',(-0.0573960494825499,0.126824048933643,
1.37344520725389));
#14769=CARTESIAN_POINT('Ctrl Pts',(-0.11489462347839,0.0507140179075799,
1.37913089755716));
#14770=CARTESIAN_POINT('Ctrl Pts',(-0.117921788132912,0.00589240827474643,
1.38217025798132));
#14771=CARTESIAN_POINT('Ctrl Pts',(-0.117872752581409,8.97255421561322E-5,
1.38256328852638));
#14772=CARTESIAN_POINT('Ctrl Pts',(-0.117917347702326,6.89762296073276E-5,
1.34243671147361));
#14773=CARTESIAN_POINT('Ctrl Pts',(-0.117673982084908,-0.0349283870656527,
1.34480951870776));
#14774=CARTESIAN_POINT('Ctrl Pts',(-0.0826049238592893,-0.109396528181867,
1.34982971531618));
#14775=CARTESIAN_POINT('Ctrl Pts',(0.0440301174146577,-0.132080378229483,
1.35749730129884));
#14776=CARTESIAN_POINT('Ctrl Pts',(0.13486394497766,-0.0345773583278084,
1.36543946942163));
#14777=CARTESIAN_POINT('Ctrl Pts',(0.102148545386143,0.0946020732301706,
1.3733816375444));
#14778=CARTESIAN_POINT('Ctrl Pts',(-0.0241454188302812,0.137116288461919,
1.38132380566719));
#14779=CARTESIAN_POINT('Ctrl Pts',(-0.107458038693719,0.07065895059964,
1.38767549697692));
#14780=CARTESIAN_POINT('Ctrl Pts',(-0.117687250167678,0.015753490298928,
1.3913797989124));
#14781=CARTESIAN_POINT('Ctrl Pts',(-0.117613151267609,6.1407627239024E-5,
1.39243671147361));
#14782=CARTESIAN_POINT('Origin',(0.,0.,-0.0924367114736175));
#14783=CARTESIAN_POINT('',(-0.117590388001671,-3.33269891443968E-5,1.28256328852638));
#14784=CARTESIAN_POINT('',(-0.117823716245033,-0.000102811805890834,1.29243671147362));
#14785=CARTESIAN_POINT('',(-0.117775,2.85464118895969E-14,-0.0924367114736175));
#14786=CARTESIAN_POINT('Ctrl Pts',(-0.117590388001671,-3.33269891444124E-5,
1.28256328852638));
#14787=CARTESIAN_POINT('Ctrl Pts',(-0.117634977734708,-0.017625925033684,
1.28374763276543));
#14788=CARTESIAN_POINT('Ctrl Pts',(-0.105676786131388,-0.0744702911817869,
1.28757830688358));
#14789=CARTESIAN_POINT('Ctrl Pts',(-0.0175857351491984,-0.138091953858251,
1.29405531088083));
#14790=CARTESIAN_POINT('Ctrl Pts',(0.106487712804436,-0.089660542174548,
1.30199430051814));
#14791=CARTESIAN_POINT('Ctrl Pts',(0.133078957772855,0.0408489510387311,
1.30993329015544));
#14792=CARTESIAN_POINT('Ctrl Pts',(0.0378455373822902,0.133964029124136,
1.31787227979275));
#14793=CARTESIAN_POINT('Ctrl Pts',(-0.0855601048685178,0.105915403748908,
1.32541561258306));
#14794=CARTESIAN_POINT('Ctrl Pts',(-0.117590074669608,0.0331395035428114,
1.33031261549427));
#14795=CARTESIAN_POINT('Ctrl Pts',(-0.117871679003533,-9.01049542302501E-5,
1.33256328852638));
#14796=CARTESIAN_POINT('Ctrl Pts',(-0.117823716245033,-0.000102811805890825,
1.29243671147362));
#14797=CARTESIAN_POINT('Ctrl Pts',(-0.117892441435953,-0.00760726064997237,
1.29294445975461));
#14798=CARTESIAN_POINT('Ctrl Pts',(-0.113819337750002,-0.0541654333254181,
1.29609959740987));
#14799=CARTESIAN_POINT('Ctrl Pts',(-0.0518146499729274,-0.129225073214149,
1.30190212443939));
#14800=CARTESIAN_POINT('Ctrl Pts',(0.0805213734929343,-0.11357898534207,
1.30984429256217));
#14801=CARTESIAN_POINT('Ctrl Pts',(0.1390915465469,0.0061171215252809,1.31778646068495));
#14802=CARTESIAN_POINT('Ctrl Pts',(0.0702395735793815,0.120209316621791,
1.32572862880773));
#14803=CARTESIAN_POINT('Ctrl Pts',(-0.0629590648350173,0.124177428154433,
1.33367079693051));
#14804=CARTESIAN_POINT('Ctrl Pts',(-0.115917830154768,0.0471875384414626,
1.33924015781913));
#14805=CARTESIAN_POINT('Ctrl Pts',(-0.117945510062545,0.00411888419242175,
1.3421621293335));
#14806=CARTESIAN_POINT('Ctrl Pts',(-0.117917347702326,6.89762296073276E-5,
1.34243671147361));
#14807=CARTESIAN_POINT('Origin',(0.,0.,-0.0924367114736175));
#14808=CARTESIAN_POINT('',(-0.11774949833287,0.000107383800510985,1.23256328852638));
#14809=CARTESIAN_POINT('',(-0.117581795058195,-8.20683476789735E-6,1.24243671147361));
#14810=CARTESIAN_POINT('',(-0.117775,2.85464118895969E-14,-0.0924367114736175));
#14811=CARTESIAN_POINT('Ctrl Pts',(-0.11774949833287,0.000107383800510997,
1.23256328852638));
#14812=CARTESIAN_POINT('Ctrl Pts',(-0.1174869159147,-0.0291008736543001,
1.23453632015749));
#14813=CARTESIAN_POINT('Ctrl Pts',(-0.0917482398636095,-0.0978979247776974,
1.23915568166769));
#14814=CARTESIAN_POINT('Ctrl Pts',(0.0236422145726536,-0.137184880695923,
1.246421373057));
#14815=CARTESIAN_POINT('Ctrl Pts',(0.128082862902196,-0.0545291301253663,
1.2543603626943));
#14816=CARTESIAN_POINT('Ctrl Pts',(0.115272428336817,0.0780443019497631,
1.26229935233161));
#14817=CARTESIAN_POINT('Ctrl Pts',(-0.00306201423577413,0.139173524314926,
1.27023834196891));
#14818=CARTESIAN_POINT('Ctrl Pts',(-0.101358337705897,0.08278581645186,
1.27699298736717));
#14819=CARTESIAN_POINT('Ctrl Pts',(-0.117535345263889,0.02168343817453,
1.28110130288633));
#14820=CARTESIAN_POINT('Ctrl Pts',(-0.117590388001671,-3.33269891444124E-5,
1.28256328852638));
#14821=CARTESIAN_POINT('Ctrl Pts',(-0.117581795058195,-8.20683476789562E-6,
1.24243671147361));
#14822=CARTESIAN_POINT('Ctrl Pts',(-0.117593699448189,-0.0191748937105988,
1.24372679017572));
#14823=CARTESIAN_POINT('Ctrl Pts',(-0.104100832827715,-0.0776580224685839,
1.24766425825208));
#14824=CARTESIAN_POINT('Ctrl Pts',(-0.0120149744006178,-0.138706589206355,
1.25424911570271));
#14825=CARTESIAN_POINT('Ctrl Pts',(0.110059129405696,-0.0852693704304675,
1.26219128382548));
#14826=CARTESIAN_POINT('Ctrl Pts',(0.13130776387206,0.0462833517151888,
1.27013345194827));
#14827=CARTESIAN_POINT('Ctrl Pts',(0.0322649968732001,0.135435768819968,
1.27807562007105));
#14828=CARTESIAN_POINT('Ctrl Pts',(-0.0881142830049797,0.102747609761224,
1.28551003991283));
#14829=CARTESIAN_POINT('Ctrl Pts',(-0.117534109666069,0.0315207854174475,
1.29029707038035));
#14830=CARTESIAN_POINT('Ctrl Pts',(-0.117823716245033,-0.000102811805890825,
1.29243671147362));
#14831=CARTESIAN_POINT('Origin',(0.,0.,-0.0924367114736175));
#14832=CARTESIAN_POINT('',(-0.117957988745754,-3.12301727557783E-5,1.18256328852638));
#14833=CARTESIAN_POINT('',(-0.117793553451004,0.000106755881474893,1.19243671147362));
#14834=CARTESIAN_POINT('',(-0.117775,2.85464118895969E-14,-0.0924367114736175));
#14835=CARTESIAN_POINT('Ctrl Pts',(-0.117957988745754,-3.12301727557569E-5,
1.18256328852638));
#14836=CARTESIAN_POINT('Ctrl Pts',(-0.117964007145535,-0.00173159226684161,
1.18267867767044));
#14837=CARTESIAN_POINT('Ctrl Pts',(-0.117160216762375,-0.0424221720604921,
1.1854403966936));
#14838=CARTESIAN_POINT('Ctrl Pts',(-0.0703321751825429,-0.12013338809653,
1.19084844559586));
#14839=CARTESIAN_POINT('Ctrl Pts',(0.0627954496153871,-0.124239193932754,
1.19878743523316));
#14840=CARTESIAN_POINT('Ctrl Pts',(0.138438143943654,-0.0146125323915816,
1.20672642487047));
#14841=CARTESIAN_POINT('Ctrl Pts',(0.0873502052771435,0.108390901091839,
1.21466541450777));
#14842=CARTESIAN_POINT('Ctrl Pts',(-0.043700859820065,0.132169893139269,
1.22260440414508));
#14843=CARTESIAN_POINT('Ctrl Pts',(-0.112119660921406,0.0591163174148552,
1.22857036215128));
#14844=CARTESIAN_POINT('Ctrl Pts',(-0.117839104743291,0.0100747194789664,
1.23188999027838));
#14845=CARTESIAN_POINT('Ctrl Pts',(-0.11774949833287,0.000107383800510997,
1.23256328852638));
#14846=CARTESIAN_POINT('Ctrl Pts',(-0.117793553451004,0.000106755881474891,
1.19243671147362));
#14847=CARTESIAN_POINT('Ctrl Pts',(-0.117510050331475,-0.0305433296418112,
1.19450912059683));
#14848=CARTESIAN_POINT('Ctrl Pts',(-0.0896091397727994,-0.100804620014092,
1.19922891909429));
#14849=CARTESIAN_POINT('Ctrl Pts',(0.0288222657999454,-0.136209964735594,
1.20659610696603));
#14850=CARTESIAN_POINT('Ctrl Pts',(0.130092623711363,-0.0495962373069701,
1.21453827508881));
#14851=CARTESIAN_POINT('Ctrl Pts',(0.112184773380136,0.082452738709893,
1.22248044321158));
#14852=CARTESIAN_POINT('Ctrl Pts',(-0.00849585454694533,0.138966535376798,
1.23042261133437));
#14853=CARTESIAN_POINT('Ctrl Pts',(-0.103054997843392,0.079672038485689,
1.23707470075504));
#14854=CARTESIAN_POINT('Ctrl Pts',(-0.11756927027536,0.0201573447738481,
1.24107940080146));
#14855=CARTESIAN_POINT('Ctrl Pts',(-0.117581795058195,-8.20683476789562E-6,
1.24243671147361));
#14856=CARTESIAN_POINT('Origin',(0.,0.,-0.0924367114736175));
#14857=CARTESIAN_POINT('',(-0.117657565919426,-8.78585414499747E-5,1.13256328852638));
#14858=CARTESIAN_POINT('',(-0.117937823388479,-5.4172489969917E-5,1.14243671147362));
#14859=CARTESIAN_POINT('',(-0.117775,2.85464118895969E-14,-0.0924367114736175));
#14860=CARTESIAN_POINT('Ctrl Pts',(-0.117657565919426,-8.78585414499974E-5,
1.13256328852638));
#14861=CARTESIAN_POINT('Ctrl Pts',(-0.11775046973706,-0.0134980674796043,
1.13346736506249));
#14862=CARTESIAN_POINT('Ctrl Pts',(-0.109441032251172,-0.0660497484721492,
1.13701777147771));
#14863=CARTESIAN_POINT('Ctrl Pts',(-0.0320511128216771,-0.13546723577438,
1.14321450777202));
#14864=CARTESIAN_POINT('Ctrl Pts',(0.0964380908528195,-0.100390938007982,
1.15115349740933));
#14865=CARTESIAN_POINT('Ctrl Pts',(0.136644831685568,0.0265863832644056,
1.15909248704664));
#14866=CARTESIAN_POINT('Ctrl Pts',(0.0517625939920979,0.129225692742072,
1.16703147668394));
#14867=CARTESIAN_POINT('Ctrl Pts',(-0.0785823129332351,0.113795317289389,
1.17485507717719));
#14868=CARTESIAN_POINT('Ctrl Pts',(-0.117825981412732,0.0372644419932696,
1.18003234779134));
#14869=CARTESIAN_POINT('Ctrl Pts',(-0.117957988745754,-3.12301727557569E-5,
1.18256328852638));
#14870=CARTESIAN_POINT('Ctrl Pts',(-0.117937823388479,-5.41724899699178E-5,
1.14243671147362));
#14871=CARTESIAN_POINT('Ctrl Pts',(-0.117955293269658,-0.0031110520517566,
1.14264406164367));
#14872=CARTESIAN_POINT('Ctrl Pts',(-0.116460933142332,-0.0451799670343263,
1.14549880118799));
#14873=CARTESIAN_POINT('Ctrl Pts',(-0.0660858892268601,-0.122541963197144,
1.15100093010657));
#14874=CARTESIAN_POINT('Ctrl Pts',(0.0671705316110708,-0.121950798202395,
1.15894309822935));
#14875=CARTESIAN_POINT('Ctrl Pts',(0.138891844802359,-0.00964017357273747,
1.16688526635212));
#14876=CARTESIAN_POINT('Ctrl Pts',(0.0833739592533277,0.111501840422208,
1.17482743447491));
#14877=CARTESIAN_POINT('Ctrl Pts',(-0.0485230383040216,0.130496713571114,
1.18276960259768));
#14878=CARTESIAN_POINT('Ctrl Pts',(-0.113150295826959,0.0561813708375219,
1.18863936159726));
#14879=CARTESIAN_POINT('Ctrl Pts',(-0.117872210070015,0.00861047923971886,
1.19186173122257));
#14880=CARTESIAN_POINT('Ctrl Pts',(-0.117793553451004,0.000106755881474891,
1.19243671147362));
#14881=CARTESIAN_POINT('Origin',(0.,0.,-0.0924367114736175));
#14882=CARTESIAN_POINT('',(-0.117641451221435,8.0229283111194E-5,1.08256328852638));
#14883=CARTESIAN_POINT('',(-0.117630591849015,-7.42484764288953E-5,1.09243671147362));
#14884=CARTESIAN_POINT('',(-0.117775,2.85464118895969E-14,-0.0924367114736175));
#14885=CARTESIAN_POINT('Ctrl Pts',(-0.117641451221435,8.02292831111745E-5,
1.08256328852638));
#14886=CARTESIAN_POINT('Ctrl Pts',(-0.117483998834985,-0.0250372639622414,
1.08425605245455));
#14887=CARTESIAN_POINT('Ctrl Pts',(-0.0972946570053161,-0.0896524615425008,
1.08859514626182));
#14888=CARTESIAN_POINT('Ctrl Pts',(0.00904258428980543,-0.13891320121148,
1.09558056994819));
#14889=CARTESIAN_POINT('Ctrl Pts',(0.121617839487272,-0.067732908692211,
1.1035195595855));
#14890=CARTESIAN_POINT('Ctrl Pts',(0.122860297649024,0.0654522196953821,
1.1114585492228));
#14891=CARTESIAN_POINT('Ctrl Pts',(0.0116325734791967,0.138720326685422,
1.11939753886011));
#14892=CARTESIAN_POINT('Ctrl Pts',(-0.096364912740844,0.0911171059582243,
1.1264324519613));
#14893=CARTESIAN_POINT('Ctrl Pts',(-0.117478530206868,0.0257550656131636,
1.13082103518339));
#14894=CARTESIAN_POINT('Ctrl Pts',(-0.117657565919426,-8.78585414499974E-5,
1.13256328852638));
#14895=CARTESIAN_POINT('Ctrl Pts',(-0.117630591849015,-7.42484764288814E-5,
1.09243671147362));
#14896=CARTESIAN_POINT('Ctrl Pts',(-0.117715241483118,-0.0147626739157663,
1.09342639206478));
#14897=CARTESIAN_POINT('Ctrl Pts',(-0.108350501834675,-0.0686384992808382,
1.0970634620302));
#14898=CARTESIAN_POINT('Ctrl Pts',(-0.0276126195379174,-0.136460326620484,
1.10334792136989));
#14899=CARTESIAN_POINT('Ctrl Pts',(0.0997182217817603,-0.0971604536002107,
1.11129008949267));
#14900=CARTESIAN_POINT('Ctrl Pts',(0.135696927507188,0.0311483765905046,
1.11923225761545));
#14901=CARTESIAN_POINT('Ctrl Pts',(0.0473633069609982,0.130922093830007,
1.12717442573822));
#14902=CARTESIAN_POINT('Ctrl Pts',(-0.0809210029008042,0.111284164335459,
1.13490924369095));
#14903=CARTESIAN_POINT('Ctrl Pts',(-0.117732242679493,0.0359183370635313,
1.13999667226941));
#14904=CARTESIAN_POINT('Ctrl Pts',(-0.117937823388479,-5.41724899699178E-5,
1.14243671147362));
#14905=CARTESIAN_POINT('Origin',(0.,0.,-0.0924367114736175));
#14906=CARTESIAN_POINT('',(-0.117948158721073,4.38502512853227E-5,1.03256328852638));
#14907=CARTESIAN_POINT('',(-0.117667547954054,9.20194976846214E-5,1.04243671147362));
#14908=CARTESIAN_POINT('',(-0.117775,2.85464118895969E-14,-0.0924367114736175));
#14909=CARTESIAN_POINT('Ctrl Pts',(-0.117948158721073,4.38502512853157E-5,
1.03256328852638));
#14910=CARTESIAN_POINT('Ctrl Pts',(-0.117773439871091,-0.0365306738650768,
1.03504473984661));
#14911=CARTESIAN_POINT('Ctrl Pts',(-0.0798690478914953,-0.112422454385097,
1.04017252104593));
#14912=CARTESIAN_POINT('Ctrl Pts',(0.0493427524230464,-0.130168884856471,
1.04794663212436));
#14913=CARTESIAN_POINT('Ctrl Pts',(0.136125055048066,-0.0291310004912345,
1.05588562176166));
#14914=CARTESIAN_POINT('Ctrl Pts',(0.0982941990358779,0.0985743183458784,
1.06382461139897));
#14915=CARTESIAN_POINT('Ctrl Pts',(-0.0295182596522469,0.136041604476578,
1.07176360103627));
#14916=CARTESIAN_POINT('Ctrl Pts',(-0.108818061611988,0.067537217334308,
1.07800982674541));
#14917=CARTESIAN_POINT('Ctrl Pts',(-0.11773014713001,0.0142293884972668,
1.08160972257545));
#14918=CARTESIAN_POINT('Ctrl Pts',(-0.117641451221435,8.02292831111745E-5,
1.08256328852638));
#14919=CARTESIAN_POINT('Ctrl Pts',(-0.117667547954054,9.20194976846197E-5,
1.04243671147362));
#14920=CARTESIAN_POINT('Ctrl Pts',(-0.117475882803567,-0.0261866690710452,
1.04420872248589));
#14921=CARTESIAN_POINT('Ctrl Pts',(-0.0957916308421219,-0.0920126959480487,
1.04862812287242));
#14922=CARTESIAN_POINT('Ctrl Pts',(0.0132451643780021,-0.13859452774087,
1.05569491263321));
#14923=CARTESIAN_POINT('Ctrl Pts',(0.123654649330263,-0.0639797248987874,
1.06363708075599));
#14924=CARTESIAN_POINT('Ctrl Pts',(0.120783771971213,0.0692470788374567,
1.07157924887876));
#14925=CARTESIAN_POINT('Ctrl Pts',(0.00726255089817806,0.139036444335888,
1.07952141700155));
#14926=CARTESIAN_POINT('Ctrl Pts',(-0.0979368667310299,0.0886295245336828,
1.08647390453316));
#14927=CARTESIAN_POINT('Ctrl Pts',(-0.117488804242801,0.0245287720112504,
1.09077900269052));
#14928=CARTESIAN_POINT('Ctrl Pts',(-0.117630591849015,-7.42484764288814E-5,
1.09243671147362));
#14929=CARTESIAN_POINT('Origin',(0.,0.,-0.0924367114736175));
#14930=CARTESIAN_POINT('',(-0.117771476475648,-0.000107683352847938,0.982563288526384));
#14931=CARTESIAN_POINT('',(-0.11796176292438,2.53781033017321E-5,0.992436711473616));
#14932=CARTESIAN_POINT('',(-0.117775,2.85464118895969E-14,-0.0924367114736175));
#14933=CARTESIAN_POINT('Ctrl Pts',(-0.117771476475648,-0.000107683352847945,
0.982563288526384));
#14934=CARTESIAN_POINT('Ctrl Pts',(-0.117856103358663,-0.00933799346614349,
0.983187097359559));
#14935=CARTESIAN_POINT('Ctrl Pts',(-0.112646870919438,-0.057630810124202,
0.986457236071836));
#14936=CARTESIAN_POINT('Ctrl Pts',(-0.0461590140787468,-0.131331607851033,
0.992373704663214));
#14937=CARTESIAN_POINT('Ctrl Pts',(0.0853128637208732,-0.110001641284132,
1.00031269430052));
#14938=CARTESIAN_POINT('Ctrl Pts',(0.138686661656432,0.0120272889735618,
1.00825168393783));
#14939=CARTESIAN_POINT('Ctrl Pts',(0.0651023256631918,0.123046060459907,
1.01619067357513));
#14940=CARTESIAN_POINT('Ctrl Pts',(-0.0680787277209358,0.121424596492465,
1.02412966321244));
#14941=CARTESIAN_POINT('Ctrl Pts',(-0.116790117880403,0.0438975063746073,
1.02958720152952));
#14942=CARTESIAN_POINT('Ctrl Pts',(-0.11795976781127,0.00247402277930658,
1.0323984099675));
#14943=CARTESIAN_POINT('Ctrl Pts',(-0.117948158721073,4.38502512853157E-5,
1.03256328852638));
#14944=CARTESIAN_POINT('Ctrl Pts',(-0.11796176292438,2.53781033017319E-5,
0.992436711473616));
#14945=CARTESIAN_POINT('Ctrl Pts',(-0.117851518882229,-0.0376119105440478,
0.994991052906992));
#14946=CARTESIAN_POINT('Ctrl Pts',(-0.077958511321084,-0.114458475672252,
1.00019278371463));
#14947=CARTESIAN_POINT('Ctrl Pts',(0.0529591494285269,-0.128760265574912,
1.00804190389653));
#14948=CARTESIAN_POINT('Ctrl Pts',(0.136912761112491,-0.0252739657289669,
1.0159840720193));
#14949=CARTESIAN_POINT('Ctrl Pts',(0.0954402180350474,0.101365883217864,
1.02392624014209));
#14950=CARTESIAN_POINT('Ctrl Pts',(-0.0334653697086341,0.135144169424284,
1.03186840826486));
#14951=CARTESIAN_POINT('Ctrl Pts',(-0.109792739119276,0.0652029671457737,
1.03803856537538));
#14952=CARTESIAN_POINT('Ctrl Pts',(-0.117762231070763,0.0130737646421874,
1.04156133311163));
#14953=CARTESIAN_POINT('Ctrl Pts',(-0.117667547954054,9.20194976846197E-5,
1.04243671147362));
#14954=CARTESIAN_POINT('Origin',(0.,0.,-0.0924367114736175));
#14955=CARTESIAN_POINT('',(-0.117585265278523,2.16484251076657E-5,0.932563288526384));
#14956=CARTESIAN_POINT('',(-0.117742563953077,-0.000107211314308964,0.942436711473616));
#14957=CARTESIAN_POINT('',(-0.117775,2.85464118895969E-14,-0.0924367114736175));
#14958=CARTESIAN_POINT('Ctrl Pts',(-0.117585265278523,2.16484251076635E-5,
0.932563288526384));
#14959=CARTESIAN_POINT('Ctrl Pts',(-0.117550805757046,-0.0209622679161363,
0.933975784751614));
#14960=CARTESIAN_POINT('Ctrl Pts',(-0.102172791552808,-0.0813069697478888,
0.938034610855947));
#14961=CARTESIAN_POINT('Ctrl Pts',(-0.00565790085648466,-0.139092177922979,
0.944739766839381));
#14962=CARTESIAN_POINT('Ctrl Pts',(0.113796373024222,-0.0801812402497705,
0.952678756476687));
#14963=CARTESIAN_POINT('Ctrl Pts',(0.129077866376032,0.0521301276928276,
0.960617746113992));
#14964=CARTESIAN_POINT('Ctrl Pts',(0.026197419344502,0.13671993644362,0.968556735751298));
#14965=CARTESIAN_POINT('Ctrl Pts',(-0.0906967139502387,0.0993396518733501,
0.975871916555428));
#14966=CARTESIAN_POINT('Ctrl Pts',(-0.117497098103867,0.02981894716558,
0.980540767480457));
#14967=CARTESIAN_POINT('Ctrl Pts',(-0.117771476475648,-0.000107683352847945,
0.982563288526384));
#14968=CARTESIAN_POINT('Ctrl Pts',(-0.117742563953077,-0.000107211314308957,
0.942436711473616));
#14969=CARTESIAN_POINT('Ctrl Pts',(-0.117833632602859,-0.0103126986533654,
0.943125993953839));
#14970=CARTESIAN_POINT('Ctrl Pts',(-0.111944766202914,-0.0596118697348184,
0.946462665808322));
#14971=CARTESIAN_POINT('Ctrl Pts',(-0.0428565117498991,-0.132465832952297,
0.952446727037066));
#14972=CARTESIAN_POINT('Ctrl Pts',(0.0880997963686447,-0.107806787258123,
0.960388895159846));
#14973=CARTESIAN_POINT('Ctrl Pts',(0.138347640177547,0.0156143509765511,
0.968331063282625));
#14974=CARTESIAN_POINT('Ctrl Pts',(0.061854832590724,0.124731139593481,
0.976273231405407));
#14975=CARTESIAN_POINT('Ctrl Pts',(-0.0713033562375951,0.119581390225944,
0.984215399528185));
#14976=CARTESIAN_POINT('Ctrl Pts',(-0.117322772537986,0.0417718924351975,
0.989603226217589));
#14977=CARTESIAN_POINT('Ctrl Pts',(-0.11796577882491,0.00139640554830399,
0.992343663532733));
#14978=CARTESIAN_POINT('Ctrl Pts',(-0.11796176292438,2.53781033017319E-5,
0.992436711473616));
#14979=CARTESIAN_POINT('Origin',(0.,0.,-0.0924367114736175));
#14980=CARTESIAN_POINT('',(-0.117850913371472,9.6525574830472E-5,0.882563288526384));
#14981=CARTESIAN_POINT('',(-0.117591231449503,3.54948526558943E-5,0.892436711473616));
#14982=CARTESIAN_POINT('',(-0.117775,2.85464118895969E-14,-0.0924367114736175));
#14983=CARTESIAN_POINT('Ctrl Pts',(-0.117850913371472,9.65255748304767E-5,
0.882563288526384));
#14984=CARTESIAN_POINT('Ctrl Pts',(-0.117563006813672,-0.0324172738354332,
0.884764472143669));
#14985=CARTESIAN_POINT('Ctrl Pts',(-0.0867151192651892,-0.104499852648429,
0.889611985640057));
#14986=CARTESIAN_POINT('Ctrl Pts',(0.0353397195745277,-0.134646760160997,
0.897105829015547));
#14987=CARTESIAN_POINT('Ctrl Pts',(0.132293719443212,-0.0433245611326863,
0.905044818652852));
#14988=CARTESIAN_POINT('Ctrl Pts',(0.108141885842356,0.0876583043865096,
0.912983808290157));
#14989=CARTESIAN_POINT('Ctrl Pts',(-0.0150064327997127,0.138395999855801,
0.920922797927463));
#14990=CARTESIAN_POINT('Ctrl Pts',(-0.104951114476159,0.0759553573435841,
0.927449291339539));
#14991=CARTESIAN_POINT('Ctrl Pts',(-0.117615366114572,0.01835136974357,
0.931329454872513));
#14992=CARTESIAN_POINT('Ctrl Pts',(-0.117585265278523,2.16484251076635E-5,
0.932563288526384));
#14993=CARTESIAN_POINT('Ctrl Pts',(-0.117591231449503,3.54948526559117E-5,
0.892436711473616));
#14994=CARTESIAN_POINT('Ctrl Pts',(-0.117532234588281,-0.0218238662162972,
0.893908324374946));
#14995=CARTESIAN_POINT('Ctrl Pts',(-0.101194437785642,-0.0830895288483654,
0.898027326650536));
#14996=CARTESIAN_POINT('Ctrl Pts',(-0.00250162451743248,-0.139203517821528,
0.904793718300386));
#14997=CARTESIAN_POINT('Ctrl Pts',(0.115632500949424,-0.0775435504945224,
0.912735886423165));
#14998=CARTESIAN_POINT('Ctrl Pts',(0.127835376168433,0.0551542754370876,
0.920678054545947));
#14999=CARTESIAN_POINT('Ctrl Pts',(0.0229279137899797,0.137325118854324,
0.928620222668725));
#15000=CARTESIAN_POINT('Ctrl Pts',(-0.0920562790907298,0.0974788594069619,
0.935873108311283));
#15001=CARTESIAN_POINT('Ctrl Pts',(-0.117483857027998,0.0288844367965532,
0.94047860457958));
#15002=CARTESIAN_POINT('Ctrl Pts',(-0.117742563953077,-0.000107211314308957,
0.942436711473616));
#15003=CARTESIAN_POINT('Origin',(0.,0.,-0.0924367114736175));
#15004=CARTESIAN_POINT('',(-0.11789232318732,-8.18790992476613E-5,0.832563288526384));
#15005=CARTESIAN_POINT('',(-0.117872825429845,8.99519344067963E-5,0.842436711473616));
#15006=CARTESIAN_POINT('',(-0.117775,2.85464118895969E-14,-0.0924367114736175));
#15007=CARTESIAN_POINT('Ctrl Pts',(-0.11789232318732,-8.18790992476734E-5,
0.832563288526384));
#15008=CARTESIAN_POINT('Ctrl Pts',(-0.117932494517479,-0.00515170743829337,
0.832906829656623));
#15009=CARTESIAN_POINT('Ctrl Pts',(-0.115332713682068,-0.0492334187378749,
0.835896700665964));
#15010=CARTESIAN_POINT('Ctrl Pts',(-0.059752088941783,-0.125731196083361,
0.841532901554406));
#15011=CARTESIAN_POINT('Ctrl Pts',(0.0732361146625898,-0.118385460722959,
0.849471891191712));
#15012=CARTESIAN_POINT('Ctrl Pts',(0.139181674492094,-0.00266594955618734,
0.857410880829018));
#15013=CARTESIAN_POINT('Ctrl Pts',(0.077715950067195,0.115494055719818,
0.865349870466323));
#15014=CARTESIAN_POINT('Ctrl Pts',(-0.0548934004223171,0.127927168308903,
0.87328886010363));
#15015=CARTESIAN_POINT('Ctrl Pts',(-0.114416768398411,0.0522742940766184,
0.879026666123649));
#15016=CARTESIAN_POINT('Ctrl Pts',(-0.117909136832228,0.0066718045071592,
0.882118142264567));
#15017=CARTESIAN_POINT('Ctrl Pts',(-0.117850913371472,9.65255748304767E-5,
0.882563288526384));
#15018=CARTESIAN_POINT('Ctrl Pts',(-0.117872825429845,8.99519344067998E-5,
0.842436711473616));
#15019=CARTESIAN_POINT('Ctrl Pts',(-0.117591169542271,-0.0331870933343037,
0.844690654796053));
#15020=CARTESIAN_POINT('Ctrl Pts',(-0.0854771005934613,-0.106025606004136,
0.84959198749275));
#15021=CARTESIAN_POINT('Ctrl Pts',(0.0380692928980519,-0.133920149482284,
0.857140709563706));
#15022=CARTESIAN_POINT('Ctrl Pts',(0.133179650076608,-0.0405839661022353,
0.865082877686486));
#15023=CARTESIAN_POINT('Ctrl Pts',(0.106283765719693,0.0899312995767124,
0.873025045809266));
#15024=CARTESIAN_POINT('Ctrl Pts',(-0.0179789669825735,0.138060255849953,
0.880967213932046));
#15025=CARTESIAN_POINT('Ctrl Pts',(-0.105798194743126,0.0742290978659706,
0.887437769153496));
#15026=CARTESIAN_POINT('Ctrl Pts',(-0.117638368248411,0.0175004969839459,
0.891260935000686));
#15027=CARTESIAN_POINT('Ctrl Pts',(-0.117591231449503,3.54948526559117E-5,
0.892436711473616));
#15028=CARTESIAN_POINT('Origin',(0.,0.,-0.0924367114736175));
#15029=CARTESIAN_POINT('',(-0.117598114366551,-4.51832715892789E-5,0.782563288526384));
#15030=CARTESIAN_POINT('',(-0.117874685330111,-8.92836445515327E-5,0.792436711473617));
#15031=CARTESIAN_POINT('',(-0.117775,2.85464118895969E-14,-0.0924367114736175));
#15032=CARTESIAN_POINT('Ctrl Pts',(-0.117598114366551,-4.518327158929E-5,
0.782563288526384));
#15033=CARTESIAN_POINT('Ctrl Pts',(-0.117656123976761,-0.0168608793038394,
0.783695517048678));
#15034=CARTESIAN_POINT('Ctrl Pts',(-0.106420815930739,-0.0729055463807818,
0.787474075450074));
#15035=CARTESIAN_POINT('Ctrl Pts',(-0.0202952816069424,-0.137719814645367,
0.793898963730571));
#15036=CARTESIAN_POINT('Ctrl Pts',(0.104705698854998,-0.0917352845351548,
0.801837953367879));
#15037=CARTESIAN_POINT('Ctrl Pts',(0.133855787965376,0.0382266115373486,
0.809776943005182));
#15038=CARTESIAN_POINT('Ctrl Pts',(0.0404700769297216,0.133194664588195,
0.81771593264249));
#15039=CARTESIAN_POINT('Ctrl Pts',(-0.0843190215395119,0.107398870964955,
0.825311381149555));
#15040=CARTESIAN_POINT('Ctrl Pts',(-0.117623050954756,0.0339016606582783,
0.830260499777521));
#15041=CARTESIAN_POINT('Ctrl Pts',(-0.11789232318732,-8.18790992476734E-5,
0.832563288526384));
#15042=CARTESIAN_POINT('Ctrl Pts',(-0.117874685330111,-8.9283644551537E-5,
0.792436711473617));
#15043=CARTESIAN_POINT('Ctrl Pts',(-0.11792303416021,-0.00583050672374999,
0.7928255958429));
#15044=CARTESIAN_POINT('Ctrl Pts',(-0.114931453360353,-0.0506053896743902,
0.795861869586443));
#15045=CARTESIAN_POINT('Ctrl Pts',(-0.0575513573065257,-0.126774282767806,
0.801545532704245));
#15046=CARTESIAN_POINT('Ctrl Pts',(0.0753527000357912,-0.117071978271622,
0.809487700827026));
#15047=CARTESIAN_POINT('Ctrl Pts',(0.139225942868322,-0.000119714417332432,
0.817429868949805));
#15048=CARTESIAN_POINT('Ctrl Pts',(0.0755539188089132,0.116942220141962,
0.825372037072586));
#15049=CARTESIAN_POINT('Ctrl Pts',(-0.0573332568284509,0.12687306712048,
0.833314205195366));
#15050=CARTESIAN_POINT('Ctrl Pts',(-0.114890414736801,0.0507419104293215,
0.839002429995709));
#15051=CARTESIAN_POINT('Ctrl Pts',(-0.117921990994851,0.00589875908008548,
0.842043265421793));
#15052=CARTESIAN_POINT('Ctrl Pts',(-0.117872825429845,8.99519344067998E-5,
0.842436711473616));
#15053=CARTESIAN_POINT('Origin',(0.,0.,-0.0924367114736175));
#15054=CARTESIAN_POINT('',(-0.11772691567491,0.000105512987197037,0.732563288526384));
#15055=CARTESIAN_POINT('',(-0.117591850253004,-3.65476421498312E-5,0.742436711473616));
#15056=CARTESIAN_POINT('',(-0.117775,2.85464118895969E-14,-0.0924367114736175));
#15057=CARTESIAN_POINT('Ctrl Pts',(-0.11772691567491,0.000105512987197042,
0.732563288526384));
#15058=CARTESIAN_POINT('Ctrl Pts',(-0.117479624464894,-0.0283451130369189,
0.734484204440733));
#15059=CARTESIAN_POINT('Ctrl Pts',(-0.0928318426870313,-0.096374559506161,
0.739051450234184));
#15060=CARTESIAN_POINT('Ctrl Pts',(0.0209425314183671,-0.137622876656644,
0.746265025906738));
#15061=CARTESIAN_POINT('Ctrl Pts',(0.126986869252672,-0.0570349089493802,
0.754204015544043));
#15062=CARTESIAN_POINT('Ctrl Pts',(0.11678343126468,0.0757646090434518,
0.762143005181349));
#15063=CARTESIAN_POINT('Ctrl Pts',(-0.000327234354877375,0.139206819944772,
0.770081994818654));
#15064=CARTESIAN_POINT('Ctrl Pts',(-0.100479183608201,0.0843410365921374,
0.776888755933667));
#15065=CARTESIAN_POINT('Ctrl Pts',(-0.117520539541507,0.0224420334666934,
0.781049187169576));
#15066=CARTESIAN_POINT('Ctrl Pts',(-0.117598114366551,-4.518327158929E-5,
0.782563288526384));
#15067=CARTESIAN_POINT('Ctrl Pts',(-0.117591850253004,-3.65476421498364E-5,
0.742436711473616));
#15068=CARTESIAN_POINT('Ctrl Pts',(-0.117640211257931,-0.0174335619022046,
0.743607926264006));
#15069=CARTESIAN_POINT('Ctrl Pts',(-0.105863856762799,-0.0740921523660566,
0.747426530428656));
#15070=CARTESIAN_POINT('Ctrl Pts',(-0.0182163644075178,-0.138029133036789,
0.753892523967566));
#15071=CARTESIAN_POINT('Ctrl Pts',(0.106128952536144,-0.0901139441634624,
0.761834692090347));
#15072=CARTESIAN_POINT('Ctrl Pts',(0.133249245915149,0.0403548753208232,
0.769776860213125));
#15073=CARTESIAN_POINT('Ctrl Pts',(0.0382995408207276,0.133854483197375,
0.777719028335907));
#15074=CARTESIAN_POINT('Ctrl Pts',(-0.0853693283863186,0.106155717082476,
0.785272312089402));
#15075=CARTESIAN_POINT('Ctrl Pts',(-0.117593892160246,0.0332537408718532,
0.79017820646864));
#15076=CARTESIAN_POINT('Ctrl Pts',(-0.117874685330111,-8.9283644551537E-5,
0.792436711473617));
#15077=CARTESIAN_POINT('Origin',(0.,0.,-0.0924367114736175));
#15078=CARTESIAN_POINT('',(-0.117964947617991,-1.73329198795185E-5,0.682563288526384));
#15079=CARTESIAN_POINT('',(-0.117740574064672,0.000107068518266168,0.692436711473616));
#15080=CARTESIAN_POINT('',(-0.117775,2.85464118895969E-14,-0.0924367114736175));
#15081=CARTESIAN_POINT('Ctrl Pts',(-0.117964947617991,-1.73329198795367E-5,
0.682563288526384));
#15082=CARTESIAN_POINT('Ctrl Pts',(-0.117966864156947,-0.000949576032666658,
0.682626561953687));
#15083=CARTESIAN_POINT('Ctrl Pts',(-0.117534558560489,-0.0408698671952461,
0.685336165260092));
#15084=CARTESIAN_POINT('Ctrl Pts',(-0.0726787294560835,-0.118728463672822,
0.690692098445597));
#15085=CARTESIAN_POINT('Ctrl Pts',(0.0603425395611779,-0.125448888878168,
0.698631088082904));
#15086=CARTESIAN_POINT('Ctrl Pts',(0.138124349154501,-0.0173294538893964,
0.706570077720209));
#15087=CARTESIAN_POINT('Ctrl Pts',(0.0894627833767505,0.106653908470079,
0.714509067357515));
#15088=CARTESIAN_POINT('Ctrl Pts',(-0.0410958292974484,0.133002927094911,
0.72244805699482));
#15089=CARTESIAN_POINT('Ctrl Pts',(-0.111546724107196,0.0606813038481789,
0.728466130717777));
#15090=CARTESIAN_POINT('Ctrl Pts',(-0.117820302634623,0.0108495967181263,
0.731837874561632));
#15091=CARTESIAN_POINT('Ctrl Pts',(-0.11772691567491,0.000105512987197042,
0.732563288526384));
#15092=CARTESIAN_POINT('Ctrl Pts',(-0.117740574064672,0.000107068518266165,
0.692436711473616));
#15093=CARTESIAN_POINT('Ctrl Pts',(-0.117483171888848,-0.0288182833237499,
0.694390256685113));
#15094=CARTESIAN_POINT('Ctrl Pts',(-0.0921515028359353,-0.0973455904149804,
0.698991191270869));
#15095=CARTESIAN_POINT('Ctrl Pts',(0.022691720100341,-0.137364345221032,
0.706239515230886));
#15096=CARTESIAN_POINT('Ctrl Pts',(0.127740337615313,-0.0553740340325759,
0.714181683353665));
#15097=CARTESIAN_POINT('Ctrl Pts',(0.115765682611161,0.077344581120379,
0.722123851476446));
#15098=CARTESIAN_POINT('Ctrl Pts',(-0.00226223072526165,0.139207614056346,
0.730066019599226));
#15099=CARTESIAN_POINT('Ctrl Pts',(-0.101117998472899,0.083225715609228,
0.736836972931616));
#15100=CARTESIAN_POINT('Ctrl Pts',(-0.117530897055598,0.0218902846491045,
0.740960536889746));
#15101=CARTESIAN_POINT('Ctrl Pts',(-0.117591850253004,-3.65476421498364E-5,
0.742436711473616));
#15102=CARTESIAN_POINT('Origin',(0.,0.,-0.0924367114736175));
#15103=CARTESIAN_POINT('',(-0.117676160015555,-9.46906955630148E-5,0.632563288526383));
#15104=CARTESIAN_POINT('',(-0.117962383120995,-2.41598447144192E-5,0.642436711473616));
#15105=CARTESIAN_POINT('',(-0.117775,2.85464118895969E-14,-0.0924367114736175));
#15106=CARTESIAN_POINT('Ctrl Pts',(-0.117676160015555,-9.46906955630045E-5,
0.632563288526383));
#15107=CARTESIAN_POINT('Ctrl Pts',(-0.117771520970562,-0.0127268345011372,
0.633415249345741));
#15108=CARTESIAN_POINT('Ctrl Pts',(-0.110078248258936,-0.064483421762156,
0.636913540044201));
#15109=CARTESIAN_POINT('Ctrl Pts',(-0.0347063025259737,-0.134811417789573,
0.643058160621763));
#15110=CARTESIAN_POINT('Ctrl Pts',(0.0944472082050275,-0.102266175560326,
0.65099715025907));
#15111=CARTESIAN_POINT('Ctrl Pts',(0.137140772714236,0.0238967416356601,
0.658936139896373));
#15112=CARTESIAN_POINT('Ctrl Pts',(0.054291358674537,0.128183829614862,
0.666875129533682));
#15113=CARTESIAN_POINT('Ctrl Pts',(-0.0772016597727435,0.11523146575827,
0.674750845743682));
#15114=CARTESIAN_POINT('Ctrl Pts',(-0.117886707375211,0.0380402955314478,
0.679980232074585));
#15115=CARTESIAN_POINT('Ctrl Pts',(-0.117964947617991,-1.73329198795367E-5,
0.682563288526384));
#15116=CARTESIAN_POINT('Ctrl Pts',(-0.117962383120995,-2.41598447144253E-5,
0.642436711473616));
#15117=CARTESIAN_POINT('Ctrl Pts',(-0.117966033213387,-0.0013279541977536,
0.642525197731959));
#15118=CARTESIAN_POINT('Ctrl Pts',(-0.117355585052125,-0.0416360146359673,
0.645261073364563));
#15119=CARTESIAN_POINT('Ctrl Pts',(-0.0715088964667609,-0.119458592094588,
0.650644338371427));
#15120=CARTESIAN_POINT('Ctrl Pts',(0.0616402393688536,-0.124837327709565,
0.658586506494205));
#15121=CARTESIAN_POINT('Ctrl Pts',(0.138320583400205,-0.0158522461166236,
0.666528674616987));
#15122=CARTESIAN_POINT('Ctrl Pts',(0.0882850628235238,0.107655121482266,
0.674470842739765));
#15123=CARTESIAN_POINT('Ctrl Pts',(-0.0426286451686149,0.132539337972556,
0.682413010862546));
#15124=CARTESIAN_POINT('Ctrl Pts',(-0.111894847147975,0.059748848130285,
0.68840163377383));
#15125=CARTESIAN_POINT('Ctrl Pts',(-0.117831996057943,0.0103805377030848,
0.691742867310853));
#15126=CARTESIAN_POINT('Ctrl Pts',(-0.117740574064672,0.000107068518266165,
0.692436711473616));
#15127=CARTESIAN_POINT('Origin',(0.,0.,-0.0924367114736175));
#15128=CARTESIAN_POINT('',(-0.117626285855324,7.11112359239178E-5,0.582563288526384));
#15129=CARTESIAN_POINT('',(-0.11766919235599,-9.26074537421634E-5,0.592436711473616));
#15130=CARTESIAN_POINT('',(-0.117775,2.85464118895969E-14,-0.0924367114736175));
#15131=CARTESIAN_POINT('Ctrl Pts',(-0.117626285855324,7.11112359239024E-5,
0.582563288526383));
#15132=CARTESIAN_POINT('Ctrl Pts',(-0.117492102008102,-0.0242809575267813,
0.584203936737797));
#15133=CARTESIAN_POINT('Ctrl Pts',(-0.0982512120079041,-0.0881067492982899,
0.588490914828312));
#15134=CARTESIAN_POINT('Ctrl Pts',(0.00631176444456456,-0.139064040754811,
0.595424222797929));
#15135=CARTESIAN_POINT('Ctrl Pts',(0.120263693490807,-0.0701091280034811,
0.603363212435234));
#15136=CARTESIAN_POINT('Ctrl Pts',(0.124122453355413,0.0630258865426945,
0.611302202072541));
#15137=CARTESIAN_POINT('Ctrl Pts',(0.0143556138404206,0.138465021405133,
0.619241191709845));
#15138=CARTESIAN_POINT('Ctrl Pts',(-0.0953630726970595,0.0926558297308384,
0.626328220527794));
#15139=CARTESIAN_POINT('Ctrl Pts',(-0.117475314221613,0.0265106736450616,
0.630768919466639));
#15140=CARTESIAN_POINT('Ctrl Pts',(-0.117676160015555,-9.46906955630045E-5,
0.632563288526383));
#15141=CARTESIAN_POINT('Ctrl Pts',(-0.11766919235599,-9.26074537421669E-5,
0.592436711473616));
#15142=CARTESIAN_POINT('Ctrl Pts',(-0.117764072896019,-0.0130062487266101,
0.593307528153066));
#15143=CARTESIAN_POINT('Ctrl Pts',(-0.109848366281979,-0.0650658641993071,
0.596825734206776));
#15144=CARTESIAN_POINT('Ctrl Pts',(-0.0336977294021144,-0.135086418755761,
0.602991329634746));
#15145=CARTESIAN_POINT('Ctrl Pts',(0.0952657566843092,-0.101529863106778,
0.610933497757526));
#15146=CARTESIAN_POINT('Ctrl Pts',(0.136956022624868,0.025038477707157,
0.618875665880307));
#15147=CARTESIAN_POINT('Ctrl Pts',(0.0531805018142573,0.128669000640787,
0.626817834003085));
#15148=CARTESIAN_POINT('Ctrl Pts',(-0.0778376600742765,0.114584191752874,
0.634671515867523));
#15149=CARTESIAN_POINT('Ctrl Pts',(-0.117856827377429,0.0376798124439797,
0.639877808357699));
#15150=CARTESIAN_POINT('Ctrl Pts',(-0.117962383120995,-2.41598447144253E-5,
0.642436711473616));
#15151=CARTESIAN_POINT('Origin',(0.,0.,-0.0924367114736175));
#15152=CARTESIAN_POINT('',(-0.117934829819181,5.63106208242181E-5,0.532563288526383));
#15153=CARTESIAN_POINT('',(-0.117629301205424,7.34277634442948E-5,0.542436711473615));
#15154=CARTESIAN_POINT('',(-0.117775,2.85464118895969E-14,-0.0924367114736175));
#15155=CARTESIAN_POINT('Ctrl Pts',(-0.117934829819181,5.63106208242166E-5,
0.532563288526383));
#15156=CARTESIAN_POINT('Ctrl Pts',(-0.117723349859012,-0.0357608023914865,
0.534992624129852));
#15157=CARTESIAN_POINT('Ctrl Pts',(-0.0811985738067347,-0.110967619805887,
0.540068289612422));
#15158=CARTESIAN_POINT('Ctrl Pts',(0.0467759446245483,-0.131113145053959,
0.547790284974095));
#15159=CARTESIAN_POINT('Ctrl Pts',(0.135526478334676,-0.031799677225719,
0.555729274611401));
#15160=CARTESIAN_POINT('Ctrl Pts',(0.100211809365564,0.0966242157284558,
0.563668264248707));
#15161=CARTESIAN_POINT('Ctrl Pts',(-0.0268399031138932,0.136595261273209,
0.571607253886012));
#15162=CARTESIAN_POINT('Ctrl Pts',(-0.108142973925314,0.0691035501437442,
0.577905595311905));
#15163=CARTESIAN_POINT('Ctrl Pts',(-0.117708537635025,0.0149983997031143,
0.581557606858695));
#15164=CARTESIAN_POINT('Ctrl Pts',(-0.117626285855324,7.11112359239024E-5,
0.582563288526383));
#15165=CARTESIAN_POINT('Ctrl Pts',(-0.117629301205424,7.34277634442983E-5,
0.542436711473615));
#15166=CARTESIAN_POINT('Ctrl Pts',(-0.11748956090956,-0.0244625652698295,
0.544089858574172));
#15167=CARTESIAN_POINT('Ctrl Pts',(-0.0980201725405651,-0.0884941619373469,
0.548390395048989));
#15168=CARTESIAN_POINT('Ctrl Pts',(0.00702343738442799,-0.139048728244533,
0.555338320898066));
#15169=CARTESIAN_POINT('Ctrl Pts',(0.12066450826877,-0.0694546898587181,
0.563280489020846));
#15170=CARTESIAN_POINT('Ctrl Pts',(0.123764493242992,0.063766979789076,
0.571222657143626));
#15171=CARTESIAN_POINT('Ctrl Pts',(0.0134834875971477,0.13857154491934,
0.579164825266405));
#15172=CARTESIAN_POINT('Ctrl Pts',(-0.0957036897026042,0.092147346049863,
0.586236176709736));
#15173=CARTESIAN_POINT('Ctrl Pts',(-0.117475624432153,0.0262528025703711,
0.590660138778806));
#15174=CARTESIAN_POINT('Ctrl Pts',(-0.11766919235599,-9.26074537421669E-5,
0.592436711473616));
#15175=CARTESIAN_POINT('Origin',(0.,0.,-0.0924367114736175));
#15176=CARTESIAN_POINT('',(-0.117794891956694,-0.000106411733115368,0.482563288526384));
#15177=CARTESIAN_POINT('',(-0.117936566864074,5.52347650140707E-5,0.492436711473616));
#15178=CARTESIAN_POINT('',(-0.117775,2.85464118895969E-14,-0.0924367114736175));
#15179=CARTESIAN_POINT('Ctrl Pts',(-0.117794891956694,-0.000106411733115381,
0.482563288526384));
#15180=CARTESIAN_POINT('Ctrl Pts',(-0.117872998614688,-0.00856127641466401,
0.483134981642805));
#15181=CARTESIAN_POINT('Ctrl Pts',(-0.113184542395844,-0.0560672187853419,
0.486353004638329));
#15182=CARTESIAN_POINT('Ctrl Pts',(-0.0487302328423073,-0.130399425645183,
0.492217357512954));
#15183=CARTESIAN_POINT('Ctrl Pts',(0.0831353173341669,-0.111656458896056,
0.50015634715026));
#15184=CARTESIAN_POINT('Ctrl Pts',(0.13889618212661,0.00930034365552528,
0.508095336787567));
#15185=CARTESIAN_POINT('Ctrl Pts',(0.0675071113591811,0.12174331898465,
0.516034326424871));
#15186=CARTESIAN_POINT('Ctrl Pts',(-0.0656800932930844,0.122738629397884,
0.523973316062178));
#15187=CARTESIAN_POINT('Ctrl Pts',(-0.116384786286051,0.04545243224792,
0.529482970096015));
#15188=CARTESIAN_POINT('Ctrl Pts',(-0.117953719733239,0.00325558390455253,
0.53234629425075));
#15189=CARTESIAN_POINT('Ctrl Pts',(-0.117934829819181,5.63106208242166E-5,
0.532563288526383));
#15190=CARTESIAN_POINT('Ctrl Pts',(-0.117936566864074,5.52347650140663E-5,
0.492436711473616));
#15191=CARTESIAN_POINT('Ctrl Pts',(-0.117728017843002,-0.0358510361847084,
0.494872188995279));
#15192=CARTESIAN_POINT('Ctrl Pts',(-0.0810366231971402,-0.111156550628637,
0.499955055891203));
#15193=CARTESIAN_POINT('Ctrl Pts',(0.0471380885036503,-0.131003351527116,
0.507685312161385));
#15194=CARTESIAN_POINT('Ctrl Pts',(0.135643160584381,-0.031381690295376,
0.515627480284167));
#15195=CARTESIAN_POINT('Ctrl Pts',(0.0998851624184703,0.0969888232104648,
0.523569648406945));
#15196=CARTESIAN_POINT('Ctrl Pts',(-0.0273779061153799,0.136507610615132,
0.531511816529727));
#15197=CARTESIAN_POINT('Ctrl Pts',(-0.108290992649607,0.0687756007668377,
0.537800837551949));
#15198=CARTESIAN_POINT('Ctrl Pts',(-0.117713344367368,0.0148299618267192,
0.541442469199912));
#15199=CARTESIAN_POINT('Ctrl Pts',(-0.117629301205424,7.34277634442983E-5,
0.542436711473615));
#15200=CARTESIAN_POINT('Origin',(0.,0.,-0.0924367114736175));
#15201=CARTESIAN_POINT('',(-0.117582256074849,9.06819982020624E-6,0.432563288526383));
#15202=CARTESIAN_POINT('',(-0.11779560903417,-0.000106574656651148,0.442436711473616));
#15203=CARTESIAN_POINT('',(-0.117775,2.85464118895969E-14,-0.0924367114736175));
#15204=CARTESIAN_POINT('Ctrl Pts',(-0.117582256074849,9.06819982019261E-6,
0.432563288526383));
#15205=CARTESIAN_POINT('Ctrl Pts',(-0.117568373935691,-0.020201912089319,
0.43392366903486));
#15206=CARTESIAN_POINT('Ctrl Pts',(-0.10300922874285,-0.0797477867736473,
0.437930379422439));
#15207=CARTESIAN_POINT('Ctrl Pts',(-0.00838939967687663,-0.138954178686792,
0.44458341968912));
#15208=CARTESIAN_POINT('Ctrl Pts',(0.11219917790857,-0.0824013973067221,
0.452522409326426));
#15209=CARTESIAN_POINT('Ctrl Pts',(0.13007709763057,0.0495842159710775,
0.460461398963732));
#15210=CARTESIAN_POINT('Ctrl Pts',(0.0288783492374893,0.136178877755608,
0.468400388601037));
#15211=CARTESIAN_POINT('Ctrl Pts',(-0.0895654556576369,0.100852400902523,
0.475767685121922));
#15212=CARTESIAN_POINT('Ctrl Pts',(-0.117511448025972,0.0305757367622385,
0.480488651763704));
#15213=CARTESIAN_POINT('Ctrl Pts',(-0.117794891956694,-0.000106411733115381,
0.482563288526384));
#15214=CARTESIAN_POINT('Ctrl Pts',(-0.11779560903417,-0.000106574656651151,
0.442436711473616));
#15215=CARTESIAN_POINT('Ctrl Pts',(-0.117873644338608,-0.00854245500997505,
0.443007130042126));
#15216=CARTESIAN_POINT('Ctrl Pts',(-0.113196618671047,-0.056044542179559,
0.446224937984896));
#15217=CARTESIAN_POINT('Ctrl Pts',(-0.0487473834415776,-0.130413074907061,
0.452090135301926));
#15218=CARTESIAN_POINT('Ctrl Pts',(0.0831820848081396,-0.111645054821459,
0.460032303424706));
#15219=CARTESIAN_POINT('Ctrl Pts',(0.138908217753341,0.00940130521287039,
0.467974471547486));
#15220=CARTESIAN_POINT('Ctrl Pts',(0.0673801526530663,0.121835103839429,
0.475916639670265));
#15221=CARTESIAN_POINT('Ctrl Pts',(-0.0658750545035054,0.12265543075329,
0.483858807793047));
#15222=CARTESIAN_POINT('Ctrl Pts',(-0.116424939330292,0.0453161125527027,
0.489365498394162));
#15223=CARTESIAN_POINT('Ctrl Pts',(-0.11795471279604,0.00317945345687678,
0.492224799621019));
#15224=CARTESIAN_POINT('Ctrl Pts',(-0.117936566864074,5.52347650140663E-5,
0.492436711473616));
#15225=CARTESIAN_POINT('Origin',(0.,0.,-0.0924367114736175));
#15226=CARTESIAN_POINT('',(-0.117828183671793,0.000101754196006455,0.382563288526383));
#15227=CARTESIAN_POINT('',(-0.117581664177921,7.09484545444172E-6,0.392436711473616));
#15228=CARTESIAN_POINT('',(-0.117775,2.85464118895969E-14,-0.0924367114736175));
#15229=CARTESIAN_POINT('Ctrl Pts',(-0.117828183671793,0.000101754196006446,
0.382563288526384));
#15230=CARTESIAN_POINT('Ctrl Pts',(-0.117538790254565,-0.0316580736410773,
0.384712356426916));
#15231=CARTESIAN_POINT('Ctrl Pts',(-0.0879068326507716,-0.103002379129266,
0.38950775420655));
#15232=CARTESIAN_POINT('Ctrl Pts',(0.0326876424682324,-0.135315053971568,
0.396949481865287));
#15233=CARTESIAN_POINT('Ctrl Pts',(0.13141703692502,-0.0459152284901983,
0.404888471502591));
#15234=CARTESIAN_POINT('Ctrl Pts',(0.109843140674695,0.0855168418978295,
0.412827461139898));
#15235=CARTESIAN_POINT('Ctrl Pts',(-0.0122846228212416,0.13866410438033,
0.420766450777203));
#15236=CARTESIAN_POINT('Ctrl Pts',(-0.104166535924894,0.0775181589932739,
0.427345059906032));
#15237=CARTESIAN_POINT('Ctrl Pts',(-0.117595378674006,0.0191142356295008,
0.431277339155758));
#15238=CARTESIAN_POINT('Ctrl Pts',(-0.117582256074849,9.06819982019261E-6,
0.432563288526383));
#15239=CARTESIAN_POINT('Ctrl Pts',(-0.117581664177921,7.09484545444172E-6,
0.392436711473616));
#15240=CARTESIAN_POINT('Ctrl Pts',(-0.117570873504463,-0.0200907396801347,
0.393789460463232));
#15241=CARTESIAN_POINT('Ctrl Pts',(-0.10312708440739,-0.079535468422451,
0.397789598827109));
#15242=CARTESIAN_POINT('Ctrl Pts',(-0.00873482453528946,-0.138951719454826,
0.404437126565246));
#15243=CARTESIAN_POINT('Ctrl Pts',(0.112042812448737,-0.0826455423945668,
0.412379294688026));
#15244=CARTESIAN_POINT('Ctrl Pts',(0.130177722634257,0.049372441998279,
0.420321462810806));
#15245=CARTESIAN_POINT('Ctrl Pts',(0.0290564652212241,0.136160197297018,
0.428263630933586));
#15246=CARTESIAN_POINT('Ctrl Pts',(-0.0895090212855029,0.100936776489487,
0.435635380487856));
#15247=CARTESIAN_POINT('Ctrl Pts',(-0.117511471984497,0.0306096014671689,
0.440359740667866));
#15248=CARTESIAN_POINT('Ctrl Pts',(-0.11779560903417,-0.000106574656651151,
0.442436711473616));
#15249=CARTESIAN_POINT('Origin',(0.,0.,-0.0924367114736175));
#15250=CARTESIAN_POINT('',(-0.117911328466355,-7.22474488887591E-5,0.332563288526384));
#15251=CARTESIAN_POINT('',(-0.117821685414254,0.000103165543095151,0.342436711473616));
#15252=CARTESIAN_POINT('',(-0.117775,2.85464118895969E-14,-0.0924367114736175));
#15253=CARTESIAN_POINT('Ctrl Pts',(-0.117911328466355,-7.22474488887752E-5,
0.332563288526384));
#15254=CARTESIAN_POINT('Ctrl Pts',(-0.117942332027964,-0.00437115939612809,
0.332854713939869));
#15255=CARTESIAN_POINT('Ctrl Pts',(-0.115777752883067,-0.0476754067323583,
0.335792469232457));
#15256=CARTESIAN_POINT('Ctrl Pts',(-0.0622106591311991,-0.12453304658572,
0.341376554404146));
#15257=CARTESIAN_POINT('Ctrl Pts',(0.0708961914151981,-0.119801401679107,
0.349315544041452));
#15258=CARTESIAN_POINT('Ctrl Pts',(0.1391024375543,-0.00539978406154301,
0.357254533678757));
#15259=CARTESIAN_POINT('Ctrl Pts',(0.0799699354250877,0.113944965792994,
0.365193523316063));
#15260=CARTESIAN_POINT('Ctrl Pts',(-0.0523695618881846,0.128980908622551,
0.373132512953369));
#15261=CARTESIAN_POINT('Ctrl Pts',(-0.113921748517257,0.0538356345748906,
0.378922434690143));
#15262=CARTESIAN_POINT('Ctrl Pts',(-0.117895144954496,0.00745050051778832,
0.382066026547814));
#15263=CARTESIAN_POINT('Ctrl Pts',(-0.117828183671793,0.000101754196006446,
0.382563288526384));
#15264=CARTESIAN_POINT('Ctrl Pts',(-0.117821685414254,0.000103165543095145,
0.342436711473616));
#15265=CARTESIAN_POINT('Ctrl Pts',(-0.117532262555972,-0.0314544122979593,
0.344571790884339));
#15266=CARTESIAN_POINT('Ctrl Pts',(-0.0882170202347594,-0.102616110661261,
0.349354259669323));
#15267=CARTESIAN_POINT('Ctrl Pts',(0.0320320385160992,-0.135491055083419,
0.356784117828566));
#15268=CARTESIAN_POINT('Ctrl Pts',(0.131227975626944,-0.0465090949381858,
0.364726285951346));
#15269=CARTESIAN_POINT('Ctrl Pts',(0.110205605501345,0.0850799742312894,
0.372668454074126));
#15270=CARTESIAN_POINT('Ctrl Pts',(-0.0117764211155082,0.138727046407055,
0.380610622196906));
#15271=CARTESIAN_POINT('Ctrl Pts',(-0.10403099481448,0.0777947493501838,
0.387200041330069));
#15272=CARTESIAN_POINT('Ctrl Pts',(-0.117591991327853,0.019241607989002,
0.391142071088973));
#15273=CARTESIAN_POINT('Ctrl Pts',(-0.117581664177921,7.09484545444172E-6,
0.392436711473616));
#15274=CARTESIAN_POINT('Origin',(0.,0.,-0.0924367114736175));
#15275=CARTESIAN_POINT('',(-0.117608153246896,-5.64262068778628E-5,0.282563288526383));
#15276=CARTESIAN_POINT('',(-0.117918861549493,-6.80329776671096E-5,0.292436711473615));
#15277=CARTESIAN_POINT('',(-0.117775,2.85464118895969E-14,-0.0924367114736175));
#15278=CARTESIAN_POINT('Ctrl Pts',(-0.117608153246896,-5.64262068778604E-5,
0.282563288526383));
#15279=CARTESIAN_POINT('Ctrl Pts',(-0.117677606263852,-0.0160946837114709,
0.283643401331924));
#15280=CARTESIAN_POINT('Ctrl Pts',(-0.107144424846824,-0.0713401098021974,
0.287369844016567));
#15281=CARTESIAN_POINT('Ctrl Pts',(-0.0229969941138309,-0.137294515779738,
0.293742616580312));
#15282=CARTESIAN_POINT('Ctrl Pts',(0.102883268653204,-0.0937746172089793,
0.301681606217617));
#15283=CARTESIAN_POINT('Ctrl Pts',(0.134580950019115,0.0355895166223291,
0.309620595854923));
#15284=CARTESIAN_POINT('Ctrl Pts',(0.0430789950773988,0.13237388709478,
0.317559585492229));
#15285=CARTESIAN_POINT('Ctrl Pts',(-0.0830523456774332,0.10887452531409,
0.325207149716049));
#15286=CARTESIAN_POINT('Ctrl Pts',(-0.11766079978112,0.0346657214219864,
0.330208384060767));
#15287=CARTESIAN_POINT('Ctrl Pts',(-0.117911328466355,-7.22474488887752E-5,
0.332563288526384));
#15288=CARTESIAN_POINT('Ctrl Pts',(-0.117918861549493,-6.80329776671157E-5,
0.292436711473616));
#15289=CARTESIAN_POINT('Ctrl Pts',(-0.117946256357307,-0.00405052459867665,
0.292706731931186));
#15290=CARTESIAN_POINT('Ctrl Pts',(-0.11595553950755,-0.0470512577090033,
0.295624141763016));
#15291=CARTESIAN_POINT('Ctrl Pts',(-0.0631725212350128,-0.124068972994571,
0.301188940969106));
#15292=CARTESIAN_POINT('Ctrl Pts',(0.0700327441786229,-0.12032993078169,
0.309131109091886));
#15293=CARTESIAN_POINT('Ctrl Pts',(0.139080821187468,-0.00635631000930847,
0.317073277214666));
#15294=CARTESIAN_POINT('Ctrl Pts',(0.0807165776729536,0.11344034374014,
0.325015445337446));
#15295=CARTESIAN_POINT('Ctrl Pts',(-0.0515923433190751,0.129313988454311,
0.332957613460226));
#15296=CARTESIAN_POINT('Ctrl Pts',(-0.113774867115171,0.0543021652640841,
0.338764702172283));
#15297=CARTESIAN_POINT('Ctrl Pts',(-0.117891132111753,0.00767537174388221,
0.341924401510079));
#15298=CARTESIAN_POINT('Ctrl Pts',(-0.117821685414254,0.000103165543095145,
0.342436711473616));
#15299=CARTESIAN_POINT('Origin',(0.,0.,-0.0924367114736175));
#15300=CARTESIAN_POINT('',(-0.117705188630573,0.000102098618198066,0.232563288526383));
#15301=CARTESIAN_POINT('',(-0.1176142238744,-6.23262858038681E-5,0.242436711473616));
#15302=CARTESIAN_POINT('',(-0.117775,2.85464118895969E-14,-0.0924367114736175));
#15303=CARTESIAN_POINT('Ctrl Pts',(-0.117705188630573,0.000102098618198071,
0.232563288526383));
#15304=CARTESIAN_POINT('Ctrl Pts',(-0.117475649963863,-0.0275896003179174,
0.234432088723979));
#15305=CARTESIAN_POINT('Ctrl Pts',(-0.0938913217252411,-0.0948462909608301,
0.238947218800678));
#15306=CARTESIAN_POINT('Ctrl Pts',(0.0182347644767634,-0.138007750384372,
0.246108678756477));
#15307=CARTESIAN_POINT('Ctrl Pts',(0.125841858853055,-0.0595186723796334,
0.254047668393783));
#15308=CARTESIAN_POINT('Ctrl Pts',(0.118249355954961,0.073455671106145,
0.261986658031089));
#15309=CARTESIAN_POINT('Ctrl Pts',(0.00240767183786234,0.139186381940956,
0.269925647668394));
#15310=CARTESIAN_POINT('Ctrl Pts',(-0.0995777503027144,0.0858938305448248,
0.27678452450016));
#15311=CARTESIAN_POINT('Ctrl Pts',(-0.117507442931816,0.0231998416616275,
0.280997071452822));
#15312=CARTESIAN_POINT('Ctrl Pts',(-0.117608153246896,-5.64262068778604E-5,
0.282563288526383));
#15313=CARTESIAN_POINT('Ctrl Pts',(-0.1176142238744,-6.2326285803882E-5,
0.242436711473616));
#15314=CARTESIAN_POINT('Ctrl Pts',(-0.117689148257971,-0.0156863246439697,
0.243489062352292));
#15315=CARTESIAN_POINT('Ctrl Pts',(-0.107519643382358,-0.0705218816827611,
0.247188802605229));
#15316=CARTESIAN_POINT('Ctrl Pts',(-0.024381182195918,-0.137074561658528,
0.253535932232426));
#15317=CARTESIAN_POINT('Ctrl Pts',(0.101985705091022,-0.094777599970642,
0.261478100355206));
#15318=CARTESIAN_POINT('Ctrl Pts',(0.134923209124943,0.0343453801629359,
0.269420268477986));
#15319=CARTESIAN_POINT('Ctrl Pts',(0.0442571924125319,0.132004463632409,
0.277362436600766));
#15320=CARTESIAN_POINT('Ctrl Pts',(-0.0824920331482911,0.109525057495754,
0.285034584265976));
#15321=CARTESIAN_POINT('Ctrl Pts',(-0.117677666622401,0.0349954280503056,
0.290059342556926));
#15322=CARTESIAN_POINT('Ctrl Pts',(-0.117918861549493,-6.80329776671157E-5,
0.292436711473616));
#15323=CARTESIAN_POINT('Origin',(0.,0.,-0.0924367114736175));
#15324=CARTESIAN_POINT('',(-0.117967994073432,-3.0724305424694E-6,0.182563288526383));
#15325=CARTESIAN_POINT('',(-0.117691121003631,9.91971943564221E-5,0.192436711473615));
#15326=CARTESIAN_POINT('',(-0.117775,2.85464118895969E-14,-0.0924367114736175));
#15327=CARTESIAN_POINT('Ctrl Pts',(-0.117967994073432,-3.07243054247449E-6,
0.182563288526383));
#15328=CARTESIAN_POINT('Ctrl Pts',(-0.117968057042159,-0.000167453844217198,
0.182574446236933));
#15329=CARTESIAN_POINT('Ctrl Pts',(-0.117893299674953,-0.0393189363008842,
0.185231933826584));
#15330=CARTESIAN_POINT('Ctrl Pts',(-0.0749972298318695,-0.11727771015962,
0.190535751295337));
#15331=CARTESIAN_POINT('Ctrl Pts',(0.0578663373665801,-0.126610160769685,
0.198474740932643));
#15332=CARTESIAN_POINT('Ctrl Pts',(0.13775723856723,-0.0200396862227523,
0.206413730569949));
#15333=CARTESIAN_POINT('Ctrl Pts',(0.091540828968026,0.104875747581476,
0.214352720207254));
#15334=CARTESIAN_POINT('Ctrl Pts',(-0.0384749358425138,0.133784622116252,
0.22229170984456));
#15335=CARTESIAN_POINT('Ctrl Pts',(-0.110955338697302,0.0622468391270206,
0.22836189928427));
#15336=CARTESIAN_POINT('Ctrl Pts',(-0.11780069007939,0.0116234575531164,
0.231785758844877));
#15337=CARTESIAN_POINT('Ctrl Pts',(-0.117705188630573,0.000102098618198071,
0.232563288526383));
#15338=CARTESIAN_POINT('Ctrl Pts',(-0.117691121003631,9.91971943564221E-5,
0.192436711473615));
#15339=CARTESIAN_POINT('Ctrl Pts',(-0.117474218986382,-0.0270951350261672,
0.194271392773399));
#15340=CARTESIAN_POINT('Ctrl Pts',(-0.0945676524372527,-0.0938598508209937,
0.198753463447442));
#15341=CARTESIAN_POINT('Ctrl Pts',(0.0165156171993534,-0.138242945169174,
0.205882923495746));
#15342=CARTESIAN_POINT('Ctrl Pts',(0.125131592687617,-0.061040658666823,
0.213825091618526));
#15343=CARTESIAN_POINT('Ctrl Pts',(0.119114174013628,0.0720811421096423,
0.221767259741306));
#15344=CARTESIAN_POINT('Ctrl Pts',(0.0039759348809324,0.139169211541763,
0.229709427864086));
#15345=CARTESIAN_POINT('Ctrl Pts',(-0.0990660356104632,0.0867677816679632,
0.236599245108189));
#15346=CARTESIAN_POINT('Ctrl Pts',(-0.117500661679058,0.0236188235484957,
0.240841672978032));
#15347=CARTESIAN_POINT('Ctrl Pts',(-0.1176142238744,-6.2326285803882E-5,
0.242436711473616));
#15348=CARTESIAN_POINT('Origin',(0.,0.,-0.0924367114736175));
#15349=CARTESIAN_POINT('',(-0.117696212882312,-0.000100181105204699,0.132563288526383));
#15350=CARTESIAN_POINT('',(-0.117967699956222,8.3697257429456E-6,0.142436711473616));
#15351=CARTESIAN_POINT('',(-0.117775,2.85464118895969E-14,-0.0924367114736175));
#15352=CARTESIAN_POINT('Ctrl Pts',(-0.117696212882312,-0.000100181105204706,
0.132563288526383));
#15353=CARTESIAN_POINT('Ctrl Pts',(-0.117792074781153,-0.0119544960022407,
0.133363133628988));
#15354=CARTESIAN_POINT('Ctrl Pts',(-0.110696412003459,-0.0629173266909915,
0.136809308610694));
#15355=CARTESIAN_POINT('Ctrl Pts',(-0.0373480950846616,-0.134103559412242,
0.142901813471503));
#15356=CARTESIAN_POINT('Ctrl Pts',(0.0924198687735613,-0.104101940294199,
0.150840803108809));
#15357=CARTESIAN_POINT('Ctrl Pts',(0.137583777756591,0.0211978768359354,
0.158779792746114));
#15358=CARTESIAN_POINT('Ctrl Pts',(0.0567991668878991,0.127092487218924,
0.16671878238342));
#15359=CARTESIAN_POINT('Ctrl Pts',(-0.0757945745091616,0.116657324056303,
0.174646614310176));
#15360=CARTESIAN_POINT('Ctrl Pts',(-0.117953122434976,0.0388197061692436,
0.179928116357831));
#15361=CARTESIAN_POINT('Ctrl Pts',(-0.117967994073432,-3.07243054247449E-6,
0.182563288526383));
#15362=CARTESIAN_POINT('Ctrl Pts',(-0.117967699956222,8.3697257429579E-6,
0.142436711473616));
#15363=CARTESIAN_POINT('Ctrl Pts',(-0.117928252023989,-0.038547130539091,
0.145053723194506));
#15364=CARTESIAN_POINT('Ctrl Pts',(-0.0762804946418446,-0.116178754198862,
0.150318124289656));
#15365=CARTESIAN_POINT('Ctrl Pts',(0.0559861945572589,-0.127473226882309,
0.158229914759066));
#15366=CARTESIAN_POINT('Ctrl Pts',(0.137471621702818,-0.0220324926503626,
0.166172082881846));
#15367=CARTESIAN_POINT('Ctrl Pts',(0.0930189202108026,0.103592267873211,
0.174114251004626));
#15368=CARTESIAN_POINT('Ctrl Pts',(-0.0366486683060043,0.134315868829211,
0.182056419127406));
#15369=CARTESIAN_POINT('Ctrl Pts',(-0.110544190454925,0.0633195416932908,
0.188163905950403));
#15370=CARTESIAN_POINT('Ctrl Pts',(-0.11778720200735,0.0121454601492482,
0.191624003399139));
#15371=CARTESIAN_POINT('Ctrl Pts',(-0.117691121003631,9.91971943564221E-5,
0.192436711473615));
#15372=CARTESIAN_POINT('Origin',(0.,0.,-0.0924367114736175));
#15373=CARTESIAN_POINT('',(-0.117613109409711,6.11591708146705E-5,0.0825632885263832));
#15374=CARTESIAN_POINT('',(-0.117715749944134,-0.000104199409386274,0.0924367114736155));
#15375=CARTESIAN_POINT('',(-0.117775,2.85464118895969E-14,-0.0924367114736175));
#15376=CARTESIAN_POINT('Ctrl Pts',(-0.117613109409711,6.11591708146765E-5,
0.0825632885263832));
#15377=CARTESIAN_POINT('Ctrl Pts',(-0.117502393620717,-0.0235240259785673,
0.0841518210210431));
#15378=CARTESIAN_POINT('Ctrl Pts',(-0.0991849320095013,-0.0865581493706475,
0.088386683394805));
#15379=CARTESIAN_POINT('Ctrl Pts',(0.00357853460314598,-0.139161043603659,
0.0952678756476685));
#15380=CARTESIAN_POINT('Ctrl Pts',(0.118863112008681,-0.0724583686054966,
0.103206865284975));
#15381=CARTESIAN_POINT('Ctrl Pts',(0.125336705278751,0.0605752693714656,
0.11114585492228));
#15382=CARTESIAN_POINT('Ctrl Pts',(0.0170731091066207,0.138156245709763,
0.119084844559586));
#15383=CARTESIAN_POINT('Ctrl Pts',(-0.094337657277608,0.0941904991302726,
0.126223989094287));
#15384=CARTESIAN_POINT('Ctrl Pts',(-0.11747491061231,0.0272661325996615,
0.130716803749886));
#15385=CARTESIAN_POINT('Ctrl Pts',(-0.117696212882312,-0.000100181105204706,
0.132563288526383));
#15386=CARTESIAN_POINT('Ctrl Pts',(-0.117715749944134,-0.000104199409386274,
0.0924367114736155));
#15387=CARTESIAN_POINT('Ctrl Pts',(-0.117810584636384,-0.011244028442556,
0.0931886642413524));
#15388=CARTESIAN_POINT('Ctrl Pts',(-0.111246641208053,-0.0614941526881817,
0.0965880063833492));
#15389=CARTESIAN_POINT('Ctrl Pts',(-0.0397151780004399,-0.133441281507892,
0.102634737899606));
#15390=CARTESIAN_POINT('Ctrl Pts',(0.0906220264938673,-0.105695447092796,
0.110576906022386));
#15391=CARTESIAN_POINT('Ctrl Pts',(0.137940159127448,0.0188783162799928,
0.118519074145166));
#15392=CARTESIAN_POINT('Ctrl Pts',(0.0588909273047484,0.126157580947307,
0.126461242267946));
#15393=CARTESIAN_POINT('Ctrl Pts',(-0.074108440039672,0.117863552156501,
0.134403410390726));
#15394=CARTESIAN_POINT('Ctrl Pts',(-0.117763087033452,0.0399060678969832,
0.139728566792616));
#15395=CARTESIAN_POINT('Ctrl Pts',(-0.117968157858494,0.000455912857932787,
0.142406333820246));
#15396=CARTESIAN_POINT('Ctrl Pts',(-0.117967699956222,8.3697257429579E-6,
0.142436711473616));
#15397=CARTESIAN_POINT('Origin',(0.,0.,-0.0924367114736175));
#15398=CARTESIAN_POINT('',(-0.117917485785546,7.60014832213593E-5,0.0325632885263832));
#15399=CARTESIAN_POINT('',(-0.117600989619072,5.04992496179954E-5,0.0424367114736154));
#15400=CARTESIAN_POINT('',(-0.117775,2.85464118895969E-14,-0.0924367114736175));
#15401=CARTESIAN_POINT('Ctrl Pts',(-0.117917485785546,7.60014832213644E-5,
0.0325632885263832));
#15402=CARTESIAN_POINT('Ctrl Pts',(-0.117676727567847,-0.0349830640657269,
0.0349405084130983));
#15403=CARTESIAN_POINT('Ctrl Pts',(-0.0825043195215805,-0.109517225708346,
0.0399640581789154));
#15404=CARTESIAN_POINT('Ctrl Pts',(0.0441923146003338,-0.131999388615902,
0.0476339378238343));
#15405=CARTESIAN_POINT('Ctrl Pts',(0.134874939024977,-0.034459980695041,
0.0555729274611401));
#15406=CARTESIAN_POINT('Ctrl Pts',(0.102091080224759,0.094638871230671,
0.0635119170984456));
#15407=CARTESIAN_POINT('Ctrl Pts',(-0.0241513666277066,0.137095110112719,
0.0714509067357516));
#15408=CARTESIAN_POINT('Ctrl Pts',(-0.107448046275642,0.0706698818446754,
0.0778013638783972));
#15409=CARTESIAN_POINT('Ctrl Pts',(-0.117686834607281,0.0157664388843013,
0.0815054911419412));
#15410=CARTESIAN_POINT('Ctrl Pts',(-0.117613109409711,6.11591708146765E-5,
0.0825632885263832));
#15411=CARTESIAN_POINT('Ctrl Pts',(-0.117600989619072,5.04992496179954E-5,
0.0424367114736154));
#15412=CARTESIAN_POINT('Ctrl Pts',(-0.117514779739531,-0.0227353060542692,
0.043970994662459));
#15413=CARTESIAN_POINT('Ctrl Pts',(-0.100129952091853,-0.0849605109884783,
0.0481526672255625));
#15414=CARTESIAN_POINT('Ctrl Pts',(0.000787973702835166,-0.139222729671589,
0.054981729162926));
#15415=CARTESIAN_POINT('Ctrl Pts',(0.117431922513572,-0.0747907597173192,
0.0629238972857061));
#15416=CARTESIAN_POINT('Ctrl Pts',(0.126496838785129,0.0581591461343325,
0.070866065408486));
#15417=CARTESIAN_POINT('Ctrl Pts',(0.0196773008918215,0.137828289815661,
0.0788082335312661));
#15418=CARTESIAN_POINT('Ctrl Pts',(-0.0933482651079043,0.0956446566614129,
0.085998448886309));
#15419=CARTESIAN_POINT('Ctrl Pts',(-0.11747670148927,0.0279758085988667,
0.0905412748670923));
#15420=CARTESIAN_POINT('Ctrl Pts',(-0.117715749944134,-0.000104199409386274,
0.0924367114736155));
#15421=CARTESIAN_POINT('Origin',(0.,0.,1.55));
#15422=CARTESIAN_POINT('',(-0.143211704627722,-5.70397197726547E-6,1.50700023576178));
#15423=CARTESIAN_POINT('Ctrl Pts',(-0.0334019664626774,0.112939183906323,
1.532225));
#15424=CARTESIAN_POINT('Ctrl Pts',(-0.0250606930336426,0.115799676338094,
1.53184761307169));
#15425=CARTESIAN_POINT('Ctrl Pts',(-0.0164287086124659,0.117635554524944,
1.53147359869818));
#15426=CARTESIAN_POINT('Ctrl Pts',(-0.00767226928320402,0.118510614220874,
1.53110056493424));
#15427=CARTESIAN_POINT('Ctrl Pts',(-0.0042150196872779,0.118856108509867,
1.53095328237096));
#15428=CARTESIAN_POINT('Ctrl Pts',(-0.000736351480830917,0.119051293525916,
1.53080607672538));
#15429=CARTESIAN_POINT('Ctrl Pts',(0.00274830211697625,0.119097943881266,
1.53065904037218));
#15430=CARTESIAN_POINT('Ctrl Pts',(0.00972321854123044,0.119191319684798,
1.53036473098213));
#15431=CARTESIAN_POINT('Ctrl Pts',(0.0166907125456733,0.118690968429664,
1.53007241075126));
#15432=CARTESIAN_POINT('Ctrl Pts',(0.0235721318645625,0.11762150546261,
1.52978094357425));
#15433=CARTESIAN_POINT('Ctrl Pts',(0.0273478463565568,0.117034709826966,
1.52962102062912));
#15434=CARTESIAN_POINT('Ctrl Pts',(0.0310977188904398,0.116276259986281,
1.52946135449799));
#15435=CARTESIAN_POINT('Ctrl Pts',(0.0348087249896146,0.115347945392283,
1.52930175751644));
#15436=CARTESIAN_POINT('Ctrl Pts',(0.0378768737129624,0.114580442682688,
1.52916980751093));
#15437=CARTESIAN_POINT('Ctrl Pts',(0.0409182562642153,0.113696477767379,
1.52903790896105));
#15438=CARTESIAN_POINT('Ctrl Pts',(0.0439120268522727,0.112701821307647,
1.52890655030309));
#15439=CARTESIAN_POINT('Ctrl Pts',(0.0504861734289241,0.110517613410832,
1.52861809430882));
#15440=CARTESIAN_POINT('Ctrl Pts',(0.0568477403450367,0.107796947733889,
1.528331525126));
#15441=CARTESIAN_POINT('Ctrl Pts',(0.0629211062797432,0.10455513280498,
1.52804576869741));
#15442=CARTESIAN_POINT('Ctrl Pts',(0.0667529140263229,0.102509807084265,
1.52786547926507));
#15443=CARTESIAN_POINT('Ctrl Pts',(0.0704699809867569,0.100256700264741,
1.52768551335768));
#15444=CARTESIAN_POINT('Ctrl Pts',(0.0740519796445933,0.0977963961590643,
1.52750560123222));
#15445=CARTESIAN_POINT('Ctrl Pts',(0.0761474027326905,0.0963571499395001,
1.52740035495562));
#15446=CARTESIAN_POINT('Ctrl Pts',(0.0781972522873126,0.0948464165467323,
1.52729509152825));
#15447=CARTESIAN_POINT('Ctrl Pts',(0.0801950758490376,0.0932655888959708,
1.52718986717129));
#15448=CARTESIAN_POINT('Ctrl Pts',(0.0872135629190184,0.0877120362002772,
1.52682020700562));
#15449=CARTESIAN_POINT('Ctrl Pts',(0.0935342345834078,0.0813437113039547,
1.52645409167081));
#15450=CARTESIAN_POINT('Ctrl Pts',(0.0991216768718319,0.0743433873765979,
1.52608928877518));
#15451=CARTESIAN_POINT('Ctrl Pts',(0.101857856375295,0.0709153174549959,
1.52591064420861));
#15452=CARTESIAN_POINT('Ctrl Pts',(0.104417791592617,0.0673349702414553,
1.52573231437502));
#15453=CARTESIAN_POINT('Ctrl Pts',(0.106794530290299,0.0636205708890664,
1.52555403711528));
#15454=CARTESIAN_POINT('Ctrl Pts',(0.108394385735532,0.0611202951812291,
1.52543403324399));
#15455=CARTESIAN_POINT('Ctrl Pts',(0.109912312880749,0.0585571637778213,
1.52531395827658));
#15456=CARTESIAN_POINT('Ctrl Pts',(0.111341951189028,0.0559432008961949,
1.5251940432238));
#15457=CARTESIAN_POINT('Ctrl Pts',(0.115894033640165,0.0476201345006791,
1.52481222412716));
#15458=CARTESIAN_POINT('Ctrl Pts',(0.119530893641226,0.0388304356906876,
1.52443409356659));
#15459=CARTESIAN_POINT('Ctrl Pts',(0.122195159250079,0.0297595052710396,
1.52405718851832));
#15460=CARTESIAN_POINT('Ctrl Pts',(0.123464283518865,0.0254385629829291,
1.52387764960816));
#15461=CARTESIAN_POINT('Ctrl Pts',(0.124512110981915,0.0210533134598664,
1.52369838877875));
#15462=CARTESIAN_POINT('Ctrl Pts',(0.12532867129748,0.0166220814218575,
1.52351913980531));
#15463=CARTESIAN_POINT('Ctrl Pts',(0.126067828800149,0.012610891624201,
1.52335688207487));
#15464=CARTESIAN_POINT('Ctrl Pts',(0.12661735951473,0.00855739899605222,
1.52319445303817));
#15465=CARTESIAN_POINT('Ctrl Pts',(0.126966826155483,0.00450415768051923,
1.52303280899981));
#15466=CARTESIAN_POINT('Ctrl Pts',(0.127602972227412,-0.00287409603749457,
1.52273856283131));
#15467=CARTESIAN_POINT('Ctrl Pts',(0.12758177643555,-0.010267620141741,
1.52244625042084));
#15468=CARTESIAN_POINT('Ctrl Pts',(0.126865581413421,-0.0175939782534482,
1.52215473434257));
#15469=CARTESIAN_POINT('Ctrl Pts',(0.126426462283551,-0.0220859726121444,
1.52197599770985));
#15470=CARTESIAN_POINT('Ctrl Pts',(0.12572570473317,-0.0265528301690258,
1.52179756043894));
#15471=CARTESIAN_POINT('Ctrl Pts',(0.124776542651163,-0.0309793260681717,
1.52161916036391));
#15472=CARTESIAN_POINT('Ctrl Pts',(0.124151644840291,-0.0338935887106027,
1.52150170748789));
#15473=CARTESIAN_POINT('Ctrl Pts',(0.123418330834614,-0.0367926408403149,
1.52138417707714));
#15474=CARTESIAN_POINT('Ctrl Pts',(0.122581975874549,-0.0396644408336013,
1.52126680258073));
#15475=CARTESIAN_POINT('Ctrl Pts',(0.120074191833131,-0.0482754427851461,
1.52091485884509));
#15476=CARTESIAN_POINT('Ctrl Pts',(0.116656903439717,-0.0566007293654626,
1.52056600333313));
#15477=CARTESIAN_POINT('Ctrl Pts',(0.112443760417108,-0.0645262187619275,
1.52021830866717));
#15478=CARTESIAN_POINT('Ctrl Pts',(0.109356904590302,-0.0703330102694749,
1.51996356219884));
#15479=CARTESIAN_POINT('Ctrl Pts',(0.105841781173658,-0.0759253337267248,
1.51970943888381));
#15480=CARTESIAN_POINT('Ctrl Pts',(0.101930367117466,-0.0812537151913617,
1.51945518067311));
#15481=CARTESIAN_POINT('Ctrl Pts',(0.100130771446666,-0.0837052409256295,
1.51933819945644));
#15482=CARTESIAN_POINT('Ctrl Pts',(0.0982476276828181,-0.0860996963839449,
1.51922123442864));
#15483=CARTESIAN_POINT('Ctrl Pts',(0.0962924325256194,-0.0884227179472683,
1.51910469697823));
#15484=CARTESIAN_POINT('Ctrl Pts',(0.0906946176521128,-0.0950736369671782,
1.51877104482549));
#15485=CARTESIAN_POINT('Ctrl Pts',(0.0844921899154374,-0.101162815315101,
1.51843983772287));
#15486=CARTESIAN_POINT('Ctrl Pts',(0.0777644521522082,-0.106582693579069,
1.51810941878));
#15487=CARTESIAN_POINT('Ctrl Pts',(0.0731067700043679,-0.110334931124879,
1.5178806663426));
#15488=CARTESIAN_POINT('Ctrl Pts',(0.0681966627772886,-0.113766151308436,
1.51765229166508));
#15489=CARTESIAN_POINT('Ctrl Pts',(0.0630541948599911,-0.116833686038022,
1.5174237449583));
#15490=CARTESIAN_POINT('Ctrl Pts',(0.0607686815400033,-0.118197018118406,
1.51732216988754));
#15491=CARTESIAN_POINT('Ctrl Pts',(0.0584414404741937,-0.119485783651375,
1.51722075040181));
#15492=CARTESIAN_POINT('Ctrl Pts',(0.0560784264268894,-0.12069488199044,
1.51711960151386));
#15493=CARTESIAN_POINT('Ctrl Pts',(0.0475595529450054,-0.125053787850271,
1.51675495087613));
#15494=CARTESIAN_POINT('Ctrl Pts',(0.038563113830939,-0.128389854466075,
1.51639315730301));
#15495=CARTESIAN_POINT('Ctrl Pts',(0.0292711048986314,-0.130741856378471,
1.51603205677802));
#15496=CARTESIAN_POINT('Ctrl Pts',(0.0254547302664753,-0.13170786066222,
1.51588374709674));
#15497=CARTESIAN_POINT('Ctrl Pts',(0.0215881861914954,-0.132507324978224,
1.51573555432397));
#15498=CARTESIAN_POINT('Ctrl Pts',(0.0176832233642019,-0.13314066674995,
1.51558732853105));
#15499=CARTESIAN_POINT('Ctrl Pts',(0.0144414794405867,-0.133666441752394,
1.51546427740745));
#15500=CARTESIAN_POINT('Ctrl Pts',(0.0111713231872828,-0.134077605234841,
1.5153411329761));
#15501=CARTESIAN_POINT('Ctrl Pts',(0.00789687394913892,-0.134372952697723,
1.51521845803943));
#15502=CARTESIAN_POINT('Ctrl Pts',(-0.00208492598009478,-0.135273287095873,
1.51484449692866));
#15503=CARTESIAN_POINT('Ctrl Pts',(-0.0121386692885745,-0.135107999768821,
1.51447364169918));
#15504=CARTESIAN_POINT('Ctrl Pts',(-0.0220717676774029,-0.133899092645375,
1.51410356562093));
#15505=CARTESIAN_POINT('Ctrl Pts',(-0.0271373055616968,-0.133282591671289,
1.51391483957382));
#15506=CARTESIAN_POINT('Ctrl Pts',(-0.0321716696217597,-0.132393849601707,
1.51372631615657));
#15507=CARTESIAN_POINT('Ctrl Pts',(-0.0371491047637803,-0.131230566976147,
1.51353768678866));
#15508=CARTESIAN_POINT('Ctrl Pts',(-0.0401763453142056,-0.130523066780721,
1.51342296375255));
#15509=CARTESIAN_POINT('Ctrl Pts',(-0.0431793745847511,-0.129714439573166,
1.51330831773957));
#15510=CARTESIAN_POINT('Ctrl Pts',(-0.0461427198170546,-0.128807808452418,
1.51319405707679));
#15511=CARTESIAN_POINT('Ctrl Pts',(-0.0557912886485991,-0.125855842991896,
1.51282202756853));
#15512=CARTESIAN_POINT('Ctrl Pts',(-0.0650506639775802,-0.121862017750276,
1.51245293010828));
#15513=CARTESIAN_POINT('Ctrl Pts',(-0.0737251756215706,-0.116823260910032,
1.51208446868514));
#15514=CARTESIAN_POINT('Ctrl Pts',(-0.0774533877539874,-0.114657657224767,
1.51192610791459));
#15515=CARTESIAN_POINT('Ctrl Pts',(-0.0810733781510443,-0.112298364258586,
1.51176786463208));
#15516=CARTESIAN_POINT('Ctrl Pts',(-0.0845783705992567,-0.109758519633299,
1.51160955655689));
#15517=CARTESIAN_POINT('Ctrl Pts',(-0.0871260289206952,-0.107912394030924,
1.51149448786814));
#15518=CARTESIAN_POINT('Ctrl Pts',(-0.0896122610481647,-0.105970921032248,
1.51137940572563));
#15519=CARTESIAN_POINT('Ctrl Pts',(-0.0920243025666997,-0.10394826075131,
1.51126473391974));
#15520=CARTESIAN_POINT('Ctrl Pts',(-0.0995315444015674,-0.0976529296958118,
1.51090782920982));
#15521=CARTESIAN_POINT('Ctrl Pts',(-0.106349817996106,-0.090554906599088,
1.51055366538392));
#15522=CARTESIAN_POINT('Ctrl Pts',(-0.112409916721278,-0.0828189535999138,
1.51020021897155));
#15523=CARTESIAN_POINT('Ctrl Pts',(-0.11567060314877,-0.0786565598680515,
1.51001004419521));
#15524=CARTESIAN_POINT('Ctrl Pts',(-0.118711357121208,-0.0743087544864998,
1.50982007711492));
#15525=CARTESIAN_POINT('Ctrl Pts',(-0.121517490738653,-0.0697974244982526,
1.50963000253165));
#15526=CARTESIAN_POINT('Ctrl Pts',(-0.123184827969132,-0.0671169005197731,
1.50951706477726));
#15527=CARTESIAN_POINT('Ctrl Pts',(-0.124768226583796,-0.064379797453554,
1.50940414472167));
#15528=CARTESIAN_POINT('Ctrl Pts',(-0.12625918933752,-0.0616017405091787,
1.50929161182319));
#15529=CARTESIAN_POINT('Ctrl Pts',(-0.131254477666307,-0.0522942005345653,
1.50891458411209));
#15530=CARTESIAN_POINT('Ctrl Pts',(-0.135235816373665,-0.0424980109473837,
1.50854057440173));
#15531=CARTESIAN_POINT('Ctrl Pts',(-0.138100316247284,-0.0323932585971084,
1.50816719719795));
#15532=CARTESIAN_POINT('Ctrl Pts',(-0.139428601593765,-0.027707625827389,
1.5079940600046));
#15533=CARTESIAN_POINT('Ctrl Pts',(-0.140516076092011,-0.0229552175461711,
1.50782105881478));
#15534=CARTESIAN_POINT('Ctrl Pts',(-0.14134846970832,-0.01815262603916,
1.50764795577689));
#15535=CARTESIAN_POINT('Ctrl Pts',(-0.141840021659925,-0.0153165600461233,
1.5075457335416));
#15536=CARTESIAN_POINT('Ctrl Pts',(-0.142241997144177,-0.0124651428186592,
1.50744355431084));
#15537=CARTESIAN_POINT('Ctrl Pts',(-0.142550993842162,-0.00961078035088443,
1.50734168592779));
#15538=CARTESIAN_POINT('Ctrl Pts',(-0.142847161918882,-0.00687492249914849,
1.50724404681617));
#15539=CARTESIAN_POINT('Ctrl Pts',(-0.143058332724879,-0.00413406598225375,
1.5071466105924));
#15540=CARTESIAN_POINT('Ctrl Pts',(-0.143182669649515,-0.00139134585336764,
1.50704933585643));
#15541=CARTESIAN_POINT('Ctrl Pts',(-0.143203595382121,-0.00092974984559876,
1.50703296465278));
#15542=CARTESIAN_POINT('Ctrl Pts',(-0.143222061023464,-0.000468100854706259,
1.50701659802318));
#15543=CARTESIAN_POINT('Ctrl Pts',(-0.143238079070951,-6.41379011939899E-6,
1.50700023577028));
#15544=CARTESIAN_POINT('',(-0.00156744678985144,0.146109855568756,1.50365));
#15545=CARTESIAN_POINT('Ctrl Pts',(-0.00156962371672063,0.146072546381438,
1.50365));
#15546=CARTESIAN_POINT('Ctrl Pts',(-0.011711474284147,0.144648739717271,
1.50495065132295));
#15547=CARTESIAN_POINT('Ctrl Pts',(-0.0216501921041044,0.142222471223284,
1.50626105010813));
#15548=CARTESIAN_POINT('Ctrl Pts',(-0.0312062965385204,0.138804788898175,
1.50759029209282));
#15549=CARTESIAN_POINT('Ctrl Pts',(-0.0379863325344082,0.136379950477271,
1.50853338648503));
#15550=CARTESIAN_POINT('Ctrl Pts',(-0.0445735484268955,0.133455002060128,
1.5094859663039));
#15551=CARTESIAN_POINT('Ctrl Pts',(-0.0508923708069948,0.130021662144985,
1.51045128011208));
#15552=CARTESIAN_POINT('Ctrl Pts',(-0.053607485163773,0.128546401418451,
1.51086606268101));
#15553=CARTESIAN_POINT('Ctrl Pts',(-0.0562647183424556,0.126981576978965,
1.51128195276517));
#15554=CARTESIAN_POINT('Ctrl Pts',(-0.0588579379029418,0.125328026221608,
1.51169910067666));
#15555=CARTESIAN_POINT('Ctrl Pts',(-0.0624505046767585,0.123037247762191,
1.51227700458785));
#15556=CARTESIAN_POINT('Ctrl Pts',(-0.0659209207101175,0.120575889029892,
1.51285741907924));
#15557=CARTESIAN_POINT('Ctrl Pts',(-0.0692542752175272,0.117943487410649,
1.51344114883776));
#15558=CARTESIAN_POINT('Ctrl Pts',(-0.0735613784355843,0.114542101371374,
1.51419539934302));
#15559=CARTESIAN_POINT('Ctrl Pts',(-0.0776398170223455,0.110855132244726,
1.51495518495604));
#15560=CARTESIAN_POINT('Ctrl Pts',(-0.0814741368103916,0.106911749311875,
1.51572224163114));
#15561=CARTESIAN_POINT('Ctrl Pts',(-0.0845038784997064,0.103795829845314,
1.51632834224744));
#15562=CARTESIAN_POINT('Ctrl Pts',(-0.087381117690253,0.10051973853988,
1.51693898261853));
#15563=CARTESIAN_POINT('Ctrl Pts',(-0.0900959757046659,0.0970973798321736,
1.51755501917095));
#15564=CARTESIAN_POINT('Ctrl Pts',(-0.0920052356275281,0.0946905606587243,
1.51798825505079));
#15565=CARTESIAN_POINT('Ctrl Pts',(-0.093830595110286,0.092215607777745,
1.51842338946406));
#15566=CARTESIAN_POINT('Ctrl Pts',(-0.0955653742165971,0.0896840982544811,
1.51885969689116));
#15567=CARTESIAN_POINT('Ctrl Pts',(-0.0997851775729162,0.0835262696618028,
1.51992100293214));
#15568=CARTESIAN_POINT('Ctrl Pts',(-0.103479134251024,0.0770231540939269,
1.52099120961793));
#15569=CARTESIAN_POINT('Ctrl Pts',(-0.106606394578922,0.0702509006766953,
1.52207541818308));
#15570=CARTESIAN_POINT('Ctrl Pts',(-0.108879606303698,0.0653281362576702,
1.52286353153598));
#15571=CARTESIAN_POINT('Ctrl Pts',(-0.110852991156964,0.0602629640702717,
1.52365904329275));
#15572=CARTESIAN_POINT('Ctrl Pts',(-0.112503888351057,0.0550849881514033,
1.524463912762));
#15573=CARTESIAN_POINT('Ctrl Pts',(-0.113450017754745,0.0521174894567802,
1.52492518356294));
#15574=CARTESIAN_POINT('Ctrl Pts',(-0.114289979676541,0.0491121240008169,
1.52538965304266));
#15575=CARTESIAN_POINT('Ctrl Pts',(-0.115015874151616,0.0460903162170444,
1.52585530945224));
#15576=CARTESIAN_POINT('Ctrl Pts',(-0.117053612444637,0.0376074669234184,
1.52716250482259));
#15577=CARTESIAN_POINT('Ctrl Pts',(-0.118206139871793,0.0289652499882669,
1.52848357355921));
#15578=CARTESIAN_POINT('Ctrl Pts',(-0.11838625730212,0.0202925750432425,
1.52982832573377));
#15579=CARTESIAN_POINT('Ctrl Pts',(-0.118492077855379,0.015197303257165,
1.53061837930521));
#15580=CARTESIAN_POINT('Ctrl Pts',(-0.118261361656021,0.0100916471271278,
1.53141660760476));
#15581=CARTESIAN_POINT('Ctrl Pts',(-0.11766859746431,0.00500517689818842,
1.532225));
#15582=CARTESIAN_POINT('',(-0.115079981391543,0.0902137050004572,1.50365));
#15583=CARTESIAN_POINT('Origin',(0.,0.,1.50365));
#15584=CARTESIAN_POINT('Ctrl Pts',(-0.143238079070951,-6.41379011939899E-6,
1.50700023577028));
#15585=CARTESIAN_POINT('Ctrl Pts',(-0.143514357617001,0.00795674345750163,
1.50671802038504));
#15586=CARTESIAN_POINT('Ctrl Pts',(-0.14306421847979,0.0159310909218757,
1.50643710681857));
#15587=CARTESIAN_POINT('Ctrl Pts',(-0.141940608246003,0.023841490005315,
1.50615648267927));
#15588=CARTESIAN_POINT('Ctrl Pts',(-0.141317731836386,0.0282266413964,1.50600091791928));
#15589=CARTESIAN_POINT('Ctrl Pts',(-0.14048752132733,0.0325921818867556,
1.50584544210227));
#15590=CARTESIAN_POINT('Ctrl Pts',(-0.139456452513291,0.0369250818702156,
1.5056898827608));
#15591=CARTESIAN_POINT('Ctrl Pts',(-0.138790989895207,0.0397215809279161,
1.50558948313156));
#15592=CARTESIAN_POINT('Ctrl Pts',(-0.138042009924554,0.0425029011667524,
1.50548910366784));
#15593=CARTESIAN_POINT('Ctrl Pts',(-0.137214434473447,0.0452564915355094,
1.50538902890071));
#15594=CARTESIAN_POINT('Ctrl Pts',(-0.134176751889031,0.0553637675507716,
1.50502169637912));
#15595=CARTESIAN_POINT('Ctrl Pts',(-0.130076454936343,0.0651325632434767,
1.50465723703036));
#15596=CARTESIAN_POINT('Ctrl Pts',(-0.125018127980614,0.0743940890034878,
1.50429344851366));
#15597=CARTESIAN_POINT('Ctrl Pts',(-0.122034683484208,0.0798566160996726,
1.50407888293545));
#15598=CARTESIAN_POINT('Ctrl Pts',(-0.118716925567465,0.0851425936725427,
1.50386455072235));
#15599=CARTESIAN_POINT('Ctrl Pts',(-0.115078604842436,0.0902138214954005,
1.50365));
#15600=CARTESIAN_POINT('',(-0.05,-6.12323399573677E-18,1.6));
#15601=CARTESIAN_POINT('',(-0.1,-1.22464679914735E-17,1.55));
#15602=CARTESIAN_POINT('Origin',(0.,0.,1.6));
#15603=CARTESIAN_POINT('Ctrl Pts',(0.0850780204044575,-0.11908002747757,
-0.0164977839420936));
#15604=CARTESIAN_POINT('Ctrl Pts',(0.124677800165771,-0.0907875342533835,
-0.0138514540629917));
#15605=CARTESIAN_POINT('Ctrl Pts',(0.172751483861701,0.00791416360185712,
-0.00855879430478784));
#15606=CARTESIAN_POINT('Ctrl Pts',(0.0868617128612901,0.149726167188418,
-0.000619804667482127));
#15607=CARTESIAN_POINT('Ctrl Pts',(-0.078614020905812,0.154028602276276,
0.00731918496982359));
#15608=CARTESIAN_POINT('Ctrl Pts',(-0.172087192378165,0.0175525219725009,
0.0152581746071293));
#15609=CARTESIAN_POINT('Ctrl Pts',(-0.108045720411827,-0.135108484733225,
0.0231971642444351));
#15610=CARTESIAN_POINT('Ctrl Pts',(0.0549144151285058,-0.164025561655164,
0.0311361538817407));
#15611=CARTESIAN_POINT('Ctrl Pts',(0.167598788591005,-0.0428207868793744,
0.0390751435190465));
#15612=CARTESIAN_POINT('Ctrl Pts',(0.126860790413016,0.117600499296196,
0.0470141331563521));
#15613=CARTESIAN_POINT('Ctrl Pts',(-0.0300110592737492,0.170357625684536,
0.054953122793658));
#15614=CARTESIAN_POINT('Ctrl Pts',(-0.159409054995301,0.0671687418111174,
0.0628921124309635));
#15615=CARTESIAN_POINT('Ctrl Pts',(-0.142879399887002,-0.0975110083167992,
0.0708311020682695));
#15616=CARTESIAN_POINT('Ctrl Pts',(0.00444677171871267,-0.172924803493063,
0.078770091705575));
#15617=CARTESIAN_POINT('Ctrl Pts',(0.147702113712341,-0.0900384822365835,
0.0867090813428809));
#15618=CARTESIAN_POINT('Ctrl Pts',(0.155746353789385,0.0752722621313087,
0.0946480709801864));
#15619=CARTESIAN_POINT('Ctrl Pts',(0.021215449100004,0.17167621786987,0.102587060617492));
#15620=CARTESIAN_POINT('Ctrl Pts',(-0.132736728465598,0.110922462699857,
0.110526050254798));
#15621=CARTESIAN_POINT('Ctrl Pts',(-0.165177537004225,-0.0513732581591355,
0.118465039892104));
#15622=CARTESIAN_POINT('Ctrl Pts',(-0.0464096261145344,-0.166640254043574,
0.126404029529409));
#15623=CARTESIAN_POINT('Ctrl Pts',(0.114843114370719,-0.129359532685675,
0.134343019166715));
#15624=CARTESIAN_POINT('Ctrl Pts',(0.170964855654229,0.0263409830179588,
0.142282008804021));
#15625=CARTESIAN_POINT('Ctrl Pts',(0.0705799878925336,0.157928129946847,
0.150220998441327));
#15626=CARTESIAN_POINT('Ctrl Pts',(-0.0944160212638482,0.144942899583874,
0.158159988078632));
#15627=CARTESIAN_POINT('Ctrl Pts',(-0.172980633894512,-0.000727622896455919,
0.166098977715938));
#15628=CARTESIAN_POINT('Ctrl Pts',(-0.0931933312323777,-0.145732055885043,
0.174037967353244));
#15629=CARTESIAN_POINT('Ctrl Pts',(0.0719060791645076,-0.157328779695546,
0.181976956990549));
#15630=CARTESIAN_POINT('Ctrl Pts',(0.171180402159323,-0.0249017879745179,
0.189915946627855));
#15631=CARTESIAN_POINT('Ctrl Pts',(0.113750798721884,0.13032108391891,0.197854936265161));
#15632=CARTESIAN_POINT('Ctrl Pts',(-0.0478098650864174,0.16624393501773,
0.205793925902467));
#15633=CARTESIAN_POINT('Ctrl Pts',(-0.16560387403618,0.0499818570245514,
0.213732915539772));
#15634=CARTESIAN_POINT('Ctrl Pts',(-0.131798885878402,-0.112035185581475,
0.221671905177078));
#15635=CARTESIAN_POINT('Ctrl Pts',(0.0226589495323734,-0.171491694067101,
0.229610894814384));
#15636=CARTESIAN_POINT('Ctrl Pts',(0.156374069566079,-0.073959309724122,
0.237549884451689));
#15637=CARTESIAN_POINT('Ctrl Pts',(0.146939445926624,0.0912777539068999,
0.245488874088995));
#15638=CARTESIAN_POINT('Ctrl Pts',(0.00299182995941577,0.172956289510158,
0.253427863726301));
#15639=CARTESIAN_POINT('Ctrl Pts',(-0.143694601292225,0.0963051955349955,
0.261366853363607));
#15640=CARTESIAN_POINT('Ctrl Pts',(-0.15883847309497,-0.0685067047260848,
0.269305843000912));
#15641=CARTESIAN_POINT('Ctrl Pts',(-0.0285766086907934,-0.170605411881679,
0.277244832638218));
#15642=CARTESIAN_POINT('Ctrl Pts',(0.12784518248692,-0.116526556812001,
0.285183822275524));
#15643=CARTESIAN_POINT('Ctrl Pts',(0.167233470900423,0.0442243749325307,
0.293122811912829));
#15644=CARTESIAN_POINT('Ctrl Pts',(0.0535309779628647,0.164490922320707,
0.301061801550136));
#15645=CARTESIAN_POINT('Ctrl Pts',(-0.109175456582181,0.134177303623408,
0.309000791187441));
#15646=CARTESIAN_POINT('Ctrl Pts',(-0.171939242908932,-0.0189664407699395,
0.316939780824747));
#15647=CARTESIAN_POINT('Ctrl Pts',(-0.0773044361184472,-0.154747708493488,
0.324878770462053));
#15648=CARTESIAN_POINT('Ctrl Pts',(0.0880972839194656,-0.148868054644337,
0.332817760099358));
#15649=CARTESIAN_POINT('Ctrl Pts',(0.172851978230285,-0.00670989936239309,
0.340756749736664));
#15650=CARTESIAN_POINT('Ctrl Pts',(0.0993725327910066,0.141590708926387,
0.34869573937397));
#15651=CARTESIAN_POINT('Ctrl Pts',(-0.0650756559739905,0.160274727038081,
0.356634729011275));
#15652=CARTESIAN_POINT('Ctrl Pts',(-0.169951541620772,0.0322382168908211,
0.364573718648582));
#15653=CARTESIAN_POINT('Ctrl Pts',(-0.119248438453561,-0.125310171390688,
0.372512708285886));
#15654=CARTESIAN_POINT('Ctrl Pts',(0.0406184374886585,-0.168145685830938,
0.380451697923193));
#15655=CARTESIAN_POINT('Ctrl Pts',(0.163301917673335,-0.0570553486694088,
0.388390687560498));
#15656=CARTESIAN_POINT('Ctrl Pts',(0.136493684039406,0.106265249940549,
0.396329677197804));
#15657=CARTESIAN_POINT('Ctrl Pts',(-0.0152651628095069,0.172307295063139,
0.404268666835109));
#15658=CARTESIAN_POINT('Ctrl Pts',(-0.153049799296248,0.0806138205455782,
0.412207656472416));
#15659=CARTESIAN_POINT('Ctrl Pts',(-0.150727833715048,-0.0848760818555219,
0.420146646109721));
#15660=CARTESIAN_POINT('Ctrl Pts',(-0.0104248664208018,-0.172667748255674,
0.428085635747027));
#15661=CARTESIAN_POINT('Ctrl Pts',(0.139421351618932,-0.10239392482138,
0.436024625384332));
#15662=CARTESIAN_POINT('Ctrl Pts',(0.16163687742079,0.0616145192729195,
0.443963615021638));
#15663=CARTESIAN_POINT('Ctrl Pts',(0.0358849196425865,0.169219093691645,
0.451902604658944));
#15664=CARTESIAN_POINT('Ctrl Pts',(-0.122717222714247,0.121915185177559,
0.45984159429625));
#15665=CARTESIAN_POINT('Ctrl Pts',(-0.168980158036723,-0.0369937199732681,
0.467780583933555));
#15666=CARTESIAN_POINT('Ctrl Pts',(-0.0605533396431397,-0.162037409833775,
0.475719573570861));
#15667=CARTESIAN_POINT('Ctrl Pts',(0.103305911202344,-0.138746956140414,
0.483658563208167));
#15668=CARTESIAN_POINT('Ctrl Pts',(0.172595680358559,0.0115568269495825,
0.491597552845473));
#15669=CARTESIAN_POINT('Ctrl Pts',(0.0838859329010004,0.151281127008313,
0.499536542482778));
#15670=CARTESIAN_POINT('Ctrl Pts',(-0.0816156370489812,0.152517923263679,
0.507475532120084));
#15671=CARTESIAN_POINT('Ctrl Pts',(-0.172403684765527,0.0141350135070757,
0.51541452175739));
#15672=CARTESIAN_POINT('Ctrl Pts',(-0.105367974675403,-0.137187532379513,
0.523353511394695));
#15673=CARTESIAN_POINT('Ctrl Pts',(0.0581248948911363,-0.162924294448283,
0.531292501032001));
#15674=CARTESIAN_POINT('Ctrl Pts',(0.168408406744046,-0.039515030880773,
0.539231490669306));
#15675=CARTESIAN_POINT('Ctrl Pts',(0.124525564004667,0.120067535316156,
0.547170480306613));
#15676=CARTESIAN_POINT('Ctrl Pts',(-0.0333518982867267,0.169736501696743,
0.555109469943918));
#15677=CARTESIAN_POINT('Ctrl Pts',(-0.160697983451488,0.0640233335761385,
0.563048459581225));
#15678=CARTESIAN_POINT('Ctrl Pts',(-0.14093607811848,-0.100298808627811,
0.570987449218529));
#15679=CARTESIAN_POINT('Ctrl Pts',(0.00784314775175556,-0.172804265459278,
0.578926438855836));
#15680=CARTESIAN_POINT('Ctrl Pts',(0.149442509381278,-0.0871192603125336,
0.586865428493141));
#15681=CARTESIAN_POINT('Ctrl Pts',(0.154237495636292,0.0783174569774929,
0.594804418130446));
#15682=CARTESIAN_POINT('Ctrl Pts',(0.0178386252221998,0.172059909850489,
0.602743407767753));
#15683=CARTESIAN_POINT('Ctrl Pts',(-0.134890284021987,0.108293307291099,
0.610682397405058));
#15684=CARTESIAN_POINT('Ctrl Pts',(-0.164136382878957,-0.0546083962682395,
0.618621387042364));
#15685=CARTESIAN_POINT('Ctrl Pts',(-0.0431268722112106,-0.167519855601819,
0.62656037667967));
#15686=CARTESIAN_POINT('Ctrl Pts',(0.117362334288317,-0.127078368017432,
0.634499366316975));
#15687=CARTESIAN_POINT('Ctrl Pts',(0.170414367112955,0.0296946562375699,
0.642438355954282));
#15688=CARTESIAN_POINT('Ctrl Pts',(0.0674637261050104,0.159284257814778,
0.650377345591586));
#15689=CARTESIAN_POINT('Ctrl Pts',(-0.0972453325609638,0.143060037825677,
0.658316335228894));
#15690=CARTESIAN_POINT('Ctrl Pts',(-0.172932953925271,-0.00412584224812367,
0.666255324866198));
#15691=CARTESIAN_POINT('Ctrl Pts',(-0.0903123078403481,-0.147534796506203,
0.674194314503505));
#15692=CARTESIAN_POINT('Ctrl Pts',(0.0749830665657334,-0.155885755782802,
0.68213330414081));
#15693=CARTESIAN_POINT('Ctrl Pts',(0.17163658245605,-0.021533989188811,
0.690072293778116));
#15694=CARTESIAN_POINT('Ctrl Pts',(0.11116857013107,0.132530668686874,0.698011283415421));
#15695=CARTESIAN_POINT('Ctrl Pts',(-0.0510666492692211,0.165272582299639,
0.705950273052727));
#15696=CARTESIAN_POINT('Ctrl Pts',(-0.166553851089581,0.0467187736868841,
0.713889262690032));
#15697=CARTESIAN_POINT('Ctrl Pts',(-0.129572416918314,-0.114602870389546,
0.721828252327339));
#15698=CARTESIAN_POINT('Ctrl Pts',(0.0260236847639906,-0.171013440871999,
0.729767241964644));
#15699=CARTESIAN_POINT('Ctrl Pts',(0.157796886564457,-0.0708729265526718,
0.73770623160195));
#15700=CARTESIAN_POINT('Ctrl Pts',(0.145117853242075,0.0941468947867542,
0.745645221239255));
#15701=CARTESIAN_POINT('Ctrl Pts',(-0.000406629147419015,0.172981686256994,
0.753584210876562));
#15702=CARTESIAN_POINT('Ctrl Pts',(-0.145558870420566,0.0934635991681543,
0.761523200513868));
#15703=CARTESIAN_POINT('Ctrl Pts',(-0.157461941624574,-0.0716140074803496,
0.769462190151172));
#15704=CARTESIAN_POINT('Ctrl Pts',(-0.0252193968429213,-0.17113389830906,
0.777401179788479));
#15705=CARTESIAN_POINT('Ctrl Pts',(0.130109777350283,-0.113992433807847,
0.785340169425784));
#15706=CARTESIAN_POINT('Ctrl Pts',(0.166332367384696,0.0475012914327479,
0.793279159063091));
#15707=CARTESIAN_POINT('Ctrl Pts',(0.0502890745800368,0.165510839842773,
0.801218148700395));
#15708=CARTESIAN_POINT('Ctrl Pts',(-0.111790419467279,0.132006557575396,
0.809157138337702));
#15709=CARTESIAN_POINT('Ctrl Pts',(-0.171533445990104,-0.0223406811520247,
0.817096127975007));
#15710=CARTESIAN_POINT('Ctrl Pts',(-0.0742493586638003,-0.156236557391639,
0.825035117612313));
#15711=CARTESIAN_POINT('Ctrl Pts',(0.0910049278783345,-0.147108572929777,
0.832974107249618));
#15712=CARTESIAN_POINT('Ctrl Pts',(0.172950439922886,-0.00331277195964383,
0.840913096886925));
#15713=CARTESIAN_POINT('Ctrl Pts',(0.0965716772857839,0.143515644700454,
0.848852086524229));
#15714=CARTESIAN_POINT('Ctrl Pts',(-0.0682118374171683,0.158965324406771,
0.856791076161536));
#15715=CARTESIAN_POINT('Ctrl Pts',(-0.170552089827228,0.0288931442238776,
0.864730065798841));
#15716=CARTESIAN_POINT('Ctrl Pts',(-0.116763592698541,-0.127628729319482,
0.872669055436147));
#15717=CARTESIAN_POINT('Ctrl Pts',(0.0439139712140358,-0.167315248138923,
0.880608045073453));
#15718=CARTESIAN_POINT('Ctrl Pts',(0.164391304101163,-0.0538361241500125,
0.888547034710759));
#15719=CARTESIAN_POINT('Ctrl Pts',(0.134379664555536,0.108926281867684,
0.896486024348063));
#15720=CARTESIAN_POINT('Ctrl Pts',(-0.018647348250808,0.17197414204115,
0.904425013985371));
#15721=CARTESIAN_POINT('Ctrl Pts',(-0.154603991719776,0.0775914613336281,
0.912364003622676));
#15722=CARTESIAN_POINT('Ctrl Pts',(-0.149031276472826,-0.0878208845346985,
0.920302993259982));
#15723=CARTESIAN_POINT('Ctrl Pts',(-0.00703064139541984,-0.172839229369798,
0.928241982897287));
#15724=CARTESIAN_POINT('Ctrl Pts',(0.141406064038169,-0.099635105162837,
0.936180972534593));
#15725=CARTESIAN_POINT('Ctrl Pts',(0.160395209035295,0.064778129380991,
0.944119962171899));
#15726=CARTESIAN_POINT('Ctrl Pts',(0.03255353276219,0.169891426011666,0.952058951809204));
#15727=CARTESIAN_POINT('Ctrl Pts',(-0.125088671715395,0.119480765548496,
0.959997941446511));
#15728=CARTESIAN_POINT('Ctrl Pts',(-0.168220770124088,-0.040306347222682,
0.967936931083815));
#15729=CARTESIAN_POINT('Ctrl Pts',(-0.0573582824064844,-0.163195761485875,
0.975875920721122));
#15730=CARTESIAN_POINT('Ctrl Pts',(0.106011781834435,-0.136690640644722,
0.983814910358427));
#15731=CARTESIAN_POINT('Ctrl Pts',(0.17233532526783,0.014945393685262,0.991753899995733));
#15732=CARTESIAN_POINT('Ctrl Pts',(0.0808976893297158,0.152899944371113,
0.999692889633039));
#15733=CARTESIAN_POINT('Ctrl Pts',(-0.0845962369090198,0.150885074902754,
1.00763187927034));
#15734=CARTESIAN_POINT('Ctrl Pts',(-0.172648106016301,0.0107452601904448,
1.01557086890765));
#15735=CARTESIAN_POINT('Ctrl Pts',(-0.102652466413112,-0.13923110380544,
1.02350985854496));
#15736=CARTESIAN_POINT('Ctrl Pts',(0.0613144709582997,-0.161750934398167,
1.03144884818226));
#15737=CARTESIAN_POINT('Ctrl Pts',(0.169152212322519,-0.0361988700648799,
1.03938783781957));
#15738=CARTESIAN_POINT('Ctrl Pts',(0.122142696063681,0.12249077894222,1.04732682745687));
#15739=CARTESIAN_POINT('Ctrl Pts',(-0.0366800874558037,0.169048514669047,
1.05526581709418));
#15740=CARTESIAN_POINT('Ctrl Pts',(-0.161924764760067,0.0608539208677085,
1.06320480673148));
#15741=CARTESIAN_POINT('Ctrl Pts',(-0.138938417355371,-0.103048266896446,
1.07114379636879));
#15742=CARTESIAN_POINT('Ctrl Pts',(0.011236529066559,-0.172616828675865,
1.0790827860061));
#15743=CARTESIAN_POINT('Ctrl Pts',(0.151125203217684,-0.0841665140064042,
1.0870217756434));
#15744=CARTESIAN_POINT('Ctrl Pts',(0.152669111109608,0.0813324759279986,
1.09496076528071));
#15745=CARTESIAN_POINT('Ctrl Pts',(0.0144549108781955,0.172377158228925,
1.10289975491801));
#15746=CARTESIAN_POINT('Ctrl Pts',(-0.136991769602464,0.10562236594946,
1.11083874455532));
#15747=CARTESIAN_POINT('Ctrl Pts',(-0.163031873671196,-0.0578224635832477,
1.11877773419263));
#15748=CARTESIAN_POINT('Ctrl Pts',(-0.0398274706979539,-0.168334790537727,
1.12671672382993));
#15749=CARTESIAN_POINT('Ctrl Pts',(0.119836252144435,-0.124748153491552,
1.13465571346724));
#15750=CARTESIAN_POINT('Ctrl Pts',(0.169798099063322,0.0330368685268242,
1.14259470310454));
#15751=CARTESIAN_POINT('Ctrl Pts',(0.0643214233134591,0.160578901573361,
1.15053369274185));
#15752=CARTESIAN_POINT('Ctrl Pts',(-0.100037107244844,0.141121955420339,
1.15847268237915));
#15753=CARTESIAN_POINT('Ctrl Pts',(-0.172818522111203,-0.00752246920075927,
1.16641167201646));
#15754=CARTESIAN_POINT('Ctrl Pts',(-0.0873964240115842,-0.149280588817046,
1.17435066165376));
#15755=CARTESIAN_POINT('Ctrl Pts',(0.0780311106025284,-0.154382560238235,
1.18228965129107));
#15756=CARTESIAN_POINT('Ctrl Pts',(0.172026511281289,-0.01815787828917,
1.19022864092837));
#15757=CARTESIAN_POINT('Ctrl Pts',(0.10854343062882,0.134689096792963,1.19816763056568));
#15758=CARTESIAN_POINT('Ctrl Pts',(-0.0543037217972188,0.164237434607784,
1.20610662020299));
#15759=CARTESIAN_POINT('Ctrl Pts',(-0.167439538594998,0.0434376569656869,
1.21404560984029));
#15760=CARTESIAN_POINT('Ctrl Pts',(-0.127295933190098,-0.117126318651471,
1.2219845994776));
#15761=CARTESIAN_POINT('Ctrl Pts',(0.0293783748903316,-0.170469176734012,
1.2299235891149));
#15762=CARTESIAN_POINT('Ctrl Pts',(0.159158794190081,-0.0677591865323411,
1.23786257875221));
#15763=CARTESIAN_POINT('Ctrl Pts',(0.143240245273553,0.0969796950995427,
1.24580156838952));
#15764=CARTESIAN_POINT('Ctrl Pts',(-0.00380493129617075,0.172940312320012,
1.25374055802682));
#15765=CARTESIAN_POINT('Ctrl Pts',(-0.147366954032488,0.0905859259858403,
1.26167954766413));
#15766=CARTESIAN_POINT('Ctrl Pts',(-0.156024630070406,-0.074693667330688,
1.26961853730143));
#15767=CARTESIAN_POINT('Ctrl Pts',(-0.0218524503424686,-0.171596327294885,
1.27755752693874));
#15768=CARTESIAN_POINT('Ctrl Pts',(0.132324150022753,-0.111414309889572,
1.28549651657604));
#15769=CARTESIAN_POINT('Ctrl Pts',(0.165367059817933,0.0507598725070622,
1.29343550621335));
#15770=CARTESIAN_POINT('Ctrl Pts',(0.0470277596764783,0.166466870408131,
1.30137449585065));
#15771=CARTESIAN_POINT('Ctrl Pts',(-0.114362231391601,0.129784857201791,
1.30931348548797));
#15772=CARTESIAN_POINT('Ctrl Pts',(-0.171061437441431,-0.0257062980954763,
1.31725247512526));
#15773=CARTESIAN_POINT('Ctrl Pts',(-0.071165620995849,-0.157665099140374,
1.32519146476257));
#15774=CARTESIAN_POINT('Ctrl Pts',(0.0938774439379855,-0.145292307632914,
1.33313045439988));
#15775=CARTESIAN_POINT('Ctrl Pts',(0.172982143233999,8.56343898915854E-5,
1.34106944403719));
#15776=CARTESIAN_POINT('Ctrl Pts',(0.0937335447930804,0.145385183220099,
1.34900843367449));
#15777=CARTESIAN_POINT('Ctrl Pts',(-0.0713216883190155,0.157594562185848,
1.3569474233118));
#15778=CARTESIAN_POINT('Ctrl Pts',(-0.171086806821499,0.0255369173285507,
1.3648864129491));
#15779=CARTESIAN_POINT('Ctrl Pts',(-0.114233673229396,-0.129898019862958,
1.37282540258641));
#15780=CARTESIAN_POINT('Ctrl Pts',(0.0471925482590101,-0.166420232464351,
1.38076439222371));
#15781=CARTESIAN_POINT('Ctrl Pts',(0.165417247017141,-0.0505961085897048,
1.38870338186102));
#15782=CARTESIAN_POINT('Ctrl Pts',(0.132213753266125,0.111545248710567,
1.39664237149832));
#15783=CARTESIAN_POINT('Ctrl Pts',(-0.0220222951247444,0.17157464463752,
1.40458136113563));
#15784=CARTESIAN_POINT('Ctrl Pts',(-0.156098584526576,0.0745390809398717,
1.41252035077293));
#15785=CARTESIAN_POINT('Ctrl Pts',(-0.147277046608992,-0.0907316537045687,
1.42045934041024));
#15786=CARTESIAN_POINT('Ctrl Pts',(-0.00363398118293899,-0.172944250658386,
1.42839833004755));
#15787=CARTESIAN_POINT('Ctrl Pts',(0.143336722904634,-0.0968373407211472,
1.43633731968485));
#15788=CARTESIAN_POINT('Ctrl Pts',(0.159090624036536,0.0679158129692223,
1.44427630932216));
#15789=CARTESIAN_POINT('Ctrl Pts',(0.0292114869387437,0.170499931406899,
1.45221529895946));
#15790=CARTESIAN_POINT('Ctrl Pts',(-0.127415456569397,0.116996902323752,
1.46015428859677));
#15791=CARTESIAN_POINT('Ctrl Pts',(-0.167389576437263,-0.0435971050111283,
1.46809327823408));
#15792=CARTESIAN_POINT('Ctrl Pts',(-0.0541541359620402,-0.164303103757731,
1.47603226787138));
#15793=CARTESIAN_POINT('Ctrl Pts',(0.108701533888403,-0.13455879509903,
1.48397125750869));
#15794=CARTESIAN_POINT('Ctrl Pts',(0.171961157005542,0.0182848320604298,
1.49191024714599));
#15795=CARTESIAN_POINT('Ctrl Pts',(0.0779697431325927,0.154543202561513,
1.4998492367833));
#15796=CARTESIAN_POINT('Ctrl Pts',(-0.0877325682749983,0.149025855561406,
1.5077882264206));
#15797=CARTESIAN_POINT('Ctrl Pts',(-0.144149484752264,0.0548439265155397,
1.51308088617881));
#15798=CARTESIAN_POINT('Ctrl Pts',(-0.146217781693078,0.00621955116994065,
1.51572721605791));
#15799=CARTESIAN_POINT('Ctrl Pts',(0.0795408277542855,-0.111329858282327,
-0.0109985226280624));
#15800=CARTESIAN_POINT('Ctrl Pts',(0.116563307192903,-0.0848787452970238,
-0.00835219274896048));
#15801=CARTESIAN_POINT('Ctrl Pts',(0.16150817751539,0.00739908052493189,
-0.00305953299075667));
#15802=CARTESIAN_POINT('Ctrl Pts',(0.0812084309002137,0.139981433724326,
0.00487945664654907));
#15803=CARTESIAN_POINT('Ctrl Pts',(-0.0734975292821143,0.144003850402812,
0.0128184462838548));
#15804=CARTESIAN_POINT('Ctrl Pts',(-0.160887120581772,0.0164101388376342,
0.0207574359211605));
#15805=CARTESIAN_POINT('Ctrl Pts',(-0.101013704785435,-0.126315124179183,
0.0286964255584662));
#15806=CARTESIAN_POINT('Ctrl Pts',(0.0513403816191153,-0.153350170642076,
0.0366354151957719));
#15807=CARTESIAN_POINT('Ctrl Pts',(0.156690838735662,-0.0400338514845966,
0.0445744048330777));
#15808=CARTESIAN_POINT('Ctrl Pts',(0.118604220350264,0.109946623274354,
0.0525133944703833));
#15809=CARTESIAN_POINT('Ctrl Pts',(-0.0280578283917351,0.15927012049393,
0.0604523841076892));
#15810=CARTESIAN_POINT('Ctrl Pts',(-0.14903412333264,0.0627971513379326,
0.0683913737449947));
#15811=CARTESIAN_POINT('Ctrl Pts',(-0.133580279395553,-0.0911646307683348,
0.0763303633823007));
#15812=CARTESIAN_POINT('Ctrl Pts',(0.0041573593468571,-0.161670216863261,
0.0842693530196062));
#15813=CARTESIAN_POINT('Ctrl Pts',(0.138089113144455,-0.0841784443595545,
0.0922083426569122));
#15814=CARTESIAN_POINT('Ctrl Pts',(0.14560980428584,0.0703732645446943,
0.100147332294218));
#15815=CARTESIAN_POINT('Ctrl Pts',(0.0198346691022095,0.160502893816501,
0.108086321931524));
#15816=CARTESIAN_POINT('Ctrl Pts',(-0.124097730593135,0.103703218031488,
0.116025311568829));
#15817=CARTESIAN_POINT('Ctrl Pts',(-0.154427171169137,-0.0480296962598115,
0.123964301206135));
#15818=CARTESIAN_POINT('Ctrl Pts',(-0.0433891157712434,-0.155794689166463,
0.13190329084344));
#15819=CARTESIAN_POINT('Ctrl Pts',(0.107368699171666,-0.12094033522185,
0.139842280480747));
#15820=CARTESIAN_POINT('Ctrl Pts',(0.15983782968835,0.0246266142906177,
0.147781270118052));
#15821=CARTESIAN_POINT('Ctrl Pts',(0.0659863808909888,0.147649582370873,
0.155720259755358));
#15822=CARTESIAN_POINT('Ctrl Pts',(-0.0882710769349216,0.135509478890084,
0.163659249392663));
#15823=CARTESIAN_POINT('Ctrl Pts',(-0.161722413615419,-0.00068026650363694,
0.171598239029969));
#15824=CARTESIAN_POINT('Ctrl Pts',(-0.0871279640988751,-0.136247273976568,
0.179537228667275));
#15825=CARTESIAN_POINT('Ctrl Pts',(0.0672261652318651,-0.147089240053593,
0.187476218304581));
#15826=CARTESIAN_POINT('Ctrl Pts',(0.160039347628626,-0.023281087390596,
0.195415207941886));
#15827=CARTESIAN_POINT('Ctrl Pts',(0.106347475470598,0.121839305139765,
0.203354197579192));
#15828=CARTESIAN_POINT('Ctrl Pts',(-0.0446982220051161,0.15542416405057,
0.211293187216498));
#15829=CARTESIAN_POINT('Ctrl Pts',(-0.154825760608133,0.0467288526640558,
0.219232176853804));
#15830=CARTESIAN_POINT('Ctrl Pts',(-0.12322092627477,-0.104743520787053,
0.227171166491109));
#15831=CARTESIAN_POINT('Ctrl Pts',(0.0211842211805034,-0.160330379506191,
0.235110156128415));
#15832=CARTESIAN_POINT('Ctrl Pts',(0.146196665995071,-0.0691457639426259,
0.24304914576572));
#15833=CARTESIAN_POINT('Ctrl Pts',(0.137376082602736,0.0853370596399817,
0.250988135403027));
#15834=CARTESIAN_POINT('Ctrl Pts',(0.00279711058556459,0.161699653653757,
0.258927125040332));
#15835=CARTESIAN_POINT('Ctrl Pts',(-0.134342424474264,0.0900372967480426,
0.266866114677638));
#15836=CARTESIAN_POINT('Ctrl Pts',(-0.148500677015507,-0.0640480346713102,
0.274805104314944));
#15837=CARTESIAN_POINT('Ctrl Pts',(-0.0267167371651392,-0.159501779847699,
0.282744093952249));
#15838=CARTESIAN_POINT('Ctrl Pts',(0.119524544542348,-0.108942576944327,
0.290683083589556));
#15839=CARTESIAN_POINT('Ctrl Pts',(0.156349297273321,0.0413460888291301,
0.29862207322686));
#15840=CARTESIAN_POINT('Ctrl Pts',(0.0500469836677093,0.153785243912065,
0.306561062864167));
#15841=CARTESIAN_POINT('Ctrl Pts',(-0.102069913541897,0.125444547784578,
0.314500052501472));
#15842=CARTESIAN_POINT('Ctrl Pts',(-0.160748800211922,-0.0177320345633525,
0.322439042138778));
#15843=CARTESIAN_POINT('Ctrl Pts',(-0.0722731771226978,-0.144676154524232,
0.330378031776084));
#15844=CARTESIAN_POINT('Ctrl Pts',(0.082363586418043,-0.139179170322594,
0.338317021413389));
#15845=CARTESIAN_POINT('Ctrl Pts',(0.16160213133829,-0.00627319426210969,
0.346256011050695));
#15846=CARTESIAN_POINT('Ctrl Pts',(0.0929050003357002,0.132375461215256,
0.354195000688001));
#15847=CARTESIAN_POINT('Ctrl Pts',(-0.0608402912787218,0.149843454232904,
0.362133990325306));
#15848=CARTESIAN_POINT('Ctrl Pts',(-0.158890465884947,0.0301400343429239,
0.370072979962613));
#15849=CARTESIAN_POINT('Ctrl Pts',(-0.1114873084483,-0.117154521356547,
0.378011969599918));
#15850=CARTESIAN_POINT('Ctrl Pts',(0.0379748391485164,-0.157202141877815,
0.385950959237223));
#15851=CARTESIAN_POINT('Ctrl Pts',(0.152673624090564,-0.0533419752763387,
0.39388994887453));
#15852=CARTESIAN_POINT('Ctrl Pts',(0.127610169584502,0.0993491139263089,
0.401828938511835));
#15853=CARTESIAN_POINT('Ctrl Pts',(-0.014271649480085,0.16109289816887,
0.409767928149142));
#15854=CARTESIAN_POINT('Ctrl Pts',(-0.143088751545671,0.0753671745551693,
0.417706917786446));
#15855=CARTESIAN_POINT('Ctrl Pts',(-0.140917908083783,-0.0793520321139836,
0.425645907423752));
#15856=CARTESIAN_POINT('Ctrl Pts',(-0.00974637750615997,-0.161429891732714,
0.433584897061058));
#15857=CARTESIAN_POINT('Ctrl Pts',(0.130347293715478,-0.0957297489831606,
0.441523886698364));
#15858=CARTESIAN_POINT('Ctrl Pts',(0.15111695082405,0.0576044181723055,
0.449462876335669));
#15859=CARTESIAN_POINT('Ctrl Pts',(0.0335493961742207,0.158205688379633,
0.457401865972975));
#15860=CARTESIAN_POINT('Ctrl Pts',(-0.114730331382826,0.113980493419335,
0.465340855610281));
#15861=CARTESIAN_POINT('Ctrl Pts',(-0.157982303542021,-0.03458603167299,
0.473279845247587));
#15862=CARTESIAN_POINT('Ctrl Pts',(-0.0566123040428622,-0.151491415104245,
0.481218834884892));
#15863=CARTESIAN_POINT('Ctrl Pts',(0.0965823799129518,-0.129716790392294,
0.489157824522198));
#15864=CARTESIAN_POINT('Ctrl Pts',(0.161362514281243,0.0108046658515635,
0.497096814159504));
#15865=CARTESIAN_POINT('Ctrl Pts',(0.0784263257203939,0.141435191000425,
0.50503580379681));
#15866=CARTESIAN_POINT('Ctrl Pts',(-0.076303789130349,0.14259149197508,
0.512974793434115));
#15867=CARTESIAN_POINT('Ctrl Pts',(-0.161183014472451,0.0132150544797126,
0.520913783071421));
#15868=CARTESIAN_POINT('Ctrl Pts',(-0.0985102366584373,-0.128258859705,
0.528852772708727));
#15869=CARTESIAN_POINT('Ctrl Pts',(0.0543419114689404,-0.152320577983508,
0.536791762346032));
#15870=CARTESIAN_POINT('Ctrl Pts',(0.157447763940923,-0.0369432463290883,
0.544730751983338));
#15871=CARTESIAN_POINT('Ctrl Pts',(0.116420979124965,0.112253095453589,
0.552669741620643));
#15872=CARTESIAN_POINT('Ctrl Pts',(-0.0311812332291155,0.158689421555565,
0.56060873125795));
#15873=CARTESIAN_POINT('Ctrl Pts',(-0.150239163551416,0.0598564579197502,
0.568547720895255));
#15874=CARTESIAN_POINT('Ctrl Pts',(-0.131763436204723,-0.0937709907106254,
0.576486710532561));
#15875=CARTESIAN_POINT('Ctrl Pts',(0.00733268664935855,-0.161557523891122,
0.584425700169866));
#15876=CARTESIAN_POINT('Ctrl Pts',(0.139716237417787,-0.0814492162095161,
0.592364689807173));
#15877=CARTESIAN_POINT('Ctrl Pts',(0.144199148209332,0.0732202668325601,
0.600303679444478));
#15878=CARTESIAN_POINT('Ctrl Pts',(0.0166776214282734,0.160861613702037,
0.608242669081784));
#15879=CARTESIAN_POINT('Ctrl Pts',(-0.126111124778327,0.101245177793678,
0.616181658719089));
#15880=CARTESIAN_POINT('Ctrl Pts',(-0.153453779210204,-0.0510542795996006,
0.624120648356396));
#15881=CARTESIAN_POINT('Ctrl Pts',(-0.0403200156494649,-0.156617042997737,
0.6320596379937));
#15882=CARTESIAN_POINT('Ctrl Pts',(0.10972395892722,-0.118807637198397,
0.639998627631007));
#15883=CARTESIAN_POINT('Ctrl Pts',(0.159323168980049,0.0277620180369333,
0.647937617268312));
#15884=CARTESIAN_POINT('Ctrl Pts',(0.0630729369615192,0.148917448414806,
0.655876606905618));
#15885=CARTESIAN_POINT('Ctrl Pts',(-0.0909162461746061,0.133749160748195,
0.663815596542924));
#15886=CARTESIAN_POINT('Ctrl Pts',(-0.161677836835157,-0.00385731715476066,
0.671754586180229));
#15887=CARTESIAN_POINT('Ctrl Pts',(-0.0844344483789265,-0.137932685561743,
0.679693575817536));
#15888=CARTESIAN_POINT('Ctrl Pts',(0.0701028908975481,-0.145740133481257,
0.687632565454841));
#15889=CARTESIAN_POINT('Ctrl Pts',(0.1604658380222,-0.0201324774223393,
0.695571555092147));
#15890=CARTESIAN_POINT('Ctrl Pts',(0.10393330787963,0.123905081947942,0.703510544729453));
#15891=CARTESIAN_POINT('Ctrl Pts',(-0.0477430426119635,0.15451603056473,
0.711449534366758));
#15892=CARTESIAN_POINT('Ctrl Pts',(-0.155713909636705,0.0436781428746717,
0.719388524004064));
#15893=CARTESIAN_POINT('Ctrl Pts',(-0.121139364160222,-0.10714409115852,
0.72732751364137));
#15894=CARTESIAN_POINT('Ctrl Pts',(0.0243299669821161,-0.159883252800214,
0.735266503278675));
#15895=CARTESIAN_POINT('Ctrl Pts',(0.147526880793862,-0.0662602540182413,
0.743205492915981));
#15896=CARTESIAN_POINT('Ctrl Pts',(0.135673045916277,0.0880194662056535,
0.751144482553287));
#15897=CARTESIAN_POINT('Ctrl Pts',(-0.000380164216571841,0.161723397486253,
0.759083472190592));
#15898=CARTESIAN_POINT('Ctrl Pts',(-0.136085360063504,0.0873806419964673,
0.767022461827899));
#15899=CARTESIAN_POINT('Ctrl Pts',(-0.147213735311121,-0.0669531026545853,
0.774961451465203));
#15900=CARTESIAN_POINT('Ctrl Pts',(-0.023578025097595,-0.159995870421162,
0.78290044110251));
#15901=CARTESIAN_POINT('Ctrl Pts',(0.121641751185188,-0.106573384050283,
0.790839430739816));
#15902=CARTESIAN_POINT('Ctrl Pts',(0.155506840911589,0.0444097314676148,
0.798778420377121));
#15903=CARTESIAN_POINT('Ctrl Pts',(0.047016075363265,0.15473878142458,0.806717410014428));
#15904=CARTESIAN_POINT('Ctrl Pts',(-0.104514684958047,0.123415081928621,
0.814656399651731));
#15905=CARTESIAN_POINT('Ctrl Pts',(-0.16036941405942,-0.020886666885039,
0.82259538928904));
#15906=CARTESIAN_POINT('Ctrl Pts',(-0.0694169354231278,-0.146068103622213,
0.830534378926343));
#15907=CARTESIAN_POINT('Ctrl Pts',(0.085081990139753,-0.137534202194171,
0.838473368563651));
#15908=CARTESIAN_POINT('Ctrl Pts',(0.161694184779289,-0.00309716449182502,
0.846412358200955));
#15909=CARTESIAN_POINT('Ctrl Pts',(0.0902864348795877,0.134175115040242,
0.854351347838261));
#15910=CARTESIAN_POINT('Ctrl Pts',(-0.0637723584188847,0.148619272374149,
0.862290337475567));
#15911=CARTESIAN_POINT('Ctrl Pts',(-0.159451928190027,0.0270126713934565,
0.870229327112872));
#15912=CARTESIAN_POINT('Ctrl Pts',(-0.109164185657521,-0.119322178948671,
0.878168316750179));
#15913=CARTESIAN_POINT('Ctrl Pts',(0.0410558873341998,-0.156425752146281,
0.886107306387484));
#15914=CARTESIAN_POINT('Ctrl Pts',(0.153692109215179,-0.0503322698109037,
0.894046296024789));
#15915=CARTESIAN_POINT('Ctrl Pts',(0.125633738317809,0.101836956040625,
0.901985285662096));
#15916=CARTESIAN_POINT('Ctrl Pts',(-0.0174337097671096,0.160781427979367,
0.909924275299401));
#15917=CARTESIAN_POINT('Ctrl Pts',(-0.144541791370401,0.072541521673891,
0.917863264936708));
#15918=CARTESIAN_POINT('Ctrl Pts',(-0.13933176907,-0.082105176128868,0.925802254574012));
#15919=CARTESIAN_POINT('Ctrl Pts',(-0.00657306121577474,-0.161590212220858,
0.933741244211319));
#15920=CARTESIAN_POINT('Ctrl Pts',(0.132202833700187,-0.0931504835251481,
0.941680233848624));
#15921=CARTESIAN_POINT('Ctrl Pts',(0.149956094815541,0.0605621288182698,
0.949619223485929));
#15922=CARTESIAN_POINT('Ctrl Pts',(0.0304348282896272,0.158834262822317,
0.957558213123236));
#15923=CARTESIAN_POINT('Ctrl Pts',(-0.116947437700435,0.111704514835484,
0.965497202760542));
#15924=CARTESIAN_POINT('Ctrl Pts',(-0.157272339407096,-0.0376830608728604,
0.973436192397847));
#15925=CARTESIAN_POINT('Ctrl Pts',(-0.0536251929639052,-0.152574376940928,
0.981375182035153));
#15926=CARTESIAN_POINT('Ctrl Pts',(0.0991121424632477,-0.127794307524525,
0.989314171672459));
#15927=CARTESIAN_POINT('Ctrl Pts',(0.161119104064031,0.0139726921146952,
0.997253161309763));
#15928=CARTESIAN_POINT('Ctrl Pts',(0.0756325681075411,0.142948649734045,
1.00519215094707));
#15929=CARTESIAN_POINT('Ctrl Pts',(-0.0790904005129918,0.141064915432658,
1.01313114058437));
#15930=CARTESIAN_POINT('Ctrl Pts',(-0.161411527883023,0.0100459188627121,
1.02107013022168));
#15931=CARTESIAN_POINT('Ctrl Pts',(-0.095971463730607,-0.130169427934261,
1.02900911985899));
#15932=CARTESIAN_POINT('Ctrl Pts',(0.0573238981132153,-0.151223584550935,
1.03694810949629));
#15933=CARTESIAN_POINT('Ctrl Pts',(0.158143159897702,-0.0338429135403315,
1.0448870991336));
#15934=CARTESIAN_POINT('Ctrl Pts',(0.114193197054413,0.114518625410106,
1.0528260887709));
#15935=CARTESIAN_POINT('Ctrl Pts',(-0.0342928115212847,0.158046211271557,
1.06076507840821));
#15936=CARTESIAN_POINT('Ctrl Pts',(-0.151386101389109,0.0568933223281485,
1.06870406804552));
#15937=CARTESIAN_POINT('Ctrl Pts',(-0.129895790602315,-0.0963415040526547,
1.07664305768282));
#15938=CARTESIAN_POINT('Ctrl Pts',(0.0105052141409744,-0.161382286187737,
1.08458204732013));
#15939=CARTESIAN_POINT('Ctrl Pts',(0.141289415307547,-0.0786886455683398,
1.09252103695743));
#15940=CARTESIAN_POINT('Ctrl Pts',(0.14273283995608,0.076039057183793,1.10046002659474));
#15941=CARTESIAN_POINT('Ctrl Pts',(0.013514131745196,0.161158214381091,
1.10839901623204));
#15942=CARTESIAN_POINT('Ctrl Pts',(-0.128075837894479,0.0987480712062529,
1.11633800586935));
#15943=CARTESIAN_POINT('Ctrl Pts',(-0.152421155552179,-0.0540591635106084,
1.12427699550666));
#15944=CARTESIAN_POINT('Ctrl Pts',(-0.0372353514058616,-0.157378938949945,
1.13221598514396));
#15945=CARTESIAN_POINT('Ctrl Pts',(0.11203686504723,-0.116629081663695,
1.14015497478127));
#15946=CARTESIAN_POINT('Ctrl Pts',(0.158747009937404,0.0308867067726846,
1.14809396441857));
#15947=CARTESIAN_POINT('Ctrl Pts',(0.0601351468730053,0.150127831962932,
1.15603295405588));
#15948=CARTESIAN_POINT('Ctrl Pts',(-0.0935263218228598,0.13193721592339,
1.16397194369318));
#15949=CARTESIAN_POINT('Ctrl Pts',(-0.161570852667341,-0.00703287904607843,
1.17191093333049));
#15950=CARTESIAN_POINT('Ctrl Pts',(-0.0817083410685703,-0.13956485524354,
1.17984992296779));
#15951=CARTESIAN_POINT('Ctrl Pts',(0.0729525569401478,-0.144334771469742,
1.1877889126051));
#15952=CARTESIAN_POINT('Ctrl Pts',(0.160830388835411,-0.016976096323307,
1.19572790224241));
#15953=CARTESIAN_POINT('Ctrl Pts',(0.101479022178261,0.125923031559255,
1.20366689187971));
#15954=CARTESIAN_POINT('Ctrl Pts',(-0.0507694344715009,0.153548254118279,
1.21160588151702));
#15955=CARTESIAN_POINT('Ctrl Pts',(-0.15654195331917,0.0406105733811438,
1.21954487115432));
#15956=CARTESIAN_POINT('Ctrl Pts',(-0.119011042423884,-0.109503304062093,
1.22748386079163));
#15957=CARTESIAN_POINT('Ctrl Pts',(0.0274663214511058,-0.159374411387982,
1.23542285042894));
#15958=CARTESIAN_POINT('Ctrl Pts',(0.148800150427453,-0.0633491677300162,
1.24336184006624));
#15959=CARTESIAN_POINT('Ctrl Pts',(0.133917639627974,0.0906678973829495,
1.25130082970354));
#15960=CARTESIAN_POINT('Ctrl Pts',(-0.00355729227603857,0.161684716318317,
1.25923981934086));
#15961=CARTESIAN_POINT('Ctrl Pts',(-0.137775766897813,0.0846902584421788,
1.26717880897816));
#15962=CARTESIAN_POINT('Ctrl Pts',(-0.14586996931591,-0.0698323268364953,
1.27511779861547));
#15963=CARTESIAN_POINT('Ctrl Pts',(-0.0204302119447119,-0.160428202816007,
1.28305678825277));
#15964=CARTESIAN_POINT('Ctrl Pts',(0.123712004283314,-0.104163053984564,
1.29099577789008));
#15965=CARTESIAN_POINT('Ctrl Pts',(0.15460435913624,0.0474562320176185,
1.29893476752738));
#15966=CARTESIAN_POINT('Ctrl Pts',(0.043967018911749,0.155632589980133,
1.30687375716469));
#15967=CARTESIAN_POINT('Ctrl Pts',(-0.106919113837756,0.121337978043289,
1.31481274680199));
#15968=CARTESIAN_POINT('Ctrl Pts',(-0.159928125575155,-0.0240332370134145,
1.3227517364393));
#15969=CARTESIAN_POINT('Ctrl Pts',(-0.0665338988230771,-0.147403670583407,
1.33069072607661));
#15970=CARTESIAN_POINT('Ctrl Pts',(0.0877675522160205,-0.135836146169277,
1.33862971571391));
#15971=CARTESIAN_POINT('Ctrl Pts',(0.161723824721502,8.00609866524728E-5,
1.34656870535122));
#15972=CARTESIAN_POINT('Ctrl Pts',(0.0876330185603928,0.135922977069285,
1.35450769498852));
#15973=CARTESIAN_POINT('Ctrl Pts',(-0.0666798087068602,0.147337724435113,
1.36244668462583));
#15974=CARTESIAN_POINT('Ctrl Pts',(-0.159951843822013,0.0238748801740983,
1.37038567426313));
#15975=CARTESIAN_POINT('Ctrl Pts',(-0.106798922716859,-0.121443775659372,
1.37832466390044));
#15976=CARTESIAN_POINT('Ctrl Pts',(0.0441210824430389,-0.155588987406456,
1.38626365353774));
#15977=CARTESIAN_POINT('Ctrl Pts',(0.154651279966657,-0.0473031264624986,
1.39420264317505));
#15978=CARTESIAN_POINT('Ctrl Pts',(0.123608792556459,0.10428547082216,1.40214163281236));
#15979=CARTESIAN_POINT('Ctrl Pts',(-0.020589002599541,0.160407931346284,
1.41008062244966));
#15980=CARTESIAN_POINT('Ctrl Pts',(-0.145939110542184,0.0696878015005003,
1.41801961208697));
#15981=CARTESIAN_POINT('Ctrl Pts',(-0.137691710982408,-0.0848265016612731,
1.42595860172427));
#15982=CARTESIAN_POINT('Ctrl Pts',(-0.00339746822928561,-0.161688398335044,
1.43389759136158));
#15983=CARTESIAN_POINT('Ctrl Pts',(0.134007838137522,-0.0905348079547059,
1.44183658099889));
#15984=CARTESIAN_POINT('Ctrl Pts',(0.148736417039967,0.0634956003383226,
1.44977557063619));
#15985=CARTESIAN_POINT('Ctrl Pts',(0.0273102951854726,0.159403164432859,
1.4577145602735));
#15986=CARTESIAN_POINT('Ctrl Pts',(-0.119122786779006,0.109382310628272,
1.4656535499108));
#15987=CARTESIAN_POINT('Ctrl Pts',(-0.156495242883694,-0.0407596439572756,
1.47359253954811));
#15988=CARTESIAN_POINT('Ctrl Pts',(-0.0506295842364637,-0.153609649276743,
1.48153152918541));
#15989=CARTESIAN_POINT('Ctrl Pts',(0.10162683549218,-0.125801210382132,
1.48947051882272));
#15990=CARTESIAN_POINT('Ctrl Pts',(0.160769288057966,0.017094787472962,
1.49740950846002));
#15991=CARTESIAN_POINT('Ctrl Pts',(0.0728951834924312,0.144484958595688,
1.50534849809733));
#15992=CARTESIAN_POINT('Ctrl Pts',(-0.0820226078184241,0.139326700971572,
1.51328748773464));
#15993=CARTESIAN_POINT('Ctrl Pts',(-0.134767702434085,0.0512744806661359,
1.51858014749284));
#15994=CARTESIAN_POINT('Ctrl Pts',(-0.136701386950156,0.00581475974600206,
1.52122647737194));
#15995=CARTESIAN_POINT('Ctrl Pts',(0.0740036351041134,-0.103579689087085,
-0.0054992613140312));
#15996=CARTESIAN_POINT('Ctrl Pts',(0.108448814220036,-0.0789699563406641,
-0.00285293143492929));
#15997=CARTESIAN_POINT('Ctrl Pts',(0.150264871169078,0.00688399744800666,
0.00243972832327453));
#15998=CARTESIAN_POINT('Ctrl Pts',(0.0755551489391376,0.130236700260234,
0.0103787179605803));
#15999=CARTESIAN_POINT('Ctrl Pts',(-0.0683810376584167,0.133979098529349,
0.0183177075978859));
#16000=CARTESIAN_POINT('Ctrl Pts',(-0.14968704878538,0.0152677557027674,
0.0262566972351917));
#16001=CARTESIAN_POINT('Ctrl Pts',(-0.0939816891590436,-0.11752176362514,
0.0341956868724974));
#16002=CARTESIAN_POINT('Ctrl Pts',(0.0477663481097245,-0.142674779628989,
0.0421346765098031));
#16003=CARTESIAN_POINT('Ctrl Pts',(0.14578288888032,-0.0372469160898187,
0.0500736661471088));
#16004=CARTESIAN_POINT('Ctrl Pts',(0.110347650287512,0.102292747252513,
0.0580126557844146));
#16005=CARTESIAN_POINT('Ctrl Pts',(-0.0261045975097209,0.148182615303324,
0.0659516454217203));
#16006=CARTESIAN_POINT('Ctrl Pts',(-0.13865919166998,0.0584255608647477,
0.073890635059026));
#16007=CARTESIAN_POINT('Ctrl Pts',(-0.124281158904105,-0.0848182532198701,
0.0818296246963318));
#16008=CARTESIAN_POINT('Ctrl Pts',(0.00386794697500161,-0.15041563023346,
0.0897686143336374));
#16009=CARTESIAN_POINT('Ctrl Pts',(0.128476112576568,-0.0783184064825255,
0.0977076039709433));
#16010=CARTESIAN_POINT('Ctrl Pts',(0.135473254782295,0.0654742669580799,
0.105646593608249));
#16011=CARTESIAN_POINT('Ctrl Pts',(0.0184538891044151,0.149329569763132,
0.113585583245555));
#16012=CARTESIAN_POINT('Ctrl Pts',(-0.115458732720671,0.096483973363118,
0.12152457288286));
#16013=CARTESIAN_POINT('Ctrl Pts',(-0.143676805334049,-0.0446861343604874,
0.129463562520166));
#16014=CARTESIAN_POINT('Ctrl Pts',(-0.0403686054279526,-0.144949124289353,
0.137402552157472));
#16015=CARTESIAN_POINT('Ctrl Pts',(0.0998942839726139,-0.112521137758025,
0.145341541794778));
#16016=CARTESIAN_POINT('Ctrl Pts',(0.14871080372247,0.0229122455632766,
0.153280531432083));
#16017=CARTESIAN_POINT('Ctrl Pts',(0.0613927738894439,0.137371034794898,
0.161219521069389));
#16018=CARTESIAN_POINT('Ctrl Pts',(-0.0821261326059948,0.126076058196294,
0.169158510706695));
#16019=CARTESIAN_POINT('Ctrl Pts',(-0.150464193336327,-0.000632910110818063,
0.177097500344));
#16020=CARTESIAN_POINT('Ctrl Pts',(-0.0810625969653723,-0.126762492068094,
0.185036489981306));
#16021=CARTESIAN_POINT('Ctrl Pts',(0.0625462512992226,-0.136849700411639,
0.192975479618612));
#16022=CARTESIAN_POINT('Ctrl Pts',(0.148898293097928,-0.0216603868066741,
0.200914469255917));
#16023=CARTESIAN_POINT('Ctrl Pts',(0.0989441522193119,0.113357526360621,
0.208853458893223));
#16024=CARTESIAN_POINT('Ctrl Pts',(-0.0415865789238149,0.144604393083411,
0.216792448530529));
#16025=CARTESIAN_POINT('Ctrl Pts',(-0.144047647180085,0.0434758483035601,
0.224731438167835));
#16026=CARTESIAN_POINT('Ctrl Pts',(-0.114642966671137,-0.0974518559926297,
0.232670427805141));
#16027=CARTESIAN_POINT('Ctrl Pts',(0.0197094928286333,-0.149169064945282,
0.240609417442446));
#16028=CARTESIAN_POINT('Ctrl Pts',(0.136019262424063,-0.0643322181611298,
0.248548407079752));
#16029=CARTESIAN_POINT('Ctrl Pts',(0.127812719278849,0.0793963653730636,
0.256487396717058));
#16030=CARTESIAN_POINT('Ctrl Pts',(0.00260239121171357,0.150443017797356,
0.264426386354363));
#16031=CARTESIAN_POINT('Ctrl Pts',(-0.124990247656303,0.0837693979610897,
0.272365375991669));
#16032=CARTESIAN_POINT('Ctrl Pts',(-0.138162880936044,-0.0595893646165358,
0.280304365628975));
#16033=CARTESIAN_POINT('Ctrl Pts',(-0.0248568656394851,-0.148398147813718,
0.288243355266281));
#16034=CARTESIAN_POINT('Ctrl Pts',(0.111203906597776,-0.101358597076653,
0.296182344903586));
#16035=CARTESIAN_POINT('Ctrl Pts',(0.145465123646218,0.0384678027257296,
0.304121334540892));
#16036=CARTESIAN_POINT('Ctrl Pts',(0.0465629893725541,0.143079565503422,
0.312060324178198));
#16037=CARTESIAN_POINT('Ctrl Pts',(-0.0949643705016135,0.116711791945748,
0.319999313815503));
#16038=CARTESIAN_POINT('Ctrl Pts',(-0.149558357514911,-0.0164976283567656,
0.327938303452809));
#16039=CARTESIAN_POINT('Ctrl Pts',(-0.0672419181269484,-0.134604600554976,
0.335877293090115));
#16040=CARTESIAN_POINT('Ctrl Pts',(0.0766298889166206,-0.12949028600085,
0.343816282727421));
#16041=CARTESIAN_POINT('Ctrl Pts',(0.150352284446295,-0.00583648916182633,
0.351755272364726));
#16042=CARTESIAN_POINT('Ctrl Pts',(0.0864374678803939,0.123160213504125,
0.359694262002032));
#16043=CARTESIAN_POINT('Ctrl Pts',(-0.0566049265834532,0.139412181427728,
0.367633251639338));
#16044=CARTESIAN_POINT('Ctrl Pts',(-0.147829390149123,0.0280418517950267,
0.375572241276644));
#16045=CARTESIAN_POINT('Ctrl Pts',(-0.103726178443039,-0.108998871322406,
0.383511230913949));
#16046=CARTESIAN_POINT('Ctrl Pts',(0.0353312408083745,-0.146258597924691,
0.391450220551255));
#16047=CARTESIAN_POINT('Ctrl Pts',(0.142045330507792,-0.0496286018832686,
0.399389210188561));
#16048=CARTESIAN_POINT('Ctrl Pts',(0.118726655129599,0.0924329779120693,
0.407328199825866));
#16049=CARTESIAN_POINT('Ctrl Pts',(-0.0132781361506635,0.1498785012746,
0.415267189463172));
#16050=CARTESIAN_POINT('Ctrl Pts',(-0.133127703795094,0.0701205285647604,
0.423206179100478));
#16051=CARTESIAN_POINT('Ctrl Pts',(-0.131107982452518,-0.0738279823724454,
0.431145168737783));
#16052=CARTESIAN_POINT('Ctrl Pts',(-0.00906788859151817,-0.150192035209753,
0.439084158375089));
#16053=CARTESIAN_POINT('Ctrl Pts',(0.121273235812024,-0.0890655731449414,
0.447023148012395));
#16054=CARTESIAN_POINT('Ctrl Pts',(0.14059702422731,0.0535943170716914,
0.4549621376497));
#16055=CARTESIAN_POINT('Ctrl Pts',(0.031213872705855,0.14719228306762,0.462901127287006));
#16056=CARTESIAN_POINT('Ctrl Pts',(-0.106743440051405,0.106045801661112,
0.470840116924312));
#16057=CARTESIAN_POINT('Ctrl Pts',(-0.146984449047318,-0.0321783433727119,
0.478779106561618));
#16058=CARTESIAN_POINT('Ctrl Pts',(-0.0526712684425847,-0.140945420374714,
0.486718096198923));
#16059=CARTESIAN_POINT('Ctrl Pts',(0.0898588486235595,-0.120686624644175,
0.49465708583623));
#16060=CARTESIAN_POINT('Ctrl Pts',(0.150129348203927,0.0100525047535443,
0.502596075473534));
#16061=CARTESIAN_POINT('Ctrl Pts',(0.0729667185397875,0.131589254992538,
0.510535065110842));
#16062=CARTESIAN_POINT('Ctrl Pts',(-0.0709919412117167,0.132665060686482,
0.518474054748145));
#16063=CARTESIAN_POINT('Ctrl Pts',(-0.149962344179375,0.0122950954523496,
0.526413044385453));
#16064=CARTESIAN_POINT('Ctrl Pts',(-0.0916524986414713,-0.119330187030486,
0.534352034022757));
#16065=CARTESIAN_POINT('Ctrl Pts',(0.0505589280467443,-0.141716861518734,
0.542291023660064));
#16066=CARTESIAN_POINT('Ctrl Pts',(0.146487121137799,-0.0343714617774037,
0.550230013297369));
#16067=CARTESIAN_POINT('Ctrl Pts',(0.108316394245265,0.104438655591022,
0.558169002934674));
#16068=CARTESIAN_POINT('Ctrl Pts',(-0.0290105681715044,0.147642341414387,
0.566107992571982));
#16069=CARTESIAN_POINT('Ctrl Pts',(-0.139780343651344,0.0556895822633619,
0.574046982209285));
#16070=CARTESIAN_POINT('Ctrl Pts',(-0.122590794290966,-0.0872431727934394,
0.581985971846593));
#16071=CARTESIAN_POINT('Ctrl Pts',(0.00682222554696161,-0.150310782322966,
0.589924961483898));
#16072=CARTESIAN_POINT('Ctrl Pts',(0.129989965454297,-0.0757791721064987,
0.597863951121203));
#16073=CARTESIAN_POINT('Ctrl Pts',(0.134160800782372,0.0681230766876274,
0.60580294075851));
#16074=CARTESIAN_POINT('Ctrl Pts',(0.015516617634347,0.149663317553585,
0.613741930395814));
#16075=CARTESIAN_POINT('Ctrl Pts',(-0.117331965534667,0.0941970482962578,
0.621680920033121));
#16076=CARTESIAN_POINT('Ctrl Pts',(-0.142771175541451,-0.0475001629309618,
0.629619909670426));
#16077=CARTESIAN_POINT('Ctrl Pts',(-0.0375131590877193,-0.145714230393655,
0.637558899307733));
#16078=CARTESIAN_POINT('Ctrl Pts',(0.102085583566124,-0.110536906379362,
0.645497888945037));
#16079=CARTESIAN_POINT('Ctrl Pts',(0.148231970847143,0.0258293798362968,
0.653436878582344));
#16080=CARTESIAN_POINT('Ctrl Pts',(0.0586821478180281,0.138550639014834,
0.661375868219649));
#16081=CARTESIAN_POINT('Ctrl Pts',(-0.0845871597882484,0.124438283670714,
0.669314857856955));
#16082=CARTESIAN_POINT('Ctrl Pts',(-0.150422719745043,-0.00358879206139753,
0.67725384749426));
#16083=CARTESIAN_POINT('Ctrl Pts',(-0.078556588917505,-0.128330574617282,
0.685192837131567));
#16084=CARTESIAN_POINT('Ctrl Pts',(0.065222715229363,-0.135594511179713,
0.693131826768872));
#16085=CARTESIAN_POINT('Ctrl Pts',(0.149295093588351,-0.0187309656558678,
0.701070816406178));
#16086=CARTESIAN_POINT('Ctrl Pts',(0.0966980456281902,0.11527949520901,
0.709009806043483));
#16087=CARTESIAN_POINT('Ctrl Pts',(-0.044419435954706,0.14375947882982,
0.716948795680789));
#16088=CARTESIAN_POINT('Ctrl Pts',(-0.144873968183829,0.0406375120624596,
0.724887785318095));
#16089=CARTESIAN_POINT('Ctrl Pts',(-0.112706311402131,-0.099685311927494,
0.732826774955401));
#16090=CARTESIAN_POINT('Ctrl Pts',(0.0226362492002416,-0.148753064728429,
0.740765764592706));
#16091=CARTESIAN_POINT('Ctrl Pts',(0.137256875023267,-0.0616475814838108,
0.748704754230013));
#16092=CARTESIAN_POINT('Ctrl Pts',(0.126228238590478,0.0818920376245527,
0.756643743867318));
#16093=CARTESIAN_POINT('Ctrl Pts',(-0.000353699285724532,0.150465108715513,
0.764582733504624));
#16094=CARTESIAN_POINT('Ctrl Pts',(-0.126611849706441,0.0812976848247803,
0.772521723141928));
#16095=CARTESIAN_POINT('Ctrl Pts',(-0.136965528997667,-0.0622921978288208,
0.780460712779236));
#16096=CARTESIAN_POINT('Ctrl Pts',(-0.0219366533522686,-0.148857842533265,
0.788399702416541));
#16097=CARTESIAN_POINT('Ctrl Pts',(0.113173725020093,-0.0991543342927188,
0.796338692053846));
#16098=CARTESIAN_POINT('Ctrl Pts',(0.144681314438483,0.0413181715024817,
0.804277681691154));
#16099=CARTESIAN_POINT('Ctrl Pts',(0.0437430761464933,0.143966723006387,
0.812216671328456));
#16100=CARTESIAN_POINT('Ctrl Pts',(-0.0972389504488157,0.114823606281847,
0.820155660965765));
#16101=CARTESIAN_POINT('Ctrl Pts',(-0.149205382128735,-0.0194326526180533,
0.828094650603069));
#16102=CARTESIAN_POINT('Ctrl Pts',(-0.0645845121824554,-0.135899649852787,
0.836033640240376));
#16103=CARTESIAN_POINT('Ctrl Pts',(0.0791590524011713,-0.127959831458565,
0.843972629877681));
#16104=CARTESIAN_POINT('Ctrl Pts',(0.150437929635691,-0.00288155702400619,
0.851911619514986));
#16105=CARTESIAN_POINT('Ctrl Pts',(0.0840011924733913,0.12483458538003,
0.859850609152293));
#16106=CARTESIAN_POINT('Ctrl Pts',(-0.0593328794206009,0.138273220341526,
0.867789598789597));
#16107=CARTESIAN_POINT('Ctrl Pts',(-0.148351766552825,0.0251321985630355,
0.875728588426904));
#16108=CARTESIAN_POINT('Ctrl Pts',(-0.1015647786165,-0.111015628577859,
0.883667578064211));
#16109=CARTESIAN_POINT('Ctrl Pts',(0.0381978034543637,-0.145536256153639,
0.891606567701514));
#16110=CARTESIAN_POINT('Ctrl Pts',(0.142992914329196,-0.046828415471795,
0.899545557338823));
#16111=CARTESIAN_POINT('Ctrl Pts',(0.116887812080083,0.0947476302135675,
0.907484546976125));
#16112=CARTESIAN_POINT('Ctrl Pts',(-0.0162200712834111,0.149588713917584,
0.915423536613434));
#16113=CARTESIAN_POINT('Ctrl Pts',(-0.134479591021026,0.067491582014154,
0.923362526250738));
#16114=CARTESIAN_POINT('Ctrl Pts',(-0.129632261667175,-0.0763894677230377,
0.931301515888044));
#16115=CARTESIAN_POINT('Ctrl Pts',(-0.00611548103612966,-0.150341195071919,
0.93924050552535));
#16116=CARTESIAN_POINT('Ctrl Pts',(0.122999603362204,-0.0866658618874593,
0.947179495162656));
#16117=CARTESIAN_POINT('Ctrl Pts',(0.139516980595786,0.0563461282555487,
0.95511848479996));
#16118=CARTESIAN_POINT('Ctrl Pts',(0.0283161238170646,0.147777099632969,
0.963057474437267));
#16119=CARTESIAN_POINT('Ctrl Pts',(-0.108806203685475,0.103928264122473,
0.970996464074573));
#16120=CARTESIAN_POINT('Ctrl Pts',(-0.146323908690103,-0.0350597745230392,
0.978935453711877));
#16121=CARTESIAN_POINT('Ctrl Pts',(-0.049892103521326,-0.14195299239598,
0.986874443349185));
#16122=CARTESIAN_POINT('Ctrl Pts',(0.0922125030920605,-0.118897974404329,
0.994813432986488));
#16123=CARTESIAN_POINT('Ctrl Pts',(0.149902882860231,0.0129999905441286,
1.0027524226238));
#16124=CARTESIAN_POINT('Ctrl Pts',(0.0703674468853664,0.132997355096976,
1.0106914122611));
#16125=CARTESIAN_POINT('Ctrl Pts',(-0.0735845641169637,0.131244755962562,
1.01863040189841));
#16126=CARTESIAN_POINT('Ctrl Pts',(-0.150174949749745,0.00934657753497952,
1.02656939153571));
#16127=CARTESIAN_POINT('Ctrl Pts',(-0.0892904610481016,-0.121107752063083,
1.03450838117302));
#16128=CARTESIAN_POINT('Ctrl Pts',(0.0533333252681307,-0.140696234703703,
1.04244737081032));
#16129=CARTESIAN_POINT('Ctrl Pts',(0.147134107472884,-0.031486957015783,
1.05038636044763));
#16130=CARTESIAN_POINT('Ctrl Pts',(0.106243698045146,0.106546471877992,
1.05832535008494));
#16131=CARTESIAN_POINT('Ctrl Pts',(-0.0319055355867657,0.147043907874068,
1.06626433972224));
#16132=CARTESIAN_POINT('Ctrl Pts',(-0.14084743801815,0.0529327237885883,
1.07420332935955));
#16133=CARTESIAN_POINT('Ctrl Pts',(-0.120853163849259,-0.0896347412088629,
1.08214231899685));
#16134=CARTESIAN_POINT('Ctrl Pts',(0.00977389921538986,-0.150147743699608,
1.09008130863416));
#16135=CARTESIAN_POINT('Ctrl Pts',(0.13145362739741,-0.0732107771302755,
1.09802029827146));
#16136=CARTESIAN_POINT('Ctrl Pts',(0.132796568802552,0.0707456384395876,
1.10595928790877));
#16137=CARTESIAN_POINT('Ctrl Pts',(0.0125733526121963,0.149939270533256,
1.11389827754607));
#16138=CARTESIAN_POINT('Ctrl Pts',(-0.119159906186493,0.0918737764630459,
1.12183726718338));
#16139=CARTESIAN_POINT('Ctrl Pts',(-0.141810437433163,-0.0502958634379693,
1.12977625682069));
#16140=CARTESIAN_POINT('Ctrl Pts',(-0.0346432321137694,-0.146423087362162,
1.13771524645799));
#16141=CARTESIAN_POINT('Ctrl Pts',(0.104237477950025,-0.108510009835838,
1.1456542360953));
#16142=CARTESIAN_POINT('Ctrl Pts',(0.147695920811486,0.0287365450185451,
1.1535932257326));
#16143=CARTESIAN_POINT('Ctrl Pts',(0.0559488704325515,0.139676762352502,
1.16153221536991));
#16144=CARTESIAN_POINT('Ctrl Pts',(-0.0870155364008756,0.12275247642644,
1.16947120500722));
#16145=CARTESIAN_POINT('Ctrl Pts',(-0.150323183223479,-0.00654328889139735,
1.17741019464452));
#16146=CARTESIAN_POINT('Ctrl Pts',(-0.0760202581255566,-0.129849121670035,
1.18534918428183));
#16147=CARTESIAN_POINT('Ctrl Pts',(0.0678740032777675,-0.134286982701248,
1.19328817391913));
#16148=CARTESIAN_POINT('Ctrl Pts',(0.149634266389533,-0.0157943143574443,
1.20122716355644));
#16149=CARTESIAN_POINT('Ctrl Pts',(0.0944146137277022,0.117156966325547,
1.20916615319374));
#16150=CARTESIAN_POINT('Ctrl Pts',(-0.047235147145783,0.142859073628774,
1.21710514283105));
#16151=CARTESIAN_POINT('Ctrl Pts',(-0.145644368043342,0.037783489796601,
1.22504413246835));
#16152=CARTESIAN_POINT('Ctrl Pts',(-0.11072615165767,-0.101880289472715,
1.23298312210566));
#16153=CARTESIAN_POINT('Ctrl Pts',(0.0255542680118797,-0.148279646041953,
1.24092211174296));
#16154=CARTESIAN_POINT('Ctrl Pts',(0.138441506664824,-0.0589391489276913,
1.24886110138027));
#16155=CARTESIAN_POINT('Ctrl Pts',(0.124595033982396,0.0843560996663564,
1.25680009101758));
#16156=CARTESIAN_POINT('Ctrl Pts',(-0.00330965325590636,0.150429120316621,
1.26473908065488));
#16157=CARTESIAN_POINT('Ctrl Pts',(-0.128184579763139,0.0787945908985174,
1.27267807029219));
#16158=CARTESIAN_POINT('Ctrl Pts',(-0.135715308561414,-0.0649709863423027,
1.2806170599295));
#16159=CARTESIAN_POINT('Ctrl Pts',(-0.0190079735469551,-0.149260078337129,
1.2885560495668));
#16160=CARTESIAN_POINT('Ctrl Pts',(0.115099858543875,-0.0969117980795561,
1.29649503920411));
#16161=CARTESIAN_POINT('Ctrl Pts',(0.143841658454547,0.0441525915281748,
1.30443402884141));
#16162=CARTESIAN_POINT('Ctrl Pts',(0.0409062781470196,0.144798309552134,
1.31237301847872));
#16163=CARTESIAN_POINT('Ctrl Pts',(-0.0994759962839106,0.112891098884786,
1.32031200811602));
#16164=CARTESIAN_POINT('Ctrl Pts',(-0.148794813708878,-0.0223601759313527,
1.32825099775333));
#16165=CARTESIAN_POINT('Ctrl Pts',(-0.0619021766503053,-0.13714224202644,
1.33618998739064));
#16166=CARTESIAN_POINT('Ctrl Pts',(0.0816576604940555,-0.126379984705639,
1.34412897702794));
#16167=CARTESIAN_POINT('Ctrl Pts',(0.150465506209006,7.4487583413377E-5,
1.35206796666525));
#16168=CARTESIAN_POINT('Ctrl Pts',(0.0815324923277053,0.126460770918471,
1.36000695630255));
#16169=CARTESIAN_POINT('Ctrl Pts',(-0.062037929094705,0.137080886684378,
1.36794594593986));
#16170=CARTESIAN_POINT('Ctrl Pts',(-0.148816880822527,0.0222128430196456,
1.37588493557716));
#16171=CARTESIAN_POINT('Ctrl Pts',(-0.0993641722043223,-0.112989531455785,
1.38382392521447));
#16172=CARTESIAN_POINT('Ctrl Pts',(0.0410496166270677,-0.144757742348562,
1.39176291485178));
#16173=CARTESIAN_POINT('Ctrl Pts',(0.143885312916173,-0.0440101443352923,
1.39970190448908));
#16174=CARTESIAN_POINT('Ctrl Pts',(0.115003831846793,0.0970256929337524,
1.40764089412639));
#16175=CARTESIAN_POINT('Ctrl Pts',(-0.0191557100743377,0.149241218055048,
1.41557988376369));
#16176=CARTESIAN_POINT('Ctrl Pts',(-0.135779636557791,0.0648365220611291,
1.423518873401));
#16177=CARTESIAN_POINT('Ctrl Pts',(-0.128106375355825,-0.0789213496179777,
1.4314578630383));
#16178=CARTESIAN_POINT('Ctrl Pts',(-0.00316095527563228,-0.150432546011701,
1.43939685267561));
#16179=CARTESIAN_POINT('Ctrl Pts',(0.12467895337041,-0.0842322751882648,
1.44733584231291));
#16180=CARTESIAN_POINT('Ctrl Pts',(0.138382210043398,0.0590753877074232,
1.45527483195022));
#16181=CARTESIAN_POINT('Ctrl Pts',(0.0254091034322018,0.148306397458819,
1.46321382158753));
#16182=CARTESIAN_POINT('Ctrl Pts',(-0.110830116988615,0.101767718932792,
1.47115281122483));
#16183=CARTESIAN_POINT('Ctrl Pts',(-0.145600909330124,-0.0379221829034233,
1.47909180086214));
#16184=CARTESIAN_POINT('Ctrl Pts',(-0.0471050325108872,-0.142916194795756,
1.48703079049945));
#16185=CARTESIAN_POINT('Ctrl Pts',(0.0945521370959566,-0.117043625665234,
1.49496978013675));
#16186=CARTESIAN_POINT('Ctrl Pts',(0.14957741911039,0.0159047428854941,
1.50290876977406));
#16187=CARTESIAN_POINT('Ctrl Pts',(0.0678206238522695,0.134426714629862,
1.51084775941136));
#16188=CARTESIAN_POINT('Ctrl Pts',(-0.0763126473618499,0.129627546381738,
1.51878674904867));
#16189=CARTESIAN_POINT('Ctrl Pts',(-0.125385920115907,0.0477050348167321,
1.52407940880687));
#16190=CARTESIAN_POINT('Ctrl Pts',(-0.127184992207234,0.00540996832206346,
1.52672573868597));
#16191=CARTESIAN_POINT('Ctrl Pts',(0.0684664424539414,-0.095829519891843,
-1.38777878078145E-17));
#16192=CARTESIAN_POINT('Ctrl Pts',(0.100334321247169,-0.0730611673843044,
0.00264632987910189));
#16193=CARTESIAN_POINT('Ctrl Pts',(0.139021564822767,0.00636891437108143,
0.00793898963730573));
#16194=CARTESIAN_POINT('Ctrl Pts',(0.0699018669780613,0.120491966796142,
0.0158779792746114));
#16195=CARTESIAN_POINT('Ctrl Pts',(-0.0632645460347191,0.123954346655885,
0.0238169689119172));
#16196=CARTESIAN_POINT('Ctrl Pts',(-0.138486976988987,0.0141253725679007,
0.0317559585492228));
#16197=CARTESIAN_POINT('Ctrl Pts',(-0.0869496735326521,-0.108728403071097,
0.0396949481865287));
#16198=CARTESIAN_POINT('Ctrl Pts',(0.0441923146003338,-0.131999388615902,
0.0476339378238343));
#16199=CARTESIAN_POINT('Ctrl Pts',(0.134874939024977,-0.034459980695041,
0.0555729274611401));
#16200=CARTESIAN_POINT('Ctrl Pts',(0.102091080224759,0.094638871230671,
0.0635119170984456));
#16201=CARTESIAN_POINT('Ctrl Pts',(-0.0241513666277066,0.137095110112719,
0.0714509067357516));
#16202=CARTESIAN_POINT('Ctrl Pts',(-0.128284260007319,0.0540539703915629,
0.0793898963730571));
#16203=CARTESIAN_POINT('Ctrl Pts',(-0.114982038412656,-0.0784718756714057,
0.0873288860103631));
#16204=CARTESIAN_POINT('Ctrl Pts',(0.00357853460314598,-0.139161043603659,
0.0952678756476685));
#16205=CARTESIAN_POINT('Ctrl Pts',(0.118863112008681,-0.0724583686054966,
0.103206865284975));
#16206=CARTESIAN_POINT('Ctrl Pts',(0.125336705278751,0.0605752693714656,
0.11114585492228));
#16207=CARTESIAN_POINT('Ctrl Pts',(0.0170731091066207,0.138156245709763,
0.119084844559586));
#16208=CARTESIAN_POINT('Ctrl Pts',(-0.106819734848208,0.0892647286947484,
0.127023834196891));
#16209=CARTESIAN_POINT('Ctrl Pts',(-0.132926439498961,-0.0413425724611633,
0.134962823834197));
#16210=CARTESIAN_POINT('Ctrl Pts',(-0.0373480950846616,-0.134103559412242,
0.142901813471503));
#16211=CARTESIAN_POINT('Ctrl Pts',(0.0924198687735613,-0.104101940294199,
0.150840803108809));
#16212=CARTESIAN_POINT('Ctrl Pts',(0.137583777756591,0.0211978768359354,
0.158779792746114));
#16213=CARTESIAN_POINT('Ctrl Pts',(0.0567991668878991,0.127092487218924,
0.16671878238342));
#16214=CARTESIAN_POINT('Ctrl Pts',(-0.075981188277068,0.116642637502503,
0.174657772020726));
#16215=CARTESIAN_POINT('Ctrl Pts',(-0.139205973057234,-0.000585553717998882,
0.182596761658032));
#16216=CARTESIAN_POINT('Ctrl Pts',(-0.0749972298318695,-0.11727771015962,
0.190535751295337));
#16217=CARTESIAN_POINT('Ctrl Pts',(0.0578663373665801,-0.126610160769685,
0.198474740932643));
#16218=CARTESIAN_POINT('Ctrl Pts',(0.13775723856723,-0.0200396862227523,
0.206413730569949));
#16219=CARTESIAN_POINT('Ctrl Pts',(0.091540828968026,0.104875747581476,
0.214352720207254));
#16220=CARTESIAN_POINT('Ctrl Pts',(-0.0384749358425138,0.133784622116252,
0.22229170984456));
#16221=CARTESIAN_POINT('Ctrl Pts',(-0.133269533752038,0.0402228439430644,
0.230230699481866));
#16222=CARTESIAN_POINT('Ctrl Pts',(-0.106065007067505,-0.0901601911982067,
0.238169689119172));
#16223=CARTESIAN_POINT('Ctrl Pts',(0.0182347644767634,-0.138007750384372,
0.246108678756477));
#16224=CARTESIAN_POINT('Ctrl Pts',(0.125841858853055,-0.0595186723796334,
0.254047668393783));
#16225=CARTESIAN_POINT('Ctrl Pts',(0.118249355954961,0.073455671106145,
0.261986658031089));
#16226=CARTESIAN_POINT('Ctrl Pts',(0.00240767183786234,0.139186381940956,
0.269925647668394));
#16227=CARTESIAN_POINT('Ctrl Pts',(-0.115638070838342,0.0775014991741366,
0.277864637305701));
#16228=CARTESIAN_POINT('Ctrl Pts',(-0.12782508485658,-0.0551306945617612,
0.285803626943006));
#16229=CARTESIAN_POINT('Ctrl Pts',(-0.0229969941138309,-0.137294515779738,
0.293742616580312));
#16230=CARTESIAN_POINT('Ctrl Pts',(0.102883268653204,-0.0937746172089793,
0.301681606217617));
#16231=CARTESIAN_POINT('Ctrl Pts',(0.134580950019115,0.0355895166223291,
0.309620595854923));
#16232=CARTESIAN_POINT('Ctrl Pts',(0.0430789950773988,0.13237388709478,
0.317559585492229));
#16233=CARTESIAN_POINT('Ctrl Pts',(-0.0878588274613298,0.107979036106918,
0.325498575129534));
#16234=CARTESIAN_POINT('Ctrl Pts',(-0.1383679148179,-0.0152632221501787,
0.33343756476684));
#16235=CARTESIAN_POINT('Ctrl Pts',(-0.0622106591311991,-0.12453304658572,
0.341376554404146));
#16236=CARTESIAN_POINT('Ctrl Pts',(0.0708961914151981,-0.119801401679107,
0.349315544041452));
#16237=CARTESIAN_POINT('Ctrl Pts',(0.1391024375543,-0.00539978406154301,
0.357254533678757));
#16238=CARTESIAN_POINT('Ctrl Pts',(0.0799699354250877,0.113944965792994,
0.365193523316063));
#16239=CARTESIAN_POINT('Ctrl Pts',(-0.0523695618881846,0.128980908622551,
0.373132512953369));
#16240=CARTESIAN_POINT('Ctrl Pts',(-0.136768314413298,0.0259436692471295,
0.381071502590675));
#16241=CARTESIAN_POINT('Ctrl Pts',(-0.0959650484377783,-0.100843221288265,
0.38901049222798));
#16242=CARTESIAN_POINT('Ctrl Pts',(0.0326876424682324,-0.135315053971568,
0.396949481865287));
#16243=CARTESIAN_POINT('Ctrl Pts',(0.13141703692502,-0.0459152284901983,
0.404888471502591));
#16244=CARTESIAN_POINT('Ctrl Pts',(0.109843140674695,0.0855168418978295,
0.412827461139898));
#16245=CARTESIAN_POINT('Ctrl Pts',(-0.0122846228212416,0.13866410438033,
0.420766450777203));
#16246=CARTESIAN_POINT('Ctrl Pts',(-0.123166656044517,0.0648738825743514,
0.428705440414509));
#16247=CARTESIAN_POINT('Ctrl Pts',(-0.121298056821252,-0.0683039326309071,
0.436644430051815));
#16248=CARTESIAN_POINT('Ctrl Pts',(-0.00838939967687663,-0.138954178686792,
0.44458341968912));
#16249=CARTESIAN_POINT('Ctrl Pts',(0.11219917790857,-0.0824013973067221,
0.452522409326426));
#16250=CARTESIAN_POINT('Ctrl Pts',(0.13007709763057,0.0495842159710775,
0.460461398963732));
#16251=CARTESIAN_POINT('Ctrl Pts',(0.0288783492374893,0.136178877755608,
0.468400388601037));
#16252=CARTESIAN_POINT('Ctrl Pts',(-0.0987565487199846,0.0981111099028881,
0.476339378238344));
#16253=CARTESIAN_POINT('Ctrl Pts',(-0.135986594552616,-0.0297706550724338,
0.484278367875649));
#16254=CARTESIAN_POINT('Ctrl Pts',(-0.0487302328423073,-0.130399425645183,
0.492217357512954));
#16255=CARTESIAN_POINT('Ctrl Pts',(0.0831353173341669,-0.111656458896056,
0.50015634715026));
#16256=CARTESIAN_POINT('Ctrl Pts',(0.13889618212661,0.00930034365552528,
0.508095336787567));
#16257=CARTESIAN_POINT('Ctrl Pts',(0.0675071113591811,0.12174331898465,
0.516034326424871));
#16258=CARTESIAN_POINT('Ctrl Pts',(-0.0656800932930844,0.122738629397884,
0.523973316062178));
#16259=CARTESIAN_POINT('Ctrl Pts',(-0.138741673886299,0.0113751364249866,
0.531912305699483));
#16260=CARTESIAN_POINT('Ctrl Pts',(-0.0847947606245053,-0.110401514355972,
0.539851295336789));
#16261=CARTESIAN_POINT('Ctrl Pts',(0.0467759446245483,-0.131113145053959,
0.547790284974095));
#16262=CARTESIAN_POINT('Ctrl Pts',(0.135526478334676,-0.031799677225719,
0.555729274611401));
#16263=CARTESIAN_POINT('Ctrl Pts',(0.100211809365564,0.0966242157284558,
0.563668264248707));
#16264=CARTESIAN_POINT('Ctrl Pts',(-0.0268399031138932,0.136595261273209,
0.571607253886012));
#16265=CARTESIAN_POINT('Ctrl Pts',(-0.129321523751272,0.0515227066069736,
0.579546243523318));
#16266=CARTESIAN_POINT('Ctrl Pts',(-0.113418152377209,-0.0807153548762533,
0.587485233160623));
#16267=CARTESIAN_POINT('Ctrl Pts',(0.00631176444456456,-0.139064040754811,
0.595424222797929));
#16268=CARTESIAN_POINT('Ctrl Pts',(0.120263693490807,-0.0701091280034811,
0.603363212435234));
#16269=CARTESIAN_POINT('Ctrl Pts',(0.124122453355413,0.0630258865426945,
0.611302202072541));
#16270=CARTESIAN_POINT('Ctrl Pts',(0.0143556138404206,0.138465021405133,
0.619241191709845));
#16271=CARTESIAN_POINT('Ctrl Pts',(-0.108552806291007,0.0871489187988374,
0.627180181347153));
#16272=CARTESIAN_POINT('Ctrl Pts',(-0.132088571872698,-0.043946046262323,
0.635119170984457));
#16273=CARTESIAN_POINT('Ctrl Pts',(-0.0347063025259737,-0.134811417789573,
0.643058160621763));
#16274=CARTESIAN_POINT('Ctrl Pts',(0.0944472082050275,-0.102266175560326,
0.65099715025907));
#16275=CARTESIAN_POINT('Ctrl Pts',(0.137140772714236,0.0238967416356601,
0.658936139896373));
#16276=CARTESIAN_POINT('Ctrl Pts',(0.054291358674537,0.128183829614862,
0.666875129533682));
#16277=CARTESIAN_POINT('Ctrl Pts',(-0.0782580734018908,0.115127406593233,
0.674814119170985));
#16278=CARTESIAN_POINT('Ctrl Pts',(-0.139167602654929,-0.00332026696803425,
0.682753108808293));
#16279=CARTESIAN_POINT('Ctrl Pts',(-0.0726787294560835,-0.118728463672822,
0.690692098445597));
#16280=CARTESIAN_POINT('Ctrl Pts',(0.0603425395611779,-0.125448888878168,
0.698631088082904));
#16281=CARTESIAN_POINT('Ctrl Pts',(0.138124349154501,-0.0173294538893964,
0.706570077720209));
#16282=CARTESIAN_POINT('Ctrl Pts',(0.0894627833767505,0.106653908470079,
0.714509067357515));
#16283=CARTESIAN_POINT('Ctrl Pts',(-0.0410958292974484,0.133002927094911,
0.72244805699482));
#16284=CARTESIAN_POINT('Ctrl Pts',(-0.134034026730954,0.0375968812502473,
0.730387046632127));
#16285=CARTESIAN_POINT('Ctrl Pts',(-0.104273258644039,-0.0922265326964679,
0.738326036269432));
#16286=CARTESIAN_POINT('Ctrl Pts',(0.0209425314183671,-0.137622876656644,
0.746265025906738));
#16287=CARTESIAN_POINT('Ctrl Pts',(0.126986869252672,-0.0570349089493802,
0.754204015544043));
#16288=CARTESIAN_POINT('Ctrl Pts',(0.11678343126468,0.0757646090434518,
0.762143005181349));
#16289=CARTESIAN_POINT('Ctrl Pts',(-0.000327234354877375,0.139206819944772,
0.770081994818654));
#16290=CARTESIAN_POINT('Ctrl Pts',(-0.117138339349379,0.0752147276530931,
0.778020984455961));
#16291=CARTESIAN_POINT('Ctrl Pts',(-0.126717322684213,-0.0576312930030564,
0.785959974093266));
#16292=CARTESIAN_POINT('Ctrl Pts',(-0.0202952816069424,-0.137719814645367,
0.793898963730571));
#16293=CARTESIAN_POINT('Ctrl Pts',(0.104705698854998,-0.0917352845351548,
0.801837953367879));
#16294=CARTESIAN_POINT('Ctrl Pts',(0.133855787965376,0.0382266115373486,
0.809776943005182));
#16295=CARTESIAN_POINT('Ctrl Pts',(0.0404700769297216,0.133194664588195,
0.81771593264249));
#16296=CARTESIAN_POINT('Ctrl Pts',(-0.0899632159395838,0.106232130635072,
0.825654922279794));
#16297=CARTESIAN_POINT('Ctrl Pts',(-0.13804135019805,-0.0179786383510676,
0.833593911917101));
#16298=CARTESIAN_POINT('Ctrl Pts',(-0.059752088941783,-0.125731196083361,
0.841532901554406));
#16299=CARTESIAN_POINT('Ctrl Pts',(0.0732361146625898,-0.118385460722959,
0.849471891191712));
#16300=CARTESIAN_POINT('Ctrl Pts',(0.139181674492094,-0.00266594955618734,
0.857410880829018));
#16301=CARTESIAN_POINT('Ctrl Pts',(0.077715950067195,0.115494055719818,
0.865349870466323));
#16302=CARTESIAN_POINT('Ctrl Pts',(-0.0548934004223171,0.127927168308903,
0.87328886010363));
#16303=CARTESIAN_POINT('Ctrl Pts',(-0.137251604915624,0.0232517257326144,
0.881227849740934));
#16304=CARTESIAN_POINT('Ctrl Pts',(-0.0939653715754795,-0.102709078207047,
0.889166839378241));
#16305=CARTESIAN_POINT('Ctrl Pts',(0.0353397195745277,-0.134646760160997,
0.897105829015547));
#16306=CARTESIAN_POINT('Ctrl Pts',(0.132293719443212,-0.0433245611326863,
0.905044818652852));
#16307=CARTESIAN_POINT('Ctrl Pts',(0.108141885842356,0.0876583043865096,
0.912983808290157));
#16308=CARTESIAN_POINT('Ctrl Pts',(-0.0150064327997127,0.138395999855801,
0.920922797927463));
#16309=CARTESIAN_POINT('Ctrl Pts',(-0.124417390671652,0.0624416423544169,
0.928861787564769));
#16310=CARTESIAN_POINT('Ctrl Pts',(-0.119932754264349,-0.0706737593172073,
0.936800777202075));
#16311=CARTESIAN_POINT('Ctrl Pts',(-0.00565790085648466,-0.139092177922979,
0.944739766839381));
#16312=CARTESIAN_POINT('Ctrl Pts',(0.113796373024222,-0.0801812402497705,
0.952678756476687));
#16313=CARTESIAN_POINT('Ctrl Pts',(0.129077866376032,0.0521301276928276,
0.960617746113992));
#16314=CARTESIAN_POINT('Ctrl Pts',(0.026197419344502,0.13671993644362,0.968556735751298));
#16315=CARTESIAN_POINT('Ctrl Pts',(-0.100664969670515,0.0961520134094621,
0.976495725388603));
#16316=CARTESIAN_POINT('Ctrl Pts',(-0.13537547797311,-0.0324364881732178,
0.98443471502591));
#16317=CARTESIAN_POINT('Ctrl Pts',(-0.0461590140787468,-0.131331607851033,
0.992373704663214));
#16318=CARTESIAN_POINT('Ctrl Pts',(0.0853128637208732,-0.110001641284132,
1.00031269430052));
#16319=CARTESIAN_POINT('Ctrl Pts',(0.138686661656432,0.0120272889735618,
1.00825168393783));
#16320=CARTESIAN_POINT('Ctrl Pts',(0.0651023256631918,0.123046060459907,
1.01619067357513));
#16321=CARTESIAN_POINT('Ctrl Pts',(-0.0680787277209358,0.121424596492465,
1.02412966321244));
#16322=CARTESIAN_POINT('Ctrl Pts',(-0.138938371616466,0.00864723620724691,
1.03206865284975));
#16323=CARTESIAN_POINT('Ctrl Pts',(-0.0826094583655966,-0.112046076191904,
1.04000764248705));
#16324=CARTESIAN_POINT('Ctrl Pts',(0.0493427524230464,-0.130168884856471,
1.04794663212436));
#16325=CARTESIAN_POINT('Ctrl Pts',(0.136125055048066,-0.0291310004912345,
1.05588562176166));
#16326=CARTESIAN_POINT('Ctrl Pts',(0.0982941990358779,0.0985743183458784,
1.06382461139897));
#16327=CARTESIAN_POINT('Ctrl Pts',(-0.0295182596522469,0.136041604476578,
1.07176360103627));
#16328=CARTESIAN_POINT('Ctrl Pts',(-0.130308774647192,0.0489721252490281,
1.07970259067358));
#16329=CARTESIAN_POINT('Ctrl Pts',(-0.111810537096203,-0.0829279783650712,
1.08764158031088));
#16330=CARTESIAN_POINT('Ctrl Pts',(0.00904258428980543,-0.13891320121148,
1.09558056994819));
#16331=CARTESIAN_POINT('Ctrl Pts',(0.121617839487272,-0.067732908692211,
1.1035195595855));
#16332=CARTESIAN_POINT('Ctrl Pts',(0.122860297649024,0.0654522196953821,
1.1114585492228));
#16333=CARTESIAN_POINT('Ctrl Pts',(0.0116325734791967,0.138720326685422,
1.11939753886011));
#16334=CARTESIAN_POINT('Ctrl Pts',(-0.110243974478508,0.0849994817198388,
1.12733652849741));
#16335=CARTESIAN_POINT('Ctrl Pts',(-0.131199719314147,-0.0465325633653302,
1.13527551813472));
#16336=CARTESIAN_POINT('Ctrl Pts',(-0.0320511128216771,-0.13546723577438,
1.14321450777202));
#16337=CARTESIAN_POINT('Ctrl Pts',(0.0964380908528195,-0.100390938007982,
1.15115349740933));
#16338=CARTESIAN_POINT('Ctrl Pts',(0.136644831685568,0.0265863832644056,
1.15909248704664));
#16339=CARTESIAN_POINT('Ctrl Pts',(0.0517625939920979,0.129225692742072,
1.16703147668394));
#16340=CARTESIAN_POINT('Ctrl Pts',(-0.0805047509788913,0.113567736929491,
1.17497046632125));
#16341=CARTESIAN_POINT('Ctrl Pts',(-0.139075513779617,-0.00605369873671642,
1.18290945595855));
#16342=CARTESIAN_POINT('Ctrl Pts',(-0.0703321751825429,-0.12013338809653,
1.19084844559586));
#16343=CARTESIAN_POINT('Ctrl Pts',(0.0627954496153871,-0.124239193932754,
1.19878743523316));
#16344=CARTESIAN_POINT('Ctrl Pts',(0.138438143943654,-0.0146125323915816,
1.20672642487047));
#16345=CARTESIAN_POINT('Ctrl Pts',(0.0873502052771435,0.108390901091839,
1.21466541450777));
#16346=CARTESIAN_POINT('Ctrl Pts',(-0.043700859820065,0.132169893139269,
1.22260440414508));
#16347=CARTESIAN_POINT('Ctrl Pts',(-0.134746782767514,0.0349564062120582,
1.23054339378239));
#16348=CARTESIAN_POINT('Ctrl Pts',(-0.102441260891455,-0.0942572748833364,
1.23848238341969));
#16349=CARTESIAN_POINT('Ctrl Pts',(0.0236422145726536,-0.137184880695923,
1.246421373057));
#16350=CARTESIAN_POINT('Ctrl Pts',(0.128082862902196,-0.0545291301253663,
1.2543603626943));
#16351=CARTESIAN_POINT('Ctrl Pts',(0.115272428336817,0.0780443019497631,
1.26229935233161));
#16352=CARTESIAN_POINT('Ctrl Pts',(-0.00306201423577413,0.139173524314926,
1.27023834196891));
#16353=CARTESIAN_POINT('Ctrl Pts',(-0.118593392628464,0.0728989233548558,
1.27817733160622));
#16354=CARTESIAN_POINT('Ctrl Pts',(-0.125560647806918,-0.06010964584811,
1.28611632124353));
#16355=CARTESIAN_POINT('Ctrl Pts',(-0.0175857351491984,-0.138091953858251,
1.29405531088083));
#16356=CARTESIAN_POINT('Ctrl Pts',(0.106487712804436,-0.089660542174548,
1.30199430051814));
#16357=CARTESIAN_POINT('Ctrl Pts',(0.133078957772855,0.0408489510387311,
1.30993329015544));
#16358=CARTESIAN_POINT('Ctrl Pts',(0.0378455373822902,0.133964029124136,
1.31787227979275));
#16359=CARTESIAN_POINT('Ctrl Pts',(-0.0920328787300654,0.104444219726284,
1.32581126943006));
#16360=CARTESIAN_POINT('Ctrl Pts',(-0.137661501842601,-0.0206871148492911,
1.33375025906736));
#16361=CARTESIAN_POINT('Ctrl Pts',(-0.0572704544775333,-0.126880813469472,
1.34168924870467));
#16362=CARTESIAN_POINT('Ctrl Pts',(0.0755477687720905,-0.116923823242002,
1.34962823834197));
#16363=CARTESIAN_POINT('Ctrl Pts',(0.13920718769651,6.89141801743488E-5,
1.35756722797928));
#16364=CARTESIAN_POINT('Ctrl Pts',(0.0754319660950179,0.116998564767658,
1.36550621761658));
#16365=CARTESIAN_POINT('Ctrl Pts',(-0.0573960494825499,0.126824048933643,
1.37344520725389));
#16366=CARTESIAN_POINT('Ctrl Pts',(-0.13768191782304,0.0205508058651932,
1.38138419689119));
#16367=CARTESIAN_POINT('Ctrl Pts',(-0.0919294216917856,-0.104535287252199,
1.3893231865285));
#16368=CARTESIAN_POINT('Ctrl Pts',(0.0379781508110965,-0.133926497290667,
1.39726217616581));
#16369=CARTESIAN_POINT('Ctrl Pts',(0.133119345865688,-0.0407171622080862,
1.40520116580311));
#16370=CARTESIAN_POINT('Ctrl Pts',(0.106398871137127,0.0897659150453452,
1.41314015544042));
#16371=CARTESIAN_POINT('Ctrl Pts',(-0.0177224175491345,0.138074504763813,
1.42107914507772));
#16372=CARTESIAN_POINT('Ctrl Pts',(-0.125620162573399,0.0599852426217579,
1.42901813471503));
#16373=CARTESIAN_POINT('Ctrl Pts',(-0.118521039729242,-0.0730161975746823,
1.43695712435233));
#16374=CARTESIAN_POINT('Ctrl Pts',(-0.00292444232197888,-0.139176693688359,
1.44489611398964));
#16375=CARTESIAN_POINT('Ctrl Pts',(0.115350068603298,-0.0779297424218237,
1.45283510362695));
#16376=CARTESIAN_POINT('Ctrl Pts',(0.128028003046829,0.0546551750765237,
1.46077409326425));
#16377=CARTESIAN_POINT('Ctrl Pts',(0.0235079116789307,0.137209630484779,
1.46871308290156));
#16378=CARTESIAN_POINT('Ctrl Pts',(-0.102537447198224,0.0941531272373115,
1.47665207253886));
#16379=CARTESIAN_POINT('Ctrl Pts',(-0.134706575776555,-0.0350847218495708,
1.48459106217617));
#16380=CARTESIAN_POINT('Ctrl Pts',(-0.0435804807853106,-0.132222740314769,
1.49253005181348));
#16381=CARTESIAN_POINT('Ctrl Pts',(0.0874774386997331,-0.108286040948335,
1.50046904145078));
#16382=CARTESIAN_POINT('Ctrl Pts',(0.138385550162814,0.0147146982980264,
1.50840803108809));
#16383=CARTESIAN_POINT('Ctrl Pts',(0.0627460642121078,0.124368470664037,
1.51634702072539));
#16384=CARTESIAN_POINT('Ctrl Pts',(-0.0706026869052757,0.119928391791904,
1.5242860103627));
#16385=CARTESIAN_POINT('Ctrl Pts',(-0.116004137797729,0.0441355889673283,
1.5295786701209));
#16386=CARTESIAN_POINT('Ctrl Pts',(-0.117668597464313,0.00500517689812487,
1.532225));
#16387=CARTESIAN_POINT('',(0.0684664424539461,-0.0958295198918396,0.));
#16388=CARTESIAN_POINT('Ctrl Pts',(0.0684664424539414,-0.095829519891843,
-1.38777878078145E-17));
#16389=CARTESIAN_POINT('Ctrl Pts',(0.100334321247169,-0.0730611673843044,
0.00264632987910189));
#16390=CARTESIAN_POINT('Ctrl Pts',(0.139021564822767,0.00636891437108143,
0.00793898963730573));
#16391=CARTESIAN_POINT('Ctrl Pts',(0.0699018669780613,0.120491966796142,
0.0158779792746114));
#16392=CARTESIAN_POINT('Ctrl Pts',(-0.0632645460347191,0.123954346655885,
0.0238169689119172));
#16393=CARTESIAN_POINT('Ctrl Pts',(-0.11596266760442,0.0470121293552651,
0.0293787386625077));
#16394=CARTESIAN_POINT('Ctrl Pts',(-0.117944740497024,0.00404481602818191,
0.0322941785339964));
#16395=CARTESIAN_POINT('Ctrl Pts',(-0.117917485785546,7.60014832213644E-5,
0.0325632885263832));
#16396=CARTESIAN_POINT('Ctrl Pts',(0.0635546915223951,0.132092229195826,
-2.16840434497101E-19));
#16397=CARTESIAN_POINT('Ctrl Pts',(0.0668114782730532,0.13015255741457,
-1.00603861447787E-18));
#16398=CARTESIAN_POINT('Ctrl Pts',(0.0699821360194518,0.12808121947321,
-2.9262196004085E-17));
#16399=CARTESIAN_POINT('Ctrl Pts',(0.0730575207853233,0.125877721325919,
-2.71050543121376E-17));
#16400=CARTESIAN_POINT('Ctrl Pts',(0.0789281193465506,0.121671466161783,
-2.36378102375718E-17));
#16401=CARTESIAN_POINT('Ctrl Pts',(0.0844522091809674,0.11698398814956,
1.43782932504085E-18));
#16402=CARTESIAN_POINT('Ctrl Pts',(0.0895990070394484,0.111875963994554,
9.97465998686664E-18));
#16403=CARTESIAN_POINT('Ctrl Pts',(0.0928865546640729,0.108613183302742,
1.54276111490851E-17));
#16404=CARTESIAN_POINT('Ctrl Pts',(0.0960206821069302,0.105176950779614,
-2.53636710091701E-17));
#16405=CARTESIAN_POINT('Ctrl Pts',(0.098978417360439,0.101599719103904,
-1.56125112837913E-17));
#16406=CARTESIAN_POINT('Ctrl Pts',(0.103148772110026,0.0965558852815647,
-1.86354736740503E-18));
#16407=CARTESIAN_POINT('Ctrl Pts',(0.106976174326278,0.0912251680483688,
1.1337629845105E-17));
#16408=CARTESIAN_POINT('Ctrl Pts',(0.110435561611279,0.0856523061447448,
2.03830008427275E-17));
#16409=CARTESIAN_POINT('Ctrl Pts',(0.112407683932559,0.0824753373788608,
2.55395723911076E-17));
#16410=CARTESIAN_POINT('Ctrl Pts',(0.114261188142284,0.0792174064057451,
2.29308760465575E-17));
#16411=CARTESIAN_POINT('Ctrl Pts',(0.115986535786665,0.0758936579718971,
2.08166817117217E-17));
#16412=CARTESIAN_POINT('Ctrl Pts',(0.120573220307724,0.0670577659456877,
1.51962825639422E-17));
#16413=CARTESIAN_POINT('Ctrl Pts',(0.124235263225439,0.0578042025119142,
2.52358375750583E-18));
#16414=CARTESIAN_POINT('Ctrl Pts',(0.126883306113679,0.0482911783993335,
1.30104260698261E-17));
#16415=CARTESIAN_POINT('Ctrl Pts',(0.128478610866444,0.0425600882242624,
1.93281898253259E-17));
#16416=CARTESIAN_POINT('Ctrl Pts',(0.129704960854084,0.0367345196138549,
-5.78096029915021E-19));
#16417=CARTESIAN_POINT('Ctrl Pts',(0.130533291754837,0.0308494671050701,
0.));
#16418=CARTESIAN_POINT('Ctrl Pts',(0.131003715791213,0.0275072397983871,
3.2831114661813E-19));
#16419=CARTESIAN_POINT('Ctrl Pts',(0.131345346899704,0.0241444941465381,
-1.7128612844445E-18));
#16420=CARTESIAN_POINT('Ctrl Pts',(0.131551728167405,0.0207857616715298,
2.60208521396521E-18));
#16421=CARTESIAN_POINT('Ctrl Pts',(0.131851321606701,0.0159100565018035,
8.86587880453295E-18));
#16422=CARTESIAN_POINT('Ctrl Pts',(0.131867617692795,0.0110341713389591,
-1.68111772803455E-17));
#16423=CARTESIAN_POINT('Ctrl Pts',(0.131586936334964,0.0061777758930637,
-6.93889390390723E-18));
#16424=CARTESIAN_POINT('Ctrl Pts',(0.131099036368572,-0.00226395031615145,
9.98510028643051E-18));
#16425=CARTESIAN_POINT('Ctrl Pts',(0.129715139118287,-0.0106479390144509,
1.03491660509995E-17));
#16426=CARTESIAN_POINT('Ctrl Pts',(0.127493709984164,-0.018859987399606,
1.04083408558608E-17));
#16427=CARTESIAN_POINT('Ctrl Pts',(0.126553994220251,-0.0223338732882013,
1.04333731632617E-17));
#16428=CARTESIAN_POINT('Ctrl Pts',(0.125463061762623,-0.0257782540966497,
1.75224609115742E-17));
#16429=CARTESIAN_POINT('Ctrl Pts',(0.124232565886791,-0.0291638780753137,
1.73472347597681E-17));
#16430=CARTESIAN_POINT('Ctrl Pts',(0.12170396813588,-0.0361211392462112,
1.69871551674183E-17));
#16431=CARTESIAN_POINT('Ctrl Pts',(0.118582485980247,-0.0428512226170345,
-6.45748389186585E-19));
#16432=CARTESIAN_POINT('Ctrl Pts',(0.114911168983798,-0.0492778939609075,
3.46944695195361E-18));
#16433=CARTESIAN_POINT('Ctrl Pts',(0.112347970921096,-0.0537647937721124,
6.34254691478841E-18));
#16434=CARTESIAN_POINT('Ctrl Pts',(0.109516356061708,-0.0581036184196785,
-1.05628593522785E-17));
#16435=CARTESIAN_POINT('Ctrl Pts',(0.106427098863261,-0.0622637901458048,
-1.21430643318376E-17));
#16436=CARTESIAN_POINT('Ctrl Pts',(0.104287070791936,-0.0651456752410043,
-1.32377232732828E-17));
#16437=CARTESIAN_POINT('Ctrl Pts',(0.102021590876101,-0.067943056099314,
-1.03088264066386E-17));
#16438=CARTESIAN_POINT('Ctrl Pts',(0.0996491962474235,-0.0706287444932102,
-1.04083408558608E-17));
#16439=CARTESIAN_POINT('Ctrl Pts',(0.0938611946766418,-0.0771810981592459,
-1.06511292104842E-17));
#16440=CARTESIAN_POINT('Ctrl Pts',(0.0874218747326319,-0.0830961188460978,
9.460259835177E-18));
#16441=CARTESIAN_POINT('Ctrl Pts',(0.0803902102994179,-0.0882260767030795,
2.94902990916057E-17));
#16442=CARTESIAN_POINT('Ctrl Pts',(0.0765868618375105,-0.091000813397402,
4.03243227742548E-17));
#16443=CARTESIAN_POINT('Ctrl Pts',(0.0726097989303321,-0.0935451549285004,
-2.49510848448888E-18));
#16444=CARTESIAN_POINT('Ctrl Pts',(0.0684664424539416,-0.0958295198918429,
0.));
#16445=CARTESIAN_POINT('Ctrl Pts',(-0.00156962371674571,0.146072546381438,
1.50365));
#16446=CARTESIAN_POINT('Ctrl Pts',(0.0218361081466035,0.146362061217761,
1.50238307892777));
#16447=CARTESIAN_POINT('Ctrl Pts',(0.0452966847593804,0.141345883428421,
1.50111615785553));
#16448=CARTESIAN_POINT('Ctrl Pts',(0.0660179268768178,0.130913916311315,
1.4998492367833));
#16449=CARTESIAN_POINT('Ctrl Pts',(0.109300214423576,0.109123745727819,
1.4972029069042));
#16450=CARTESIAN_POINT('Ctrl Pts',(0.140630685714559,0.0637042888941242,
1.49455657702509));
#16451=CARTESIAN_POINT('Ctrl Pts',(0.145752650840527,0.0155206226173656,
1.49191024714599));
#16452=CARTESIAN_POINT('Ctrl Pts',(0.150874615966495,-0.0326630436593903,
1.48926391726689));
#16453=CARTESIAN_POINT('Ctrl Pts',(0.129788074927449,-0.0836109193792113,
1.48661758738779));
#16454=CARTESIAN_POINT('Ctrl Pts',(0.0921021927661857,-0.114042242015571,
1.48397125750869));
#16455=CARTESIAN_POINT('Ctrl Pts',(0.0544163106049216,-0.144473564651931,
1.48132492762959));
#16456=CARTESIAN_POINT('Ctrl Pts',(0.000131087321441313,-0.154388334204831,
1.47867859775048));
#16457=CARTESIAN_POINT('Ctrl Pts',(-0.0458840977328367,-0.139228052523514,
1.47603226787138));
#16458=CARTESIAN_POINT('Ctrl Pts',(-0.0918992827871148,-0.124067770842196,
1.47338593799228));
#16459=CARTESIAN_POINT('Ctrl Pts',(-0.129644429612189,-0.0838324379266627,
1.47073960811318));
#16460=CARTESIAN_POINT('Ctrl Pts',(-0.141854649713415,-0.0369491035797489,
1.46809327823408));
#16461=CARTESIAN_POINT('Ctrl Pts',(-0.14497337938942,-0.0249741805295802,
1.46741735368415));
#16462=CARTESIAN_POINT('Ctrl Pts',(-0.146426231435716,-0.0125655473306973,
1.46674142913422));
#16463=CARTESIAN_POINT('Ctrl Pts',(-0.14631473222987,-0.000131398079681141,
1.46606550458429));
#16464=CARTESIAN_POINT('Origin',(0.,0.,-0.0924367114736175));
#16465=CARTESIAN_POINT('',(-0.0684664424539507,-0.0958295198918364,0.));
#16466=CARTESIAN_POINT('Ctrl Pts',(-0.0686146973663072,-0.0959584553529141,
8.16675286424706E-17));
#16467=CARTESIAN_POINT('Ctrl Pts',(-0.0391968190522335,-0.116741470120209,
0.00244290680874874));
#16468=CARTESIAN_POINT('Ctrl Pts',(0.0436301113039178,-0.130476273073809,
0.0075332029917574));
#16469=CARTESIAN_POINT('Ctrl Pts',(0.134092250525203,-0.0374520209666004,
0.0152708885490261));
#16470=CARTESIAN_POINT('Ctrl Pts',(0.104134301645602,0.0924305194826295,
0.023213056671806));
#16471=CARTESIAN_POINT('Ctrl Pts',(-0.0212379681243542,0.137589894578696,
0.0311552247945861));
#16472=CARTESIAN_POINT('Ctrl Pts',(-0.106685947947232,0.0723488109778776,
0.0375631097285225));
#16473=CARTESIAN_POINT('Ctrl Pts',(-0.117663533972591,0.0165813593984342,
0.041323605288199));
#16474=CARTESIAN_POINT('Ctrl Pts',(-0.117600989619072,5.04992496179954E-5,
0.0424367114736154));
#16475=CARTESIAN_POINT('Origin',(0.,0.,0.));
#16476=CARTESIAN_POINT('Ctrl Pts',(-0.0510216505388318,0.106149619882943,
-0.0164977839420939));
#16477=CARTESIAN_POINT('Ctrl Pts',(-0.0863355867949722,0.0891756983861136,
-0.0138503945678339));
#16478=CARTESIAN_POINT('Ctrl Pts',(-0.13808023131828,0.0175094743621551,
-0.00855561581931395));
#16479=CARTESIAN_POINT('Ctrl Pts',(-0.0894531427980795,-0.106808298616542,
-0.000613447696533924));
#16480=CARTESIAN_POINT('Ctrl Pts',(0.0412394829729132,-0.132934609947913,
0.00732872042624606));
#16481=CARTESIAN_POINT('Ctrl Pts',(0.134092250525203,-0.0374520209666004,
0.0152708885490261));
#16482=CARTESIAN_POINT('Ctrl Pts',(0.104134301645602,0.0924305194826295,
0.023213056671806));
#16483=CARTESIAN_POINT('Ctrl Pts',(-0.0212379681243542,0.137589894578696,
0.0311552247945861));
#16484=CARTESIAN_POINT('Ctrl Pts',(-0.127145335141994,0.0567276974868182,
0.039097392917366));
#16485=CARTESIAN_POINT('Ctrl Pts',(-0.116579117211717,-0.0761160149501382,
0.0470395610401461));
#16486=CARTESIAN_POINT('Ctrl Pts',(0.000787973702835166,-0.139222729671589,
0.054981729162926));
#16487=CARTESIAN_POINT('Ctrl Pts',(0.117431922513572,-0.0747907597173192,
0.0629238972857061));
#16488=CARTESIAN_POINT('Ctrl Pts',(0.126496838785129,0.0581591461343325,
0.070866065408486));
#16489=CARTESIAN_POINT('Ctrl Pts',(0.0196773008918215,0.137828289815661,
0.0788082335312661));
#16490=CARTESIAN_POINT('Ctrl Pts',(-0.105168479521776,0.0912330920368172,
0.0867504016540459));
#16491=CARTESIAN_POINT('Ctrl Pts',(-0.133669226619255,-0.0389412707994331,
0.0946925697768262));
#16492=CARTESIAN_POINT('Ctrl Pts',(-0.0397151780004399,-0.133441281507892,
0.102634737899606));
#16493=CARTESIAN_POINT('Ctrl Pts',(0.0906220264938673,-0.105695447092796,
0.110576906022386));
#16494=CARTESIAN_POINT('Ctrl Pts',(0.137940159127448,0.0188783162799928,
0.118519074145166));
#16495=CARTESIAN_POINT('Ctrl Pts',(0.0588909273047484,0.126157580947307,
0.126461242267946));
#16496=CARTESIAN_POINT('Ctrl Pts',(-0.074108440039672,0.117863552156501,
0.134403410390726));
#16497=CARTESIAN_POINT('Ctrl Pts',(-0.139216864956951,0.00159439502933392,
0.142345578513506));
#16498=CARTESIAN_POINT('Ctrl Pts',(-0.0767883381764272,-0.116135388594389,
0.150287746636286));
#16499=CARTESIAN_POINT('Ctrl Pts',(0.0559861945572589,-0.127473226882309,
0.158229914759066));
#16500=CARTESIAN_POINT('Ctrl Pts',(0.137471621702818,-0.0220324926503626,
0.166172082881846));
#16501=CARTESIAN_POINT('Ctrl Pts',(0.0930189202108026,0.103592267873211,
0.174114251004626));
#16502=CARTESIAN_POINT('Ctrl Pts',(-0.0366486683060043,0.134315868829211,
0.182056419127406));
#16503=CARTESIAN_POINT('Ctrl Pts',(-0.132742311638566,0.0419923350165386,
0.189998587250186));
#16504=CARTESIAN_POINT('Ctrl Pts',(-0.107230360350792,-0.0888004916405464,
0.197940755372966));
#16505=CARTESIAN_POINT('Ctrl Pts',(0.0165156171993534,-0.138242945169174,
0.205882923495746));
#16506=CARTESIAN_POINT('Ctrl Pts',(0.125131592687617,-0.061040658666823,
0.213825091618526));
#16507=CARTESIAN_POINT('Ctrl Pts',(0.119114174013628,0.0720811421096423,
0.221767259741306));
#16508=CARTESIAN_POINT('Ctrl Pts',(0.0039759348809324,0.139169211541763,
0.229709427864086));
#16509=CARTESIAN_POINT('Ctrl Pts',(-0.114804669066963,0.0787639858025777,
0.237651595986866));
#16510=CARTESIAN_POINT('Ctrl Pts',(-0.128412401817242,-0.0537971426620367,
0.245593764109646));
#16511=CARTESIAN_POINT('Ctrl Pts',(-0.024381182195918,-0.137074561658528,
0.253535932232426));
#16512=CARTESIAN_POINT('Ctrl Pts',(0.101985705091022,-0.094777599970642,
0.261478100355206));
#16513=CARTESIAN_POINT('Ctrl Pts',(0.134923209124943,0.0343453801629359,
0.269420268477986));
#16514=CARTESIAN_POINT('Ctrl Pts',(0.0442571924125319,0.132004463632409,
0.277362436600766));
#16515=CARTESIAN_POINT('Ctrl Pts',(-0.0869529592639067,0.108733897080731,
0.285304604723546));
#16516=CARTESIAN_POINT('Ctrl Pts',(-0.138505267237684,-0.0141480898545381,
0.293246772846326));
#16517=CARTESIAN_POINT('Ctrl Pts',(-0.0631725212350128,-0.124068972994571,
0.301188940969106));
#16518=CARTESIAN_POINT('Ctrl Pts',(0.0700327441786229,-0.12032993078169,
0.309131109091886));
#16519=CARTESIAN_POINT('Ctrl Pts',(0.139080821187468,-0.00635631000930847,
0.317073277214666));
#16520=CARTESIAN_POINT('Ctrl Pts',(0.0807165776729536,0.11344034374014,
0.325015445337446));
#16521=CARTESIAN_POINT('Ctrl Pts',(-0.0515923433190751,0.129313988454311,
0.332957613460226));
#16522=CARTESIAN_POINT('Ctrl Pts',(-0.136637377548019,0.026722734813544,
0.340899781583006));
#16523=CARTESIAN_POINT('Ctrl Pts',(-0.0965085366518414,-0.100349289247285,
0.348841949705786));
#16524=CARTESIAN_POINT('Ctrl Pts',(0.0320320385160992,-0.135491055083419,
0.356784117828566));
#16525=CARTESIAN_POINT('Ctrl Pts',(0.131227975626944,-0.0465090949381858,
0.364726285951346));
#16526=CARTESIAN_POINT('Ctrl Pts',(0.110205605501345,0.0850799742312894,
0.372668454074126));
#16527=CARTESIAN_POINT('Ctrl Pts',(-0.0117764211155082,0.138727046407055,
0.380610622196906));
#16528=CARTESIAN_POINT('Ctrl Pts',(-0.122970036152848,0.065285892102983,
0.388552790319686));
#16529=CARTESIAN_POINT('Ctrl Pts',(-0.121510464882371,-0.0679638464419502,
0.396494958442466));
#16530=CARTESIAN_POINT('Ctrl Pts',(-0.00873482453528946,-0.138951719454826,
0.404437126565246));
#16531=CARTESIAN_POINT('Ctrl Pts',(0.112042812448737,-0.0826455423945668,
0.412379294688026));
#16532=CARTESIAN_POINT('Ctrl Pts',(0.130177722634257,0.049372441998279,
0.420321462810806));
#16533=CARTESIAN_POINT('Ctrl Pts',(0.0290564652212241,0.136160197297018,
0.428263630933586));
#16534=CARTESIAN_POINT('Ctrl Pts',(-0.098683499418539,0.098211223603141,
0.436205799056366));
#16535=CARTESIAN_POINT('Ctrl Pts',(-0.136019240449831,-0.0297093205335648,
0.444147967179146));
#16536=CARTESIAN_POINT('Ctrl Pts',(-0.0487473834415776,-0.130413074907061,
0.452090135301926));
#16537=CARTESIAN_POINT('Ctrl Pts',(0.0831820848081396,-0.111645054821459,
0.460032303424706));
#16538=CARTESIAN_POINT('Ctrl Pts',(0.138908217753341,0.00940130521287039,
0.467974471547486));
#16539=CARTESIAN_POINT('Ctrl Pts',(0.0673801526530663,0.121835103839429,
0.475916639670265));
#16540=CARTESIAN_POINT('Ctrl Pts',(-0.0658750545035054,0.12265543075329,
0.483858807793047));
#16541=CARTESIAN_POINT('Ctrl Pts',(-0.138781944133385,0.0111107822259715,
0.491800975915825));
#16542=CARTESIAN_POINT('Ctrl Pts',(-0.084550315326251,-0.110612484274364,
0.499743144038607));
#16543=CARTESIAN_POINT('Ctrl Pts',(0.0471380885036503,-0.131003351527116,
0.507685312161385));
#16544=CARTESIAN_POINT('Ctrl Pts',(0.135643160584381,-0.031381690295376,
0.515627480284167));
#16545=CARTESIAN_POINT('Ctrl Pts',(0.0998851624184703,0.0969888232104648,
0.523569648406945));
#16546=CARTESIAN_POINT('Ctrl Pts',(-0.0273779061153799,0.136507610615132,
0.531511816529727));
#16547=CARTESIAN_POINT('Ctrl Pts',(-0.129560000008381,0.0509714027366644,
0.539453984652505));
#16548=CARTESIAN_POINT('Ctrl Pts',(-0.113051823689188,-0.0812598465397498,
0.547396152775286));
#16549=CARTESIAN_POINT('Ctrl Pts',(0.00702343738442799,-0.139048728244533,
0.555338320898066));
#16550=CARTESIAN_POINT('Ctrl Pts',(0.12066450826877,-0.0694546898587181,
0.563280489020846));
#16551=CARTESIAN_POINT('Ctrl Pts',(0.123764493242992,0.063766979789076,
0.571222657143626));
#16552=CARTESIAN_POINT('Ctrl Pts',(0.0134834875971477,0.13857154491934,
0.579164825266405));
#16553=CARTESIAN_POINT('Ctrl Pts',(-0.109149777898995,0.0864303389077871,
0.587106993389186));
#16554=CARTESIAN_POINT('Ctrl Pts',(-0.131790633456927,-0.0448899368693808,
0.595049161511966));
#16555=CARTESIAN_POINT('Ctrl Pts',(-0.0336977294021144,-0.135086418755761,
0.602991329634746));
#16556=CARTESIAN_POINT('Ctrl Pts',(0.0952657566843092,-0.101529863106778,
0.610933497757526));
#16557=CARTESIAN_POINT('Ctrl Pts',(0.136956022624868,0.025038477707157,
0.618875665880307));
#16558=CARTESIAN_POINT('Ctrl Pts',(0.0531805018142573,0.128669000640787,
0.626817834003085));
#16559=CARTESIAN_POINT('Ctrl Pts',(-0.0793138220987445,0.114425500318782,
0.634760002125867));
#16560=CARTESIAN_POINT('Ctrl Pts',(-0.139148536750765,-0.00464351367351466,
0.642702170248646));
#16561=CARTESIAN_POINT('Ctrl Pts',(-0.0715088964667609,-0.119458592094588,
0.650644338371427));
#16562=CARTESIAN_POINT('Ctrl Pts',(0.0616402393688536,-0.124837327709565,
0.658586506494205));
#16563=CARTESIAN_POINT('Ctrl Pts',(0.138320583400205,-0.0158522461166236,
0.666528674616987));
#16564=CARTESIAN_POINT('Ctrl Pts',(0.0882850628235238,0.107655121482266,
0.674470842739765));
#16565=CARTESIAN_POINT('Ctrl Pts',(-0.0426286451686149,0.132539337972556,
0.682413010862546));
#16566=CARTESIAN_POINT('Ctrl Pts',(-0.13449013477919,0.0360039045964495,
0.690355178985326));
#16567=CARTESIAN_POINT('Ctrl Pts',(-0.103144844235522,-0.0935148042116587,
0.698297347108106));
#16568=CARTESIAN_POINT('Ctrl Pts',(0.022691720100341,-0.137364345221032,
0.706239515230886));
#16569=CARTESIAN_POINT('Ctrl Pts',(0.127740337615313,-0.0553740340325759,
0.714181683353665));
#16570=CARTESIAN_POINT('Ctrl Pts',(0.115765682611161,0.077344581120379,
0.722123851476446));
#16571=CARTESIAN_POINT('Ctrl Pts',(-0.00226223072526165,0.139207614056346,
0.730066019599226));
#16572=CARTESIAN_POINT('Ctrl Pts',(-0.118217708309552,0.0735421711751344,
0.738008187722006));
#16573=CARTESIAN_POINT('Ctrl Pts',(-0.125873620115675,-0.059495455776806,
0.745950355844786));
#16574=CARTESIAN_POINT('Ctrl Pts',(-0.0182163644075178,-0.138029133036789,
0.753892523967566));
#16575=CARTESIAN_POINT('Ctrl Pts',(0.106128952536144,-0.0901139441634624,
0.761834692090347));
#16576=CARTESIAN_POINT('Ctrl Pts',(0.133249245915149,0.0403548753208232,
0.769776860213125));
#16577=CARTESIAN_POINT('Ctrl Pts',(0.0382995408207276,0.133854483197375,
0.777719028335907));
#16578=CARTESIAN_POINT('Ctrl Pts',(-0.0917364783268051,0.104729633071593,
0.785661196458685));
#16579=CARTESIAN_POINT('Ctrl Pts',(-0.137732458880487,-0.0203383202317681,
0.793603364581467));
#16580=CARTESIAN_POINT('Ctrl Pts',(-0.0575513573065257,-0.126774282767806,
0.801545532704245));
#16581=CARTESIAN_POINT('Ctrl Pts',(0.0753527000357912,-0.117071978271622,
0.809487700827026));
#16582=CARTESIAN_POINT('Ctrl Pts',(0.139225942868322,-0.000119714417332432,
0.817429868949805));
#16583=CARTESIAN_POINT('Ctrl Pts',(0.0755539188089132,0.116942220141962,
0.825372037072586));
#16584=CARTESIAN_POINT('Ctrl Pts',(-0.0573332568284509,0.12687306712048,
0.833314205195366));
#16585=CARTESIAN_POINT('Ctrl Pts',(-0.13769727914169,0.0205751504512258,
0.841256373318145));
#16586=CARTESIAN_POINT('Ctrl Pts',(-0.0919164475821765,-0.104571717796869,
0.849198541440926));
#16587=CARTESIAN_POINT('Ctrl Pts',(0.0380692928980519,-0.133920149482284,
0.857140709563706));
#16588=CARTESIAN_POINT('Ctrl Pts',(0.133179650076608,-0.0405839661022353,
0.865082877686486));
#16589=CARTESIAN_POINT('Ctrl Pts',(0.106283765719693,0.0899312995767124,
0.873025045809266));
#16590=CARTESIAN_POINT('Ctrl Pts',(-0.0179789669825735,0.138060255849953,
0.880967213932046));
#16591=CARTESIAN_POINT('Ctrl Pts',(-0.125771118879347,0.0597118342956578,
0.888909382054826));
#16592=CARTESIAN_POINT('Ctrl Pts',(-0.118344004924669,-0.0733387619032726,
0.896851550177606));
#16593=CARTESIAN_POINT('Ctrl Pts',(-0.00250162451743248,-0.139203517821528,
0.904793718300386));
#16594=CARTESIAN_POINT('Ctrl Pts',(0.115632500949424,-0.0775435504945224,
0.912735886423165));
#16595=CARTESIAN_POINT('Ctrl Pts',(0.127835376168433,0.0551542754370876,
0.920678054545947));
#16596=CARTESIAN_POINT('Ctrl Pts',(0.0229279137899797,0.137325118854324,
0.928620222668725));
#16597=CARTESIAN_POINT('Ctrl Pts',(-0.102983873094174,0.0936920454555137,
0.936562390791507));
#16598=CARTESIAN_POINT('Ctrl Pts',(-0.134551852288801,-0.0357725669300891,
0.944504558914285));
#16599=CARTESIAN_POINT('Ctrl Pts',(-0.0428565117498991,-0.132465832952297,
0.952446727037066));
#16600=CARTESIAN_POINT('Ctrl Pts',(0.0880997963686447,-0.107806787258123,
0.960388895159846));
#16601=CARTESIAN_POINT('Ctrl Pts',(0.138347640177547,0.0156143509765511,
0.968331063282625));
#16602=CARTESIAN_POINT('Ctrl Pts',(0.061854832590724,0.124731139593481,
0.976273231405407));
#16603=CARTESIAN_POINT('Ctrl Pts',(-0.0713033562375951,0.119581390225944,
0.984215399528185));
#16604=CARTESIAN_POINT('Ctrl Pts',(-0.139140345480169,0.00488280234845834,
0.992157567650966));
#16605=CARTESIAN_POINT('Ctrl Pts',(-0.0795104838321055,-0.114288934109561,
1.00009973577375));
#16606=CARTESIAN_POINT('Ctrl Pts',(0.0529591494285269,-0.128760265574912,
1.00804190389653));
#16607=CARTESIAN_POINT('Ctrl Pts',(0.136912761112491,-0.0252739657289669,
1.0159840720193));
#16608=CARTESIAN_POINT('Ctrl Pts',(0.0954402180350474,0.101365883217864,
1.02392624014209));
#16609=CARTESIAN_POINT('Ctrl Pts',(-0.0334653697086341,0.135144169424284,
1.03186840826486));
#16610=CARTESIAN_POINT('Ctrl Pts',(-0.131713240771149,0.0451165125500212,
1.03981057638765));
#16611=CARTESIAN_POINT('Ctrl Pts',(-0.109298251871946,-0.0862425048155002,
1.04775274451043));
#16612=CARTESIAN_POINT('Ctrl Pts',(0.0132451643780021,-0.13859452774087,
1.05569491263321));
#16613=CARTESIAN_POINT('Ctrl Pts',(0.123654649330263,-0.0639797248987874,
1.06363708075599));
#16614=CARTESIAN_POINT('Ctrl Pts',(0.120783771971213,0.0692470788374567,
1.07157924887876));
#16615=CARTESIAN_POINT('Ctrl Pts',(0.00726255089817806,0.139036444335888,
1.07952141700155));
#16616=CARTESIAN_POINT('Ctrl Pts',(-0.112911912907791,0.0814541430660127,
1.08746358512433));
#16617=CARTESIAN_POINT('Ctrl Pts',(-0.129647464608677,-0.0507485213543897,
1.09540575324711));
#16618=CARTESIAN_POINT('Ctrl Pts',(-0.0276126195379174,-0.136460326620484,
1.10334792136989));
#16619=CARTESIAN_POINT('Ctrl Pts',(0.0997182217817603,-0.0971604536002107,
1.11129008949267));
#16620=CARTESIAN_POINT('Ctrl Pts',(0.135696927507188,0.0311483765905046,
1.11923225761545));
#16621=CARTESIAN_POINT('Ctrl Pts',(0.0473633069609982,0.130922093830007,
1.12717442573822));
#16622=CARTESIAN_POINT('Ctrl Pts',(-0.0843599685788644,0.110757722983492,
1.13511659386101));
#16623=CARTESIAN_POINT('Ctrl Pts',(-0.138800846271631,-0.0108721006891078,
1.14305876198379));
#16624=CARTESIAN_POINT('Ctrl Pts',(-0.0660858892268601,-0.122541963197144,
1.15100093010657));
#16625=CARTESIAN_POINT('Ctrl Pts',(0.0671705316110708,-0.121950798202395,
1.15894309822935));
#16626=CARTESIAN_POINT('Ctrl Pts',(0.138891844802359,-0.00964017357273747,
1.16688526635212));
#16627=CARTESIAN_POINT('Ctrl Pts',(0.0833739592533277,0.111501840422208,
1.17482743447491));
#16628=CARTESIAN_POINT('Ctrl Pts',(-0.0485230383040216,0.130496713571114,
1.18276960259768));
#16629=CARTESIAN_POINT('Ctrl Pts',(-0.135967947813762,0.0299431906521225,
1.19071177072047));
#16630=CARTESIAN_POINT('Ctrl Pts',(-0.0988522486080867,-0.0980413710850678,
1.19865393884324));
#16631=CARTESIAN_POINT('Ctrl Pts',(0.0288222657999454,-0.136209964735594,
1.20659610696603));
#16632=CARTESIAN_POINT('Ctrl Pts',(0.130092623711363,-0.0495962373069701,
1.21453827508881));
#16633=CARTESIAN_POINT('Ctrl Pts',(0.112184773380136,0.082452738709893,
1.22248044321158));
#16634=CARTESIAN_POINT('Ctrl Pts',(-0.00849585454694533,0.138966535376798,
1.23042261133437));
#16635=CARTESIAN_POINT('Ctrl Pts',(-0.121393406896754,0.0681727090639588,
1.23836477945715));
#16636=CARTESIAN_POINT('Ctrl Pts',(-0.123082127310551,-0.0650743223999996,
1.24630694757992));
#16637=CARTESIAN_POINT('Ctrl Pts',(-0.0120149744006178,-0.138706589206355,
1.25424911570271));
#16638=CARTESIAN_POINT('Ctrl Pts',(0.110059129405696,-0.0852693704304675,
1.26219128382548));
#16639=CARTESIAN_POINT('Ctrl Pts',(0.13130776387206,0.0462833517151888,
1.27013345194827));
#16640=CARTESIAN_POINT('Ctrl Pts',(0.0322649968732001,0.135435768819968,
1.27807562007105));
#16641=CARTESIAN_POINT('Ctrl Pts',(-0.0963358219719167,0.100515107841202,
1.28601778819382));
#16642=CARTESIAN_POINT('Ctrl Pts',(-0.136683130933199,-0.0264877182308561,
1.29395995631661));
#16643=CARTESIAN_POINT('Ctrl Pts',(-0.0518146499729274,-0.129225073214149,
1.30190212443939));
#16644=CARTESIAN_POINT('Ctrl Pts',(0.0805213734929343,-0.11357898534207,
1.30984429256217));
#16645=CARTESIAN_POINT('Ctrl Pts',(0.1390915465469,0.0061171215252809,1.31778646068495));
#16646=CARTESIAN_POINT('Ctrl Pts',(0.0702395735793815,0.120209316621791,
1.32572862880773));
#16647=CARTESIAN_POINT('Ctrl Pts',(-0.0629590648350173,0.124177428154433,
1.33367079693051));
#16648=CARTESIAN_POINT('Ctrl Pts',(-0.138480731711197,0.0143862582011507,
1.34161296505328));
#16649=CARTESIAN_POINT('Ctrl Pts',(-0.0871398218994898,-0.108584202098263,
1.34955513317607));
#16650=CARTESIAN_POINT('Ctrl Pts',(0.0440301174146577,-0.132080378229483,
1.35749730129884));
#16651=CARTESIAN_POINT('Ctrl Pts',(0.13486394497766,-0.0345773583278084,
1.36543946942163));
#16652=CARTESIAN_POINT('Ctrl Pts',(0.102148545386143,0.0946020732301706,
1.3733816375444));
#16653=CARTESIAN_POINT('Ctrl Pts',(-0.0241454188302812,0.137116288461919,
1.38132380566719));
#16654=CARTESIAN_POINT('Ctrl Pts',(-0.128319693277533,0.0540178939468163,
1.38926597378996));
#16655=CARTESIAN_POINT('Ctrl Pts',(-0.114939956470138,-0.0785664351508689,
1.39720814191275));
#16656=CARTESIAN_POINT('Ctrl Pts',(0.00373660876362508,-0.139175849115243,
1.40515031003553));
#16657=CARTESIAN_POINT('Ctrl Pts',(0.118990018389619,-0.0722858665142316,
1.41309247815831));
#16658=CARTESIAN_POINT('Ctrl Pts',(0.125236419206141,0.0608253567263532,
1.42103464628109));
#16659=CARTESIAN_POINT('Ctrl Pts',(0.0167532566496359,0.13821437898841,
1.42897681440387));
#16660=CARTESIAN_POINT('Ctrl Pts',(-0.107077349343502,0.0889846891406984,
1.43691898252665));
#16661=CARTESIAN_POINT('Ctrl Pts',(-0.132814597987359,-0.0417638487589672,
1.44486115064943));
#16662=CARTESIAN_POINT('Ctrl Pts',(-0.0368790902657646,-0.134252921254984,
1.45280331877221));
#16663=CARTESIAN_POINT('Ctrl Pts',(0.0928396680879532,-0.103751556080299,
1.46074548689499));
#16664=CARTESIAN_POINT('Ctrl Pts',(0.137511141307062,0.0217950526079239,
1.46868765501776));
#16665=CARTESIAN_POINT('Ctrl Pts',(0.0562018483347667,0.127378648737854,
1.47662982314055));
#16666=CARTESIAN_POINT('Ctrl Pts',(-0.0765818961642769,0.116263681173923,
1.48457199126332));
#16667=CARTESIAN_POINT('Ctrl Pts',(-0.13923195096087,-0.00134816270381636,
1.49251415938611));
#16668=CARTESIAN_POINT('Ctrl Pts',(-0.0742871760264013,-0.117748889605885,
1.50045632750888));
#16669=CARTESIAN_POINT('Ctrl Pts',(0.0586284551779338,-0.126233948370975,
1.50839849563167));
#16670=CARTESIAN_POINT('Ctrl Pts',(0.137995068118234,-0.019163470063063,
1.51634066375444));
#16671=CARTESIAN_POINT('Ctrl Pts',(0.0906261803825392,0.105639137646141,
1.52428283187723));
#16672=CARTESIAN_POINT('Ctrl Pts',(0.00417072711528833,0.124051375507138,
1.52957761062575));
#16673=CARTESIAN_POINT('Ctrl Pts',(-0.0334019664627544,0.1129391839063,
1.53222500000001));
#16674=CARTESIAN_POINT('Ctrl Pts',(-0.0551480035117261,0.114734422509858,
-0.0109985226280628));
#16675=CARTESIAN_POINT('Ctrl Pts',(-0.093317938433455,0.0963877427684319,
-0.00835113325380276));
#16676=CARTESIAN_POINT('Ctrl Pts',(-0.149247407742026,0.0189255452031589,
-0.00305635450528277));
#16677=CARTESIAN_POINT('Ctrl Pts',(-0.0966876253720675,-0.115446371588928,
0.00488581361749726));
#16678=CARTESIAN_POINT('Ctrl Pts',(0.0445747075563756,-0.143685636564375,
0.0128279817402772));
#16679=CARTESIAN_POINT('Ctrl Pts',(0.144936900801175,-0.0404809362687151,
0.0207701498630572));
#16680=CARTESIAN_POINT('Ctrl Pts',(0.112556116319125,0.0999057960529736,
0.0287123179858373));
#16681=CARTESIAN_POINT('Ctrl Pts',(-0.0229555792165621,0.148717415239805,
0.0366544861086172));
#16682=CARTESIAN_POINT('Ctrl Pts',(-0.137428156769908,0.0613155244327884,
0.0445966542313972));
#16683=CARTESIAN_POINT('Ctrl Pts',(-0.126007400730642,-0.0822718633254329,
0.0525388223541772));
#16684=CARTESIAN_POINT('Ctrl Pts',(0.000851700720621877,-0.150482305134309,
0.0604809904769572));
#16685=CARTESIAN_POINT('Ctrl Pts',(0.126929176276611,-0.0808394286734405,
0.0684231585997372));
#16686=CARTESIAN_POINT('Ctrl Pts',(0.136727213562698,0.0628627408439891,
0.0763653267225173));
#16687=CARTESIAN_POINT('Ctrl Pts',(0.0212686937255662,0.148975090584026,
0.0843074948452972));
#16688=CARTESIAN_POINT('Ctrl Pts',(-0.113673932864549,0.0986115272026031,
0.0922496629680772));
#16689=CARTESIAN_POINT('Ctrl Pts',(-0.144479665027646,-0.0420906285100245,
0.100191831090857));
#16690=CARTESIAN_POINT('Ctrl Pts',(-0.0429271251068198,-0.144233284958223,
0.108133999213637));
#16691=CARTESIAN_POINT('Ctrl Pts',(0.0979510420095061,-0.114243518700172,
0.116076167336417));
#16692=CARTESIAN_POINT('Ctrl Pts',(0.149096007275942,0.0204050915936607,
0.124018335459197));
#16693=CARTESIAN_POINT('Ctrl Pts',(0.0636537044864716,0.136360518400275,
0.131960503581977));
#16694=CARTESIAN_POINT('Ctrl Pts',(-0.0801019266996435,0.127395713772213,
0.139902671704757));
#16695=CARTESIAN_POINT('Ctrl Pts',(-0.15047596611352,0.00172334100814176,
0.147844839827537));
#16696=CARTESIAN_POINT('Ctrl Pts',(-0.0829985603893774,-0.125527785761544,
0.155787007950317));
#16697=CARTESIAN_POINT('Ctrl Pts',(0.0605140527882773,-0.137782566606816,
0.163729176073097));
#16698=CARTESIAN_POINT('Ctrl Pts',(0.148589577098441,-0.0238143605552183,
0.171671344195877));
#16699=CARTESIAN_POINT('Ctrl Pts',(0.100541783424623,0.111970245809892,
0.179613512318657));
#16700=CARTESIAN_POINT('Ctrl Pts',(-0.0396126128240685,0.145178604134651,
0.187555680441437));
#16701=CARTESIAN_POINT('Ctrl Pts',(-0.143477786216001,0.0453884461694337,
0.195497848564217));
#16702=CARTESIAN_POINT('Ctrl Pts',(-0.115902567375552,-0.095982191346566,
0.203440016686997));
#16703=CARTESIAN_POINT('Ctrl Pts',(0.0178513102906219,-0.149423281002214,
0.211382184809777));
#16704=CARTESIAN_POINT('Ctrl Pts',(0.135251553802876,-0.0659772944027704,
0.219324352932557));
#16705=CARTESIAN_POINT('Ctrl Pts',(0.128747479107914,0.07791067196398,0.227266521055337));
#16706=CARTESIAN_POINT('Ctrl Pts',(0.00429748682099232,0.150424458749874,
0.235208689178117));
#16707=CARTESIAN_POINT('Ctrl Pts',(-0.124089444892588,0.0851339876261335,
0.243150857300897));
#16708=CARTESIAN_POINT('Ctrl Pts',(-0.138797696890977,-0.0581479623084488,
0.251093025423677));
#16709=CARTESIAN_POINT('Ctrl Pts',(-0.0263529993083425,-0.148160405002171,
0.259035193546457));
#16710=CARTESIAN_POINT('Ctrl Pts',(0.110233752987369,-0.102442695616748,
0.266977361669237));
#16711=CARTESIAN_POINT('Ctrl Pts',(0.145835062802846,0.0371230472913779,
0.274919529792017));
#16712=CARTESIAN_POINT('Ctrl Pts',(0.0478364728857143,0.142680265085169,
0.282861697914797));
#16713=CARTESIAN_POINT('Ctrl Pts',(-0.0939852406223356,0.117527701960322,
0.290803866037577));
#16714=CARTESIAN_POINT('Ctrl Pts',(-0.14970681824969,-0.01529231023972,
0.298746034160357));
#16715=CARTESIAN_POINT('Ctrl Pts',(-0.0682815703945392,-0.134102995221473,
0.306688202283137));
#16716=CARTESIAN_POINT('Ctrl Pts',(0.0756966107742644,-0.1300615596562,
0.314630370405917));
#16717=CARTESIAN_POINT('Ctrl Pts',(0.150328919865546,-0.00687037371415525,
0.322572538528697));
#16718=CARTESIAN_POINT('Ctrl Pts',(0.0872444944832666,0.122614780370367,
0.330514706651477));
#16719=CARTESIAN_POINT('Ctrl Pts',(-0.0557648508131485,0.139772198940638,
0.338456874774257));
#16720=CARTESIAN_POINT('Ctrl Pts',(-0.147687863823926,0.0288839239377102,
0.346399042897038));
#16721=CARTESIAN_POINT('Ctrl Pts',(-0.104313621021262,-0.10846499275041,
0.354341211019817));
#16722=CARTESIAN_POINT('Ctrl Pts',(0.0346226151823369,-0.146448833047075,
0.362283379142597));
#16723=CARTESIAN_POINT('Ctrl Pts',(0.141840978962514,-0.0502704970123603,
0.370225547265377));
#16724=CARTESIAN_POINT('Ctrl Pts',(0.119118434135606,0.0919607787700563,
0.378167715388157));
#16725=CARTESIAN_POINT('Ctrl Pts',(-0.0127288338612142,0.149946533709345,
0.386109883510937));
#16726=CARTESIAN_POINT('Ctrl Pts',(-0.132915182358376,0.070565859178174,
0.394052051633717));
#16727=CARTESIAN_POINT('Ctrl Pts',(-0.131337568919768,-0.0734603918663599,
0.401994219756497));
#16728=CARTESIAN_POINT('Ctrl Pts',(-0.00944124952954395,-0.150189377088511,
0.409936387879277));
#16729=CARTESIAN_POINT('Ctrl Pts',(0.121104224366159,-0.0893294633566384,
0.417878556002057));
#16730=CARTESIAN_POINT('Ctrl Pts',(0.140705787232781,0.0533654159743681,
0.425820724124838));
#16731=CARTESIAN_POINT('Ctrl Pts',(0.0314063937394313,0.147172091835368,
0.433762892247617));
#16732=CARTESIAN_POINT('Ctrl Pts',(-0.106664482920656,0.106154012011714,
0.441705060370398));
#16733=CARTESIAN_POINT('Ctrl Pts',(-0.147019735166745,-0.032112048430678,
0.449647228493177));
#16734=CARTESIAN_POINT('Ctrl Pts',(-0.052689806088835,-0.14096017351449,
0.457589396615958));
#16735=CARTESIAN_POINT('Ctrl Pts',(0.0899093983958942,-0.120674298270189,
0.465531564738737));
#16736=CARTESIAN_POINT('Ctrl Pts',(0.15014235720654,0.0101616315312987,
0.473473732861518));
#16737=CARTESIAN_POINT('Ctrl Pts',(0.0728294921055832,0.131688462906045,
0.481415900984297));
#16738=CARTESIAN_POINT('Ctrl Pts',(-0.071202669822089,0.132575133389036,
0.489358069107078));
#16739=CARTESIAN_POINT('Ctrl Pts',(-0.150005871264529,0.012009361726732,
0.497300237229857));
#16740=CARTESIAN_POINT('Ctrl Pts',(-0.0913882839399832,-0.119558219045865,
0.505242405352637));
#16741=CARTESIAN_POINT('Ctrl Pts',(0.0509503601487159,-0.141598188489932,
0.513184573475417));
#16742=CARTESIAN_POINT('Ctrl Pts',(0.146613240011817,-0.0339196703426114,
0.521126741598197));
#16743=CARTESIAN_POINT('Ctrl Pts',(0.107963329873666,0.104832750538675,
0.529068909720978));
#16744=CARTESIAN_POINT('Ctrl Pts',(-0.0295920819230583,0.147547602048875,
0.537011077843756));
#16745=CARTESIAN_POINT('Ctrl Pts',(-0.140038106568177,0.055093691941219,
0.544953245966537));
#16746=CARTESIAN_POINT('Ctrl Pts',(-0.122194838935542,-0.0878316999746162,
0.552895414089317));
#16747=CARTESIAN_POINT('Ctrl Pts',(0.00759145471482065,-0.150294231420327,
0.560837582212097));
#16748=CARTESIAN_POINT('Ctrl Pts',(0.130423195946632,-0.0750718065719766,
0.568779750334878));
#16749=CARTESIAN_POINT('Ctrl Pts',(0.133773890807325,0.0689241055160235,
0.576721918457657));
#16750=CARTESIAN_POINT('Ctrl Pts',(0.0145739585745413,0.149778456108953,
0.584664086580438));
#16751=CARTESIAN_POINT('Ctrl Pts',(-0.117977216952174,0.0934203535806499,
0.592606254703216));
#16752=CARTESIAN_POINT('Ctrl Pts',(-0.142449141490696,-0.0485203902651028,
0.600548422825998));
#16753=CARTESIAN_POINT('Ctrl Pts',(-0.036423018067407,-0.146011471938939,
0.608490590948776));
#16754=CARTESIAN_POINT('Ctrl Pts',(0.102970331784443,-0.109741044988262,
0.616432759071558));
#16755=CARTESIAN_POINT('Ctrl Pts',(0.148032279177632,0.0270634532975707,
0.624374927194337));
#16756=CARTESIAN_POINT('Ctrl Pts',(0.0574814509102497,0.139075048028633,
0.632317095317117));
#16757=CARTESIAN_POINT('Ctrl Pts',(-0.0857282916847416,0.123679611042927,
0.640259263439898));
#16758=CARTESIAN_POINT('Ctrl Pts',(-0.150402111894479,-0.00501905574730406,
0.648201431562677));
#16759=CARTESIAN_POINT('Ctrl Pts',(-0.0772921462128499,-0.129119751845818,
0.656143599685457));
#16760=CARTESIAN_POINT('Ctrl Pts',(0.0666253659236285,-0.134933490277457,
0.664085767808237));
#16761=CARTESIAN_POINT('Ctrl Pts',(0.14950719819016,-0.0171342893707992,
0.672027935931017));
#16762=CARTESIAN_POINT('Ctrl Pts',(0.0954250774564579,0.11636168087194,
0.679970104053797));
#16763=CARTESIAN_POINT('Ctrl Pts',(-0.0460762176180427,0.143258397146306,
0.687912272176577));
#16764=CARTESIAN_POINT('Ctrl Pts',(-0.145366963764729,0.0389157041403328,
0.695854440299358));
#16765=CARTESIAN_POINT('Ctrl Pts',(-0.111486636987321,-0.101077771820372,
0.703796608422136));
#16766=CARTESIAN_POINT('Ctrl Pts',(0.02452690272786,-0.148473624679578,
0.711738776544918));
#16767=CARTESIAN_POINT('Ctrl Pts',(0.138071279799868,-0.0598523840572839,
0.719680944667696));
#16768=CARTESIAN_POINT('Ctrl Pts',(0.125128179973684,0.0835997892305201,
0.727623112790477));
#16769=CARTESIAN_POINT('Ctrl Pts',(-0.00244518761474098,0.150465967050502,
0.735565280913257));
#16770=CARTESIAN_POINT('Ctrl Pts',(-0.127778512144395,0.0794898610961098,
0.743507449036036));
#16771=CARTESIAN_POINT('Ctrl Pts',(-0.136053592364468,-0.0643071239260258,
0.751449617158818));
#16772=CARTESIAN_POINT('Ctrl Pts',(-0.019689604662082,-0.149192176910068,
0.759391785281597));
#16773=CARTESIAN_POINT('Ctrl Pts',(0.114712083700712,-0.0974018687498071,
0.767333953404378));
#16774=CARTESIAN_POINT('Ctrl Pts',(0.144025718573537,0.0436185576594447,
0.775276121527157));
#16775=CARTESIAN_POINT('Ctrl Pts',(0.0413969989087525,0.14467990414796,
0.783218289649938));
#16776=CARTESIAN_POINT('Ctrl Pts',(-0.0991556246317344,0.113199594905656,
0.791160457772717));
#16777=CARTESIAN_POINT('Ctrl Pts',(-0.148871509365196,-0.021983172706469,
0.799102625895497));
#16778=CARTESIAN_POINT('Ctrl Pts',(-0.062205797368885,-0.137027095702329,
0.807044794018277));
#16779=CARTESIAN_POINT('Ctrl Pts',(0.081446815661698,-0.126540121706451,
0.814986962141057));
#16780=CARTESIAN_POINT('Ctrl Pts',(0.150485778196879,-0.000129396266831759,
0.822929130263837));
#16781=CARTESIAN_POINT('Ctrl Pts',(0.0816643079123276,0.126399869446589,
0.830871298386618));
#16782=CARTESIAN_POINT('Ctrl Pts',(-0.0619700581130299,0.137133869194964,
0.838813466509397));
#16783=CARTESIAN_POINT('Ctrl Pts',(-0.148833484480893,0.0222391564630926,
0.846755634632177));
#16784=CARTESIAN_POINT('Ctrl Pts',(-0.0993501488194509,-0.113028908304323,
0.854697802754957));
#16785=CARTESIAN_POINT('Ctrl Pts',(0.041148129789194,-0.144750881164039,
0.862639970877736));
#16786=CARTESIAN_POINT('Ctrl Pts',(0.143950494202948,-0.0438661760544617,
0.870582139000517));
#16787=CARTESIAN_POINT('Ctrl Pts',(0.114879417330645,0.0972044528644933,
0.878524307123298));
#16788=CARTESIAN_POINT('Ctrl Pts',(-0.0194330078274841,0.149225816766708,
0.886466475246077));
#16789=CARTESIAN_POINT('Ctrl Pts',(-0.135942801386891,0.0645410019599824,
0.894408643368857));
#16790=CARTESIAN_POINT('Ctrl Pts',(-0.127915022941288,-0.0792700011911429,
0.902350811491637));
#16791=CARTESIAN_POINT('Ctrl Pts',(-0.00270394227186439,-0.150461539534541,
0.910292979614417));
#16792=CARTESIAN_POINT('Ctrl Pts',(0.124984227305131,-0.0838148501630433,
0.918235147737197));
#16793=CARTESIAN_POINT('Ctrl Pts',(0.138174004553101,0.0596148525845174,
0.926177315859977));
#16794=CARTESIAN_POINT('Ctrl Pts',(0.0247821984756025,0.148431225898158,
0.934119483982757));
#16795=CARTESIAN_POINT('Ctrl Pts',(-0.11131264737753,0.101269347369872,
0.942061652105537));
#16796=CARTESIAN_POINT('Ctrl Pts',(-0.145433672650089,-0.0386656571445607,
0.950003820228317));
#16797=CARTESIAN_POINT('Ctrl Pts',(-0.0463225128062989,-0.143178947440692,
0.957945988351097));
#16798=CARTESIAN_POINT('Ctrl Pts',(0.0952248276606132,-0.116525612549003,
0.965888156473877));
#16799=CARTESIAN_POINT('Ctrl Pts',(0.149536443172165,0.0168771545685866,
0.973830324596656));
#16800=CARTESIAN_POINT('Ctrl Pts',(0.0668573142755158,0.134818714245386,
0.981772492719438));
#16801=CARTESIAN_POINT('Ctrl Pts',(-0.0770699830103684,0.129252481220654,
0.989714660842216));
#16802=CARTESIAN_POINT('Ctrl Pts',(-0.15039325815857,0.00527769678589187,
0.997656828964997));
#16803=CARTESIAN_POINT('Ctrl Pts',(-0.0859408583470751,-0.123532000103139,
1.00559899708778));
#16804=CARTESIAN_POINT('Ctrl Pts',(0.0572421967501742,-0.139173693973137,
1.01354116521056));
#16805=CARTESIAN_POINT('Ctrl Pts',(0.147985518909957,-0.0273179863069172,
1.02148333333334));
#16806=CARTESIAN_POINT('Ctrl Pts',(0.103158902618224,0.109563803299803,
1.02942550145612));
#16807=CARTESIAN_POINT('Ctrl Pts',(-0.0361718663885326,0.146073893166727,
1.0373676695789));
#16808=CARTESIAN_POINT('Ctrl Pts',(-0.142365489706367,0.0487652901517079,
1.04530983770168));
#16809=CARTESIAN_POINT('Ctrl Pts',(-0.118137698690712,-0.0932173284908804,
1.05325200582446));
#16810=CARTESIAN_POINT('Ctrl Pts',(0.0143163610725534,-0.149803297655807,
1.06119417394724));
#16811=CARTESIAN_POINT('Ctrl Pts',(0.133655163317704,-0.0691540562905145,
1.06913634207002));
#16812=CARTESIAN_POINT('Ctrl Pts',(0.130552105047211,0.0748474051030229,
1.0770785101928));
#16813=CARTESIAN_POINT('Ctrl Pts',(0.0078499064261323,0.150280954056111,
1.08502067831558));
#16814=CARTESIAN_POINT('Ctrl Pts',(-0.122043612932812,0.0880417101447944,
1.09296284643836));
#16815=CARTESIAN_POINT('Ctrl Pts',(-0.140132644828567,-0.0548527851276936,
1.10090501456114));
#16816=CARTESIAN_POINT('Ctrl Pts',(-0.0298457776877653,-0.147496493982489,
1.10884718268392));
#16817=CARTESIAN_POINT('Ctrl Pts',(0.107782887988268,-0.10501826145877,
1.1167893508067));
#16818=CARTESIAN_POINT('Ctrl Pts',(0.146671355310253,0.033667487497105,
1.12473151892948));
#16819=CARTESIAN_POINT('Ctrl Pts',(0.0511937930472066,0.141510359113225,
1.13267368705226));
#16820=CARTESIAN_POINT('Ctrl Pts',(-0.0911825429852659,0.119715203870077,
1.14061585517504));
#16821=CARTESIAN_POINT('Ctrl Pts',(-0.150026302104679,-0.0117513769282424,
1.14855802329782));
#16822=CARTESIAN_POINT('Ctrl Pts',(-0.0714305557085884,-0.132452489195471,
1.1565001914206));
#16823=CARTESIAN_POINT('Ctrl Pts',(0.0726029180563751,-0.131813513998426,
1.16444235954338));
#16824=CARTESIAN_POINT('Ctrl Pts',(0.150124660100533,-0.010419818262018,
1.17238452766616));
#16825=CARTESIAN_POINT('Ctrl Pts',(0.0901167906002831,0.120519501471002,
1.18032669578894));
#16826=CARTESIAN_POINT('Ctrl Pts',(-0.0524473171394798,0.141050576417769,
1.18826886391172));
#16827=CARTESIAN_POINT('Ctrl Pts',(-0.146964294261872,0.0323648326895764,
1.1962110320345));
#16828=CARTESIAN_POINT('Ctrl Pts',(-0.106846879624786,-0.105970422747861,
1.20415320015727));
#16829=CARTESIAN_POINT('Ctrl Pts',(0.0311532535456026,-0.14722588419309,
1.21209536828006));
#16830=CARTESIAN_POINT('Ctrl Pts',(0.140613805972886,-0.0536073106276968,
1.22003753640283));
#16831=CARTESIAN_POINT('Ctrl Pts',(0.121257666323848,0.0891210667609394,
1.22797970452562));
#16832=CARTESIAN_POINT('Ctrl Pts',(-0.00918295295119051,0.150205391241489,
1.2359218726484));
#16833=CARTESIAN_POINT('Ctrl Pts',(-0.131211043922368,0.0736861461587066,
1.24386404077118));
#16834=CARTESIAN_POINT('Ctrl Pts',(-0.133036338837895,-0.0703371788708997,
1.25180620889396));
#16835=CARTESIAN_POINT('Ctrl Pts',(-0.0129866800356469,-0.149924422041766,
1.25974837701674));
#16836=CARTESIAN_POINT('Ctrl Pts',(0.118960111851797,-0.0921654923014072,
1.26769054513952));
#16837=CARTESIAN_POINT('Ctrl Pts',(0.141927220045961,0.050026496908035,
1.2756327132623));
#16838=CARTESIAN_POINT('Ctrl Pts',(0.0348744139414821,0.146389075532006,
1.28357488138508));
#16839=CARTESIAN_POINT('Ctrl Pts',(-0.104126938119509,0.108644221848311,
1.29151704950786));
#16840=CARTESIAN_POINT('Ctrl Pts',(-0.147737317493493,-0.0286299004949125,
1.29945921763064));
#16841=CARTESIAN_POINT('Ctrl Pts',(-0.0560051364173496,-0.139676092720537,
1.30740138575342));
#16842=CARTESIAN_POINT('Ctrl Pts',(0.0870335032532438,-0.122764634549313,
1.3153435538762));
#16843=CARTESIAN_POINT('Ctrl Pts',(0.150340512633584,0.00661184096937889,
1.32328572199898));
#16844=CARTESIAN_POINT('Ctrl Pts',(0.0759201674095095,0.129931190880528,
1.33122789012176));
#16845=CARTESIAN_POINT('Ctrl Pts',(-0.0680508508044829,0.134220221643466,
1.33917005824454));
#16846=CARTESIAN_POINT('Ctrl Pts',(-0.149680298423566,0.0155497403439283,
1.34711222636732));
#16847=CARTESIAN_POINT('Ctrl Pts',(-0.0941872156892785,-0.117365900463673,
1.3550543944901));
#16848=CARTESIAN_POINT('Ctrl Pts',(0.0475910332998192,-0.142762319241037,
1.36299656261288));
#16849=CARTESIAN_POINT('Ctrl Pts',(0.145771005694385,-0.0373737865856905,
1.37093873073566));
#16850=CARTESIAN_POINT('Ctrl Pts',(0.110409762917901,0.10225297323032,1.37888089885844));
#16851=CARTESIAN_POINT('Ctrl Pts',(-0.0260981686868614,0.148205506441964,
1.38682306698121));
#16852=CARTESIAN_POINT('Ctrl Pts',(-0.138697490589939,0.0583865667538053,
1.394765235104));
#16853=CARTESIAN_POINT('Ctrl Pts',(-0.124235673603468,-0.0849204601545819,
1.40270740322677));
#16854=CARTESIAN_POINT('Ctrl Pts',(0.0040388053119065,-0.150431633134115,
1.41064957134956));
#16855=CARTESIAN_POINT('Ctrl Pts',(0.12861328245382,-0.0781319533624403,
1.41859173947234));
#16856=CARTESIAN_POINT('Ctrl Pts',(0.1353648581188,0.0657445800149866,1.42653390759512));
#16857=CARTESIAN_POINT('Ctrl Pts',(0.0181081687242482,0.149392404544468,
1.43447607571789));
#16858=CARTESIAN_POINT('Ctrl Pts',(-0.115737181672069,0.0961812857364522,
1.44241824384068));
#16859=CARTESIAN_POINT('Ctrl Pts',(-0.143555918690644,-0.0451414811888502,
1.45036041196346));
#16860=CARTESIAN_POINT('Ctrl Pts',(-0.0398616700558823,-0.145110565703753,
1.45830258008624));
#16861=CARTESIAN_POINT('Ctrl Pts',(0.100348034367198,-0.112142416378873,
1.46624474820902));
#16862=CARTESIAN_POINT('Ctrl Pts',(0.14863229283285,0.0235577176564554,
1.4741869163318));
#16863=CARTESIAN_POINT('Ctrl Pts',(0.0607471474677608,0.137680339497592,
1.48212908445458));
#16864=CARTESIAN_POINT('Ctrl Pts',(-0.0827754224726193,0.125666453945577,
1.49007125257736));
#16865=CARTESIAN_POINT('Ctrl Pts',(-0.150492272191201,-0.00145719475437189,
1.49801342070014));
#16866=CARTESIAN_POINT('Ctrl Pts',(-0.0802951178786721,-0.12727177793954,
1.50595558882292));
#16867=CARTESIAN_POINT('Ctrl Pts',(0.0633700050447994,-0.136443062004882,
1.5138977569457));
#16868=CARTESIAN_POINT('Ctrl Pts',(0.149155357006591,-0.0207133070603065,
1.52183992506848));
#16869=CARTESIAN_POINT('Ctrl Pts',(0.0979555318420461,0.114182655252422,
1.52978209319126));
#16870=CARTESIAN_POINT('Ctrl Pts',(0.00450803278943675,0.134083974545181,
1.53507687193978));
#16871=CARTESIAN_POINT('Ctrl Pts',(-0.0361033354337414,0.122073089461022,
1.53772426131404));
#16872=CARTESIAN_POINT('Ctrl Pts',(-0.0592743564846203,0.123319225136773,
-0.00549926131403157));
#16873=CARTESIAN_POINT('Ctrl Pts',(-0.100300290071938,0.10359978715075,
-0.00285187193977157));
#16874=CARTESIAN_POINT('Ctrl Pts',(-0.160414584165772,0.0203416160441626,
0.00244290680874841));
#16875=CARTESIAN_POINT('Ctrl Pts',(-0.103922107946056,-0.124084444561314,
0.0103850749315284));
#16876=CARTESIAN_POINT('Ctrl Pts',(0.0479099321398382,-0.154436663180837,
0.0183272430543084));
#16877=CARTESIAN_POINT('Ctrl Pts',(0.155781551077148,-0.0435098515708298,
0.0262694111770884));
#16878=CARTESIAN_POINT('Ctrl Pts',(0.120977930992648,0.107381072623318,
0.0342115792998684));
#16879=CARTESIAN_POINT('Ctrl Pts',(-0.0246731903087699,0.159844935900913,
0.0421537474226484));
#16880=CARTESIAN_POINT('Ctrl Pts',(-0.147710978397823,0.0659033513787588,
0.0500959155454284));
#16881=CARTESIAN_POINT('Ctrl Pts',(-0.135435684249567,-0.0884277117007276,
0.0580380836682085));
#16882=CARTESIAN_POINT('Ctrl Pts',(0.000915427738408385,-0.16174188059703,
0.0659802517909884));
#16883=CARTESIAN_POINT('Ctrl Pts',(0.13642643003965,-0.0868880976295618,
0.0739224199137684));
#16884=CARTESIAN_POINT('Ctrl Pts',(0.146957588340267,0.0675663355536457,
0.0818645880365484));
#16885=CARTESIAN_POINT('Ctrl Pts',(0.0228600865593111,0.160121891352391,
0.0898067561593285));
#16886=CARTESIAN_POINT('Ctrl Pts',(-0.122179386207322,0.105989962368389,
0.0977489242821083));
#16887=CARTESIAN_POINT('Ctrl Pts',(-0.155290103436038,-0.0452399862206161,
0.105691092404888));
#16888=CARTESIAN_POINT('Ctrl Pts',(-0.0461390722131997,-0.155025288408554,
0.113633260527668));
#16889=CARTESIAN_POINT('Ctrl Pts',(0.105280057525145,-0.122791590307548,
0.121575428650448));
#16890=CARTESIAN_POINT('Ctrl Pts',(0.160251855424436,0.0219318669073289,
0.129517596773229));
#16891=CARTESIAN_POINT('Ctrl Pts',(0.0684164816681947,0.146563455853242,
0.137459764896008));
#16892=CARTESIAN_POINT('Ctrl Pts',(-0.086095413359615,0.136927875387926,
0.145401933018789));
#16893=CARTESIAN_POINT('Ctrl Pts',(-0.16173506727009,0.00185228698694943,
0.153344101141568));
#16894=CARTESIAN_POINT('Ctrl Pts',(-0.0892087826023274,-0.134920182928699,
0.161286269264348));
#16895=CARTESIAN_POINT('Ctrl Pts',(0.0650419110192955,-0.148091906331324,
0.169228437387128));
#16896=CARTESIAN_POINT('Ctrl Pts',(0.159707532494063,-0.025596228460074,
0.177170605509908));
#16897=CARTESIAN_POINT('Ctrl Pts',(0.108064646638443,0.120348223746572,
0.185112773632688));
#16898=CARTESIAN_POINT('Ctrl Pts',(-0.0425765573421325,0.156041339440091,
0.193054941755468));
#16899=CARTESIAN_POINT('Ctrl Pts',(-0.154213260793436,0.0487845573223287,
0.200997109878248));
#16900=CARTESIAN_POINT('Ctrl Pts',(-0.124574774400312,-0.103163891052585,
0.208939278001028));
#16901=CARTESIAN_POINT('Ctrl Pts',(0.0191870033818907,-0.160603616835255,
0.216881446123808));
#16902=CARTESIAN_POINT('Ctrl Pts',(0.145371514918136,-0.0709139301387177,
0.224823614246588));
#16903=CARTESIAN_POINT('Ctrl Pts',(0.138380784202201,0.0837402018183176,
0.232765782369368));
#16904=CARTESIAN_POINT('Ctrl Pts',(0.00461903876105218,0.161679705957985,
0.240707950492149));
#16905=CARTESIAN_POINT('Ctrl Pts',(-0.133374220718213,0.0915039894496894,
0.248650118614928));
#16906=CARTESIAN_POINT('Ctrl Pts',(-0.149182991964712,-0.0624987819548612,
0.256592286737709));
#16907=CARTESIAN_POINT('Ctrl Pts',(-0.0283248164207669,-0.159246248345813,
0.264534454860488));
#16908=CARTESIAN_POINT('Ctrl Pts',(0.118481800883715,-0.110107791262854,
0.272476622983269));
#16909=CARTESIAN_POINT('Ctrl Pts',(0.156746916480749,0.0399007144198201,
0.280418791106048));
#16910=CARTESIAN_POINT('Ctrl Pts',(0.0514157533588968,0.153356066537929,
0.288360959228829));
#16911=CARTESIAN_POINT('Ctrl Pts',(-0.101017521980764,0.126321506839912,
0.296303127351608));
#16912=CARTESIAN_POINT('Ctrl Pts',(-0.160908369261695,-0.0164365306249019,
0.304245295474388));
#16913=CARTESIAN_POINT('Ctrl Pts',(-0.0733906195540655,-0.144137017448375,
0.312187463597168));
#16914=CARTESIAN_POINT('Ctrl Pts',(0.0813604773699057,-0.13979318853071,
0.320129631719948));
#16915=CARTESIAN_POINT('Ctrl Pts',(0.161577018543625,-0.00738443741900211,
0.328071799842729));
#16916=CARTESIAN_POINT('Ctrl Pts',(0.0937724112935796,0.131789217000595,
0.336013967965508));
#16917=CARTESIAN_POINT('Ctrl Pts',(-0.0599373583072218,0.150230409426965,
0.343956136088289));
#16918=CARTESIAN_POINT('Ctrl Pts',(-0.158738350099833,0.0310451130618767,
0.351898304211068));
#16919=CARTESIAN_POINT('Ctrl Pts',(-0.112118705390683,-0.116580696253536,
0.359840472333849));
#16920=CARTESIAN_POINT('Ctrl Pts',(0.0372131918485748,-0.15740661101073,
0.367782640456628));
#16921=CARTESIAN_POINT('Ctrl Pts',(0.152453982298084,-0.0540318990865351,
0.375724808579408));
#16922=CARTESIAN_POINT('Ctrl Pts',(0.128031262769868,0.0988415833088236,
0.383666976702188));
#16923=CARTESIAN_POINT('Ctrl Pts',(-0.0136812466069205,0.161166021011634,
0.391609144824968));
#16924=CARTESIAN_POINT('Ctrl Pts',(-0.142860328563903,0.0758458262533652,
0.399551312947749));
#16925=CARTESIAN_POINT('Ctrl Pts',(-0.141164672957165,-0.0789569372907697,
0.407493481070528));
#16926=CARTESIAN_POINT('Ctrl Pts',(-0.0101476745237983,-0.161427034722196,
0.415435649193308));
#16927=CARTESIAN_POINT('Ctrl Pts',(0.130165636283581,-0.0960133843187101,
0.423377817316089));
#16928=CARTESIAN_POINT('Ctrl Pts',(0.151233851831306,0.0573583899504574,
0.431319985438868));
#16929=CARTESIAN_POINT('Ctrl Pts',(0.0337563222576384,0.158183986373718,
0.439262153561649));
#16930=CARTESIAN_POINT('Ctrl Pts',(-0.114645466422773,0.114096800420287,
0.447204321684428));
#16931=CARTESIAN_POINT('Ctrl Pts',(-0.158020229883659,-0.0345147763277912,
0.455146489807208));
#16932=CARTESIAN_POINT('Ctrl Pts',(-0.0566322287360923,-0.151507272121918,
0.463088657929988));
#16933=CARTESIAN_POINT('Ctrl Pts',(0.0966367119836487,-0.129703541718919,
0.471030826052768));
#16934=CARTESIAN_POINT('Ctrl Pts',(0.161376496659739,0.0109219578497271,
0.478972994175549));
#16935=CARTESIAN_POINT('Ctrl Pts',(0.0782788315581001,0.141541821972661,
0.486915162298328));
#16936=CARTESIAN_POINT('Ctrl Pts',(-0.0765302851406724,0.142494836024782,
0.494857330421108));
#16937=CARTESIAN_POINT('Ctrl Pts',(-0.161229798395673,0.0129079412274925,
0.502799498543889));
#16938=CARTESIAN_POINT('Ctrl Pts',(-0.0982262525537151,-0.128503953817366,
0.510741666666668));
#16939=CARTESIAN_POINT('Ctrl Pts',(0.0547626317937811,-0.152193025452748,
0.518683834789449));
#16940=CARTESIAN_POINT('Ctrl Pts',(0.157583319439253,-0.0364576503898468,
0.526626002912228));
#16941=CARTESIAN_POINT('Ctrl Pts',(0.116041497328862,0.112676677866884,
0.534568171035008));
#16942=CARTESIAN_POINT('Ctrl Pts',(-0.0318062577307366,0.158587593482618,
0.542510339157789));
#16943=CARTESIAN_POINT('Ctrl Pts',(-0.150516213127973,0.0592159811457737,
0.550452507280567));
#16944=CARTESIAN_POINT('Ctrl Pts',(-0.131337854181896,-0.0944035534094825,
0.558394675403349));
#16945=CARTESIAN_POINT('Ctrl Pts',(0.00815947204521347,-0.161539734596121,
0.566336843526128));
#16946=CARTESIAN_POINT('Ctrl Pts',(0.140181883624494,-0.080688923285235,
0.574279011648909));
#16947=CARTESIAN_POINT('Ctrl Pts',(0.143783288371658,0.0740812312429708,
0.582221179771688));
#16948=CARTESIAN_POINT('Ctrl Pts',(0.0156644295519346,0.160985367298567,
0.590163347894469));
#16949=CARTESIAN_POINT('Ctrl Pts',(-0.126804656005353,0.100410368253513,
0.598105516017247));
#16950=CARTESIAN_POINT('Ctrl Pts',(-0.153107649524464,-0.0521508436608248,
0.606047684140029));
#16951=CARTESIAN_POINT('Ctrl Pts',(-0.0391483067326994,-0.156936525122116,
0.613989852262808));
#16952=CARTESIAN_POINT('Ctrl Pts',(0.110674906884577,-0.117952226869747,
0.621932020385589));
#16953=CARTESIAN_POINT('Ctrl Pts',(0.159108535730396,0.0290884288879846,
0.629874188508368));
#16954=CARTESIAN_POINT('Ctrl Pts',(0.061782400006242,0.14948109541648,0.637816356631148));
#16955=CARTESIAN_POINT('Ctrl Pts',(-0.0921427612707386,0.132933721767072,
0.645758524753929));
#16956=CARTESIAN_POINT('Ctrl Pts',(-0.161655687038194,-0.0053945978210935,
0.653700692876707));
#16957=CARTESIAN_POINT('Ctrl Pts',(-0.0830753959589387,-0.138780911597048,
0.661642860999489));
#16958=CARTESIAN_POINT('Ctrl Pts',(0.0716104924784035,-0.145029652845349,
0.669585029122267));
#16959=CARTESIAN_POINT('Ctrl Pts',(0.160693812980115,-0.0184163326249747,
0.677527197245049));
#16960=CARTESIAN_POINT('Ctrl Pts',(0.102565092089392,0.125068240261613,
0.685469365367828));
#16961=CARTESIAN_POINT('Ctrl Pts',(-0.0495237900674707,0.153977456320057,
0.693411533490608));
#16962=CARTESIAN_POINT('Ctrl Pts',(-0.156243792750268,0.0418275036842162,
0.701353701613389));
#16963=CARTESIAN_POINT('Ctrl Pts',(-0.119828429739121,-0.108640739429086,
0.709295869736167));
#16964=CARTESIAN_POINT('Ctrl Pts',(0.0263620853553792,-0.159582904138124,
0.717238037858949));
#16965=CARTESIAN_POINT('Ctrl Pts',(0.148402221984423,-0.0643307340819919,
0.725180205981728));
#16966=CARTESIAN_POINT('Ctrl Pts',(0.134490677336207,0.0898549973406614,
0.733122374104509));
#16967=CARTESIAN_POINT('Ctrl Pts',(-0.00262814450422035,0.161724320044658,
0.741064542227287));
#16968=CARTESIAN_POINT('Ctrl Pts',(-0.137339315979238,0.0854375510170853,
0.749006710350069));
#16969=CARTESIAN_POINT('Ctrl Pts',(-0.146233564613262,-0.0691187920752458,
0.756948878472847));
#16970=CARTESIAN_POINT('Ctrl Pts',(-0.0211628449166461,-0.160355220783347,
0.764891046595629));
#16971=CARTESIAN_POINT('Ctrl Pts',(0.12329521486528,-0.104689793336152,
0.772833214718408));
#16972=CARTESIAN_POINT('Ctrl Pts',(0.154802191231926,0.0468822399980663,
0.780775382841188));
#16973=CARTESIAN_POINT('Ctrl Pts',(0.0444944569967772,0.155505325098544,
0.788717550963968));
#16974=CARTESIAN_POINT('Ctrl Pts',(-0.106574770936664,0.121669556739719,
0.796659719086747));
#16975=CARTESIAN_POINT('Ctrl Pts',(-0.160010559849905,-0.0236280251811701,
0.804601887209529));
#16976=CARTESIAN_POINT('Ctrl Pts',(-0.0668602374312443,-0.147279908636853,
0.812544055332307));
#16977=CARTESIAN_POINT('Ctrl Pts',(0.0875409312876049,-0.13600826514128,
0.820486223455089));
#16978=CARTESIAN_POINT('Ctrl Pts',(0.161745613525436,-0.000139078116330951,
0.828428391577867));
#16979=CARTESIAN_POINT('Ctrl Pts',(0.0877746970157421,0.135857518751215,
0.836370559700649));
#16980=CARTESIAN_POINT('Ctrl Pts',(-0.0666068593976089,0.147394671269449,
0.844312727823428));
#16981=CARTESIAN_POINT('Ctrl Pts',(-0.159969689820096,0.0239031624749592,
0.852254895946208));
#16982=CARTESIAN_POINT('Ctrl Pts',(-0.106783850056725,-0.121486098811777,
0.860197064068988));
#16983=CARTESIAN_POINT('Ctrl Pts',(0.0442269666803361,-0.155581612845794,
0.868139232191768));
#16984=CARTESIAN_POINT('Ctrl Pts',(0.154721338329289,-0.0471483860066884,
0.876081400314548));
#16985=CARTESIAN_POINT('Ctrl Pts',(0.123475068941597,0.104477606152275,
0.884023568437328));
#16986=CARTESIAN_POINT('Ctrl Pts',(-0.0208870486723946,0.160391377683462,
0.891965736560109));
#16987=CARTESIAN_POINT('Ctrl Pts',(-0.146114483894434,0.0693701696243073,
0.899907904682887));
#16988=CARTESIAN_POINT('Ctrl Pts',(-0.137486040957907,-0.0852012404790134,
0.907850072805669));
#16989=CARTESIAN_POINT('Ctrl Pts',(-0.00290626002629624,-0.161719561247554,
0.915792240928448));
#16990=CARTESIAN_POINT('Ctrl Pts',(0.134335953660838,-0.0900861498315643,
0.923734409051229));
#16991=CARTESIAN_POINT('Ctrl Pts',(0.148512632937768,0.0640754297319473,
0.931676577174007));
#16992=CARTESIAN_POINT('Ctrl Pts',(0.0266364831612253,0.159537332941991,
0.939618745296788));
#16993=CARTESIAN_POINT('Ctrl Pts',(-0.119641421660886,0.10884664928423,
0.947560913419568));
#16994=CARTESIAN_POINT('Ctrl Pts',(-0.156315493011378,-0.0415587473590326,
0.955503081542348));
#16995=CARTESIAN_POINT('Ctrl Pts',(-0.0497885138626987,-0.153892061929087,
0.963445249665127));
#16996=CARTESIAN_POINT('Ctrl Pts',(0.102349858952582,-0.125244437839883,
0.971387417787908));
#16997=CARTESIAN_POINT('Ctrl Pts',(0.160725246166783,0.018139958160622,
0.979329585910688));
#16998=CARTESIAN_POINT('Ctrl Pts',(0.0718597959603077,0.14490628889729,
0.987271754033468));
#16999=CARTESIAN_POINT('Ctrl Pts',(-0.0828366097831417,0.138923572215364,
0.995213922156248));
#17000=CARTESIAN_POINT('Ctrl Pts',(-0.161646170836971,0.00567259122332548,
1.00315609027903));
#17001=CARTESIAN_POINT('Ctrl Pts',(-0.0923712328620446,-0.132775066096718,
1.01109825840181));
#17002=CARTESIAN_POINT('Ctrl Pts',(0.0615252440718216,-0.149587122371362,
1.01904042652459));
#17003=CARTESIAN_POINT('Ctrl Pts',(0.159058276707423,-0.0293620068848675,
1.02698259464737));
#17004=CARTESIAN_POINT('Ctrl Pts',(0.1108775872014,0.117761723381742,1.03492476277015));
#17005=CARTESIAN_POINT('Ctrl Pts',(-0.0388783630684312,0.157003616909169,
1.04286693089293));
#17006=CARTESIAN_POINT('Ctrl Pts',(-0.153017738641585,0.0524140677533946,
1.05080909901571));
#17007=CARTESIAN_POINT('Ctrl Pts',(-0.126977145509477,-0.10019215216626,
1.05875126713849));
#17008=CARTESIAN_POINT('Ctrl Pts',(0.0153875577671049,-0.161012067570745,
1.06669343526127));
#17009=CARTESIAN_POINT('Ctrl Pts',(0.143655677305146,-0.0743283876822416,
1.07463560338405));
#17010=CARTESIAN_POINT('Ctrl Pts',(0.140320438123209,0.080447731368589,
1.08257777150683));
#17011=CARTESIAN_POINT('Ctrl Pts',(0.00843726195408678,0.161525463776335,
1.09051993962961));
#17012=CARTESIAN_POINT('Ctrl Pts',(-0.131175312957834,0.094629277223576,
1.09846210775239));
#17013=CARTESIAN_POINT('Ctrl Pts',(-0.150617825048456,-0.0589570489009974,
1.10640427587517));
#17014=CARTESIAN_POINT('Ctrl Pts',(-0.0320789358376135,-0.158532661344495,
1.11434644399795));
#17015=CARTESIAN_POINT('Ctrl Pts',(0.115847554194776,-0.112876069317329,
1.12228861212073));
#17016=CARTESIAN_POINT('Ctrl Pts',(0.157645783113317,0.0361865984037055,
1.13023078024351));
#17017=CARTESIAN_POINT('Ctrl Pts',(0.0550242791334153,0.152098624396442,
1.13817294836629));
#17018=CARTESIAN_POINT('Ctrl Pts',(-0.0980051173916675,0.128672684756662,
1.14611511648907));
#17019=CARTESIAN_POINT('Ctrl Pts',(-0.161251757937727,-0.0126306531673768,
1.15405728461185));
#17020=CARTESIAN_POINT('Ctrl Pts',(-0.0767752221903169,-0.142363015193798,
1.16199945273463));
#17021=CARTESIAN_POINT('Ctrl Pts',(0.0780353045016797,-0.141676229794458,
1.16994162085741));
#17022=CARTESIAN_POINT('Ctrl Pts',(0.161357475398708,-0.0111994629512984,
1.17788378898019));
#17023=CARTESIAN_POINT('Ctrl Pts',(0.0968596219472387,0.129537162519796,
1.18582595710297));
#17024=CARTESIAN_POINT('Ctrl Pts',(-0.0563715959749383,0.151604439264423,
1.19376812522575));
#17025=CARTESIAN_POINT('Ctrl Pts',(-0.157960640709981,0.0347864747270306,
1.20171029334853));
#17026=CARTESIAN_POINT('Ctrl Pts',(-0.114841510641486,-0.113899474410655,
1.20965246147131));
#17027=CARTESIAN_POINT('Ctrl Pts',(0.03348424129126,-0.158241803650584,
1.21759462959409));
#17028=CARTESIAN_POINT('Ctrl Pts',(0.151134988234409,-0.0576183839484237,
1.22553679771687));
#17029=CARTESIAN_POINT('Ctrl Pts',(0.130330559267559,0.0957893948119858,
1.23347896583965));
#17030=CARTESIAN_POINT('Ctrl Pts',(-0.0098700513554357,0.16144424710618,
1.24142113396243));
#17031=CARTESIAN_POINT('Ctrl Pts',(-0.141028680947982,0.0791995832534545,
1.24936330208521));
#17032=CARTESIAN_POINT('Ctrl Pts',(-0.142990550365238,-0.0756000353418,
1.25730547020799));
#17033=CARTESIAN_POINT('Ctrl Pts',(-0.013958385670676,-0.161142254877177,
1.26524763833077));
#17034=CARTESIAN_POINT('Ctrl Pts',(0.127861094297897,-0.0990616141723472,
1.27318980645355));
#17035=CARTESIAN_POINT('Ctrl Pts',(0.152546676219863,0.0537696421008814,
1.28113197457633));
#17036=CARTESIAN_POINT('Ctrl Pts',(0.0374838310097642,0.157342382244044,
1.28907414269911));
#17037=CARTESIAN_POINT('Ctrl Pts',(-0.111918054267102,0.116773335855419,
1.29701631082189));
#17038=CARTESIAN_POINT('Ctrl Pts',(-0.158791504053787,-0.0307720827589687,
1.30495847894467));
#17039=CARTESIAN_POINT('Ctrl Pts',(-0.060195622861772,-0.150127112226926,
1.31290064706745));
#17040=CARTESIAN_POINT('Ctrl Pts',(0.0935456330135535,-0.131950283756556,
1.32084281519023));
#17041=CARTESIAN_POINT('Ctrl Pts',(0.161589478720268,0.00710656041347678,
1.32878498331301));
#17042=CARTESIAN_POINT('Ctrl Pts',(0.0816007612396376,0.139653065139265,
1.33672715143579));
#17043=CARTESIAN_POINT('Ctrl Pts',(-0.0731426367739486,0.144263015132499,
1.34466931955857));
#17044=CARTESIAN_POINT('Ctrl Pts',(-0.160879865135934,0.0167132224867059,
1.35261148768135));
#17045=CARTESIAN_POINT('Ctrl Pts',(-0.101234609479067,-0.126147598829082,
1.36055365580413));
#17046=CARTESIAN_POINT('Ctrl Pts',(0.051151949184981,-0.153444260252591,
1.36849582392691));
#17047=CARTESIAN_POINT('Ctrl Pts',(0.15667806641111,-0.0401702148435725,
1.37643799204969));
#17048=CARTESIAN_POINT('Ctrl Pts',(0.118670980449659,0.10990387323047,1.38438016017247));
#17049=CARTESIAN_POINT('Ctrl Pts',(-0.0280509185434417,0.159294724422008,
1.39232232829525));
#17050=CARTESIAN_POINT('Ctrl Pts',(-0.149075287902345,0.0627552395607943,
1.40026449641803));
#17051=CARTESIAN_POINT('Ctrl Pts',(-0.133531390736797,-0.0912744851582948,
1.40820666454081));
#17052=CARTESIAN_POINT('Ctrl Pts',(0.00434100186018791,-0.161687417152987,
1.41614883266359));
#17053=CARTESIAN_POINT('Ctrl Pts',(0.138236546518021,-0.0839780402106489,
1.42409100078637));
#17054=CARTESIAN_POINT('Ctrl Pts',(0.145493297031458,0.07066380330362,1.43203316890915));
#17055=CARTESIAN_POINT('Ctrl Pts',(0.0194630807988606,0.160570430100525,
1.43997533703193));
#17056=CARTESIAN_POINT('Ctrl Pts',(-0.124397014000637,0.103377882332206,
1.44791750515471));
#17057=CARTESIAN_POINT('Ctrl Pts',(-0.15429723939393,-0.0485191136187331,
1.45585967327749));
#17058=CARTESIAN_POINT('Ctrl Pts',(-0.042844249846,-0.155968210152522,1.46380184140027));
#17059=CARTESIAN_POINT('Ctrl Pts',(0.107856400646442,-0.120533276677448,
1.47174400952305));
#17060=CARTESIAN_POINT('Ctrl Pts',(0.159753444358638,0.0253203827049868,
1.47968617764583));
#17061=CARTESIAN_POINT('Ctrl Pts',(0.0652924466007548,0.147982030257331,
1.48762834576861));
#17062=CARTESIAN_POINT('Ctrl Pts',(-0.0889689487809616,0.13506922671723,
1.49557051389139));
#17063=CARTESIAN_POINT('Ctrl Pts',(-0.161752593421533,-0.00156622680492735,
1.50351268201417));
#17064=CARTESIAN_POINT('Ctrl Pts',(-0.086303059730943,-0.136794666273195,
1.51145485013695));
#17065=CARTESIAN_POINT('Ctrl Pts',(0.0681115549116652,-0.14665217563879,
1.51939701825973));
#17066=CARTESIAN_POINT('Ctrl Pts',(0.160315645894948,-0.02226314405755,
1.52733918638251));
#17067=CARTESIAN_POINT('Ctrl Pts',(0.105284883301553,0.122726172858702,
1.53528135450529));
#17068=CARTESIAN_POINT('Ctrl Pts',(0.00484533846358528,0.144116573583224,
1.54057613325381));
#17069=CARTESIAN_POINT('Ctrl Pts',(-0.0388047044047284,0.131206995015745,
1.54322352262807));
#17070=CARTESIAN_POINT('Ctrl Pts',(-0.0634007094575145,0.131904027763688,
-3.88578058618805E-16));
#17071=CARTESIAN_POINT('Ctrl Pts',(-0.107282641710421,0.110811831533068,
0.00264738937425961));
#17072=CARTESIAN_POINT('Ctrl Pts',(-0.171581760589518,0.0217576868851663,
0.0079421681227796));
#17073=CARTESIAN_POINT('Ctrl Pts',(-0.111156590520044,-0.1327225175337,
0.0158843362455596));
#17074=CARTESIAN_POINT('Ctrl Pts',(0.0512451567233008,-0.165187689797298,
0.0238265043683396));
#17075=CARTESIAN_POINT('Ctrl Pts',(0.16662620135312,-0.0465387668729445,
0.0317686724911196));
#17076=CARTESIAN_POINT('Ctrl Pts',(0.129399745666171,0.114856349193662,
0.0397108406138996));
#17077=CARTESIAN_POINT('Ctrl Pts',(-0.026390801400978,0.170972456562021,
0.0476530087366796));
#17078=CARTESIAN_POINT('Ctrl Pts',(-0.157993800025737,0.070491178324729,
0.0555951768594596));
#17079=CARTESIAN_POINT('Ctrl Pts',(-0.144863967768493,-0.0945835600760224,
0.0635373449822396));
#17080=CARTESIAN_POINT('Ctrl Pts',(0.000979154756195248,-0.17300145605975,
0.0714795131050195));
#17081=CARTESIAN_POINT('Ctrl Pts',(0.145923683802689,-0.0929367665856833,
0.0794216812277997));
#17082=CARTESIAN_POINT('Ctrl Pts',(0.157187963117837,0.0722699302633024,
0.0873638493505794));
#17083=CARTESIAN_POINT('Ctrl Pts',(0.0244514793930555,0.171268692120756,
0.0953060174733598));
#17084=CARTESIAN_POINT('Ctrl Pts',(-0.130684839550095,0.113368397534175,
0.103248185596139));
#17085=CARTESIAN_POINT('Ctrl Pts',(-0.166100541844429,-0.0483893439312075,
0.11119035371892));
#17086=CARTESIAN_POINT('Ctrl Pts',(-0.0493510193195793,-0.165817291858885,
0.119132521841699));
#17087=CARTESIAN_POINT('Ctrl Pts',(0.112609073040783,-0.131339661914923,
0.12707468996448));
#17088=CARTESIAN_POINT('Ctrl Pts',(0.17140770357293,0.0234586422209967,
0.135016858087259));
#17089=CARTESIAN_POINT('Ctrl Pts',(0.0731792588499177,0.156766393306209,
0.14295902621004));
#17090=CARTESIAN_POINT('Ctrl Pts',(-0.0920889000195865,0.146460037003638,
0.150901194332819));
#17091=CARTESIAN_POINT('Ctrl Pts',(-0.172994168426659,0.00198123296575728,
0.1588433624556));
#17092=CARTESIAN_POINT('Ctrl Pts',(-0.0954190048152776,-0.144312580095855,
0.16678553057838));
#17093=CARTESIAN_POINT('Ctrl Pts',(0.0695697692503139,-0.158401246055831,
0.17472769870116));
#17094=CARTESIAN_POINT('Ctrl Pts',(0.170825487889685,-0.0273780963649298,
0.18266986682394));
#17095=CARTESIAN_POINT('Ctrl Pts',(0.115587509852263,0.128726201683253,
0.19061203494672));
#17096=CARTESIAN_POINT('Ctrl Pts',(-0.0455405018601966,0.16690407474553,
0.198554203069499));
#17097=CARTESIAN_POINT('Ctrl Pts',(-0.164948735370872,0.0521806684752238,
0.20649637119228));
#17098=CARTESIAN_POINT('Ctrl Pts',(-0.133246981425072,-0.110345590758605,
0.214438539315059));
#17099=CARTESIAN_POINT('Ctrl Pts',(0.0205226964731592,-0.171783952668295,
0.22238070743784));
#17100=CARTESIAN_POINT('Ctrl Pts',(0.155491476033395,-0.0758505658746651,
0.230322875560619));
#17101=CARTESIAN_POINT('Ctrl Pts',(0.148014089296488,0.0895697316726553,
0.2382650436834));
#17102=CARTESIAN_POINT('Ctrl Pts',(0.00494059070111224,0.172934953166096,
0.24620721180618));
#17103=CARTESIAN_POINT('Ctrl Pts',(-0.142658996543838,0.0978739912732451,
0.25414937992896));
#17104=CARTESIAN_POINT('Ctrl Pts',(-0.159568287038446,-0.0668496016012732,
0.262091548051739));
#17105=CARTESIAN_POINT('Ctrl Pts',(-0.0302966335331915,-0.170332091689456,
0.27003371617452));
#17106=CARTESIAN_POINT('Ctrl Pts',(0.126729848780061,-0.11777288690896,
0.2779758842973));
#17107=CARTESIAN_POINT('Ctrl Pts',(0.167658770158652,0.0426783815482623,
0.28591805242008));
#17108=CARTESIAN_POINT('Ctrl Pts',(0.0549950338320791,0.164031867990689,
0.293860220542859));
#17109=CARTESIAN_POINT('Ctrl Pts',(-0.108049803339193,0.135115311719503,
0.30180238866564));
#17110=CARTESIAN_POINT('Ctrl Pts',(-0.1721099202737,-0.0175807510100837,
0.309744556788419));
#17111=CARTESIAN_POINT('Ctrl Pts',(-0.0784996687135917,-0.154171039675278,
0.3176867249112));
#17112=CARTESIAN_POINT('Ctrl Pts',(0.087024343965547,-0.14952481740522,
0.325628893033979));
#17113=CARTESIAN_POINT('Ctrl Pts',(0.172825117221703,-0.00789850112384905,
0.33357106115676));
#17114=CARTESIAN_POINT('Ctrl Pts',(0.100300328103893,0.140963653630822,
0.341513229279539));
#17115=CARTESIAN_POINT('Ctrl Pts',(-0.0641098658012952,0.160688619913292,
0.349455397402319));
#17116=CARTESIAN_POINT('Ctrl Pts',(-0.16978883637574,0.033206302186043,
0.357397565525099));
#17117=CARTESIAN_POINT('Ctrl Pts',(-0.119923789760104,-0.124696399756661,
0.36533973364788));
#17118=CARTESIAN_POINT('Ctrl Pts',(0.0398037685148125,-0.168364388974385,
0.373281901770659));
#17119=CARTESIAN_POINT('Ctrl Pts',(0.163066985633654,-0.0577933011607096,
0.38122406989344));
#17120=CARTESIAN_POINT('Ctrl Pts',(0.136944091404129,0.10572238784759,0.38916623801622));
#17121=CARTESIAN_POINT('Ctrl Pts',(-0.0146336593526265,0.172385508313924,
0.397108406138999));
#17122=CARTESIAN_POINT('Ctrl Pts',(-0.152805474769431,0.0811257933285562,
0.40505057426178));
#17123=CARTESIAN_POINT('Ctrl Pts',(-0.150991776994562,-0.0844534827151793,
0.412992742384559));
#17124=CARTESIAN_POINT('Ctrl Pts',(-0.0108540995180527,-0.172664692355881,
0.42093491050734));
#17125=CARTESIAN_POINT('Ctrl Pts',(0.139227048201004,-0.102697305280782,
0.428877078630119));
#17126=CARTESIAN_POINT('Ctrl Pts',(0.16176191642983,0.0613513639265466,
0.4368192467529));
#17127=CARTESIAN_POINT('Ctrl Pts',(0.0361062507758455,0.169195880912067,
0.444761414875679));
#17128=CARTESIAN_POINT('Ctrl Pts',(-0.12262644992489,0.12203958882886,0.45270358299846));
#17129=CARTESIAN_POINT('Ctrl Pts',(-0.169020724600573,-0.0369175042249048,
0.460645751121239));
#17130=CARTESIAN_POINT('Ctrl Pts',(-0.0605746513833496,-0.162054370729346,
0.468587919244019));
#17131=CARTESIAN_POINT('Ctrl Pts',(0.103364025571403,-0.138732785167649,
0.4765300873668));
#17132=CARTESIAN_POINT('Ctrl Pts',(0.172610636112938,0.0116822841681558,
0.484472255489579));
#17133=CARTESIAN_POINT('Ctrl Pts',(0.083728171010617,0.151395181039277,
0.49241442361236));
#17134=CARTESIAN_POINT('Ctrl Pts',(-0.081857900459256,0.152414538660527,
0.500356591735139));
#17135=CARTESIAN_POINT('Ctrl Pts',(-0.172453725526818,0.0138065207282529,
0.50829875985792));
#17136=CARTESIAN_POINT('Ctrl Pts',(-0.105064221167447,-0.137449688588867,
0.516240927980699));
#17137=CARTESIAN_POINT('Ctrl Pts',(0.0585749034388466,-0.162787862415564,
0.52418309610348));
#17138=CARTESIAN_POINT('Ctrl Pts',(0.168553398866689,-0.0389956304370821,
0.532125264226259));
#17139=CARTESIAN_POINT('Ctrl Pts',(0.124119664784058,0.120520605195094,
0.54006743234904));
#17140=CARTESIAN_POINT('Ctrl Pts',(-0.0340204335384149,0.16962758491636,
0.548009600471819));
#17141=CARTESIAN_POINT('Ctrl Pts',(-0.160994319687769,0.0633382703503284,
0.5559517685946));
#17142=CARTESIAN_POINT('Ctrl Pts',(-0.14048086942825,-0.100975406844349,
0.563893936717379));
#17143=CARTESIAN_POINT('Ctrl Pts',(0.00872748937560605,-0.172785237771916,
0.57183610484016));
#17144=CARTESIAN_POINT('Ctrl Pts',(0.149940571302356,-0.0863060399984934,
0.579778272962939));
#17145=CARTESIAN_POINT('Ctrl Pts',(0.153792685935992,0.0792383569699183,
0.58772044108572));
#17146=CARTESIAN_POINT('Ctrl Pts',(0.0167549005293281,0.17219227848818,
0.595662609208499));
#17147=CARTESIAN_POINT('Ctrl Pts',(-0.135632095058532,0.107400382926376,
0.60360477733128));
#17148=CARTESIAN_POINT('Ctrl Pts',(-0.163766157558233,-0.0557812970565469,
0.611546945454059));
#17149=CARTESIAN_POINT('Ctrl Pts',(-0.0418735953979919,-0.167861578305293,
0.61948911357684));
#17150=CARTESIAN_POINT('Ctrl Pts',(0.118379481984711,-0.126163408751231,
0.627431281699619));
#17151=CARTESIAN_POINT('Ctrl Pts',(0.17018479228316,0.0311134044783985,
0.6353734498224));
#17152=CARTESIAN_POINT('Ctrl Pts',(0.0660833491022344,0.159887142804326,
0.643315617945179));
#17153=CARTESIAN_POINT('Ctrl Pts',(-0.0985572308567358,0.142187832491218,
0.651257786067961));
#17154=CARTESIAN_POINT('Ctrl Pts',(-0.172909262181909,-0.00577013989488307,
0.659199954190738));
#17155=CARTESIAN_POINT('Ctrl Pts',(-0.0888586457050277,-0.148442071348278,
0.667142122313521));
#17156=CARTESIAN_POINT('Ctrl Pts',(0.0765956190331784,-0.155125815413241,
0.675084290436298));
#17157=CARTESIAN_POINT('Ctrl Pts',(0.171880427770071,-0.0196983758791502,
0.683026458559081));
#17158=CARTESIAN_POINT('Ctrl Pts',(0.109705106722326,0.133774799651286,
0.690968626681858));
#17159=CARTESIAN_POINT('Ctrl Pts',(-0.0529713625168984,0.164696515493808,
0.698910794804641));
#17160=CARTESIAN_POINT('Ctrl Pts',(-0.167120621735807,0.0447393032280997,
0.706852962927418));
#17161=CARTESIAN_POINT('Ctrl Pts',(-0.12817022249092,-0.116203707037801,
0.7147951310502));
#17162=CARTESIAN_POINT('Ctrl Pts',(0.0281972679828983,-0.17069218359667,
0.722737299172979));
#17163=CARTESIAN_POINT('Ctrl Pts',(0.158733164168978,-0.0688090841067,0.73067946729576));
#17164=CARTESIAN_POINT('Ctrl Pts',(0.14385317469873,0.0961102054508026,
0.738621635418538));
#17165=CARTESIAN_POINT('Ctrl Pts',(-0.00281110139369983,0.172982673038814,
0.746563803541321));
#17166=CARTESIAN_POINT('Ctrl Pts',(-0.146900119814081,0.0913852409380608,
0.754505971664098));
#17167=CARTESIAN_POINT('Ctrl Pts',(-0.156413536862055,-0.0739304602244656,
0.762448139786881));
#17168=CARTESIAN_POINT('Ctrl Pts',(-0.0226360851712103,-0.171518264656626,
0.770390307909658));
#17169=CARTESIAN_POINT('Ctrl Pts',(0.131878346029848,-0.111977717922496,
0.778332476032441));
#17170=CARTESIAN_POINT('Ctrl Pts',(0.165578663890314,0.0501459223366878,
0.786274644155218));
#17171=CARTESIAN_POINT('Ctrl Pts',(0.047591915084802,0.166330746049129,
0.794216812278001));
#17172=CARTESIAN_POINT('Ctrl Pts',(-0.113993917241593,0.130139518573781,
0.802158980400778));
#17173=CARTESIAN_POINT('Ctrl Pts',(-0.171149610334614,-0.0252728776558711,
0.81010114852356));
#17174=CARTESIAN_POINT('Ctrl Pts',(-0.0715146774936035,-0.157532721571376,
0.818043316646339));
#17175=CARTESIAN_POINT('Ctrl Pts',(0.0936350469135118,-0.14547640857611,
0.825985484769119));
#17176=CARTESIAN_POINT('Ctrl Pts',(0.173005448853992,-0.000148759965830227,
0.8339276528919));
#17177=CARTESIAN_POINT('Ctrl Pts',(0.0938850861191564,0.145315168055841,
0.841869821014678));
#17178=CARTESIAN_POINT('Ctrl Pts',(-0.0712436606821878,0.157655473343934,
0.849811989137461));
#17179=CARTESIAN_POINT('Ctrl Pts',(-0.171105895159299,0.0255671684868261,
0.857754157260238));
#17180=CARTESIAN_POINT('Ctrl Pts',(-0.114217551294,-0.129943289319231,0.86569632538302));
#17181=CARTESIAN_POINT('Ctrl Pts',(0.0473058035714782,-0.166412344527548,
0.873638493505798));
#17182=CARTESIAN_POINT('Ctrl Pts',(0.16549218245563,-0.0504305959589149,
0.88158066162858));
#17183=CARTESIAN_POINT('Ctrl Pts',(0.132070720552549,0.111750759440056,
0.889522829751358));
#17184=CARTESIAN_POINT('Ctrl Pts',(-0.022341089517305,0.171556938600217,
0.89746499787414));
#17185=CARTESIAN_POINT('Ctrl Pts',(-0.156286166401977,0.074199337288632,
0.905407165996919));
#17186=CARTESIAN_POINT('Ctrl Pts',(-0.147057058974526,-0.0911324797668838,
0.913349334119699));
#17187=CARTESIAN_POINT('Ctrl Pts',(-0.00310857778072832,-0.172977582960567,
0.92129150224248));
#17188=CARTESIAN_POINT('Ctrl Pts',(0.143687680016546,-0.0963574495000853,
0.929233670365259));
#17189=CARTESIAN_POINT('Ctrl Pts',(0.158851261322436,0.0685360068793772,
0.93717583848804));
#17190=CARTESIAN_POINT('Ctrl Pts',(0.0284907678468484,0.170643439985825,
0.945118006610819));
#17191=CARTESIAN_POINT('Ctrl Pts',(-0.127970195944242,0.116423951198588,
0.9530601747336));
#17192=CARTESIAN_POINT('Ctrl Pts',(-0.167197313372666,-0.0444518375735043,
0.961002342856378));
#17193=CARTESIAN_POINT('Ctrl Pts',(-0.0532545149190986,-0.164605176417482,
0.96894451097916));
#17194=CARTESIAN_POINT('Ctrl Pts',(0.10947489024455,-0.133963263130763,
0.976886679101939));
#17195=CARTESIAN_POINT('Ctrl Pts',(0.1719140491614,0.0194027617526574,0.984828847224719));
#17196=CARTESIAN_POINT('Ctrl Pts',(0.0768622776450996,0.154993863549195,
0.992771015347499));
#17197=CARTESIAN_POINT('Ctrl Pts',(-0.088603236555915,0.148594663210074,
1.00071318347028));
#17198=CARTESIAN_POINT('Ctrl Pts',(-0.172899083515371,0.00606748566075909,
1.00865535159306));
#17199=CARTESIAN_POINT('Ctrl Pts',(-0.0988016073770141,-0.142018132090297,
1.01659751971584));
#17200=CARTESIAN_POINT('Ctrl Pts',(0.0658082913934689,-0.160000550769587,
1.02453968783862));
#17201=CARTESIAN_POINT('Ctrl Pts',(0.170131034504888,-0.0314060274628177,
1.0324818559614));
#17202=CARTESIAN_POINT('Ctrl Pts',(0.118596271784576,0.125959643463681,
1.04042402408418));
#17203=CARTESIAN_POINT('Ctrl Pts',(-0.0415848597483297,0.167933340651612,
1.04836619220696));
#17204=CARTESIAN_POINT('Ctrl Pts',(-0.163669987576804,0.0560628453550813,
1.05630836032974));
#17205=CARTESIAN_POINT('Ctrl Pts',(-0.135816592328243,-0.107166975841641,
1.06425052845252));
#17206=CARTESIAN_POINT('Ctrl Pts',(0.0164587544616562,-0.172220837485682,
1.0721926965753));
#17207=CARTESIAN_POINT('Ctrl Pts',(0.153656191292587,-0.0795027190739688,
1.08013486469808));
#17208=CARTESIAN_POINT('Ctrl Pts',(0.150088771199207,0.0860480576341552,
1.08807703282086));
#17209=CARTESIAN_POINT('Ctrl Pts',(0.00902461748204118,0.172769973496559,
1.09601920094364));
#17210=CARTESIAN_POINT('Ctrl Pts',(-0.140307012982855,0.101216844302358,
1.10396136906642));
#17211=CARTESIAN_POINT('Ctrl Pts',(-0.161103005268346,-0.0630613126743013,
1.1119035371892));
#17212=CARTESIAN_POINT('Ctrl Pts',(-0.0343120939874615,-0.1695688287065,
1.11984570531198));
#17213=CARTESIAN_POINT('Ctrl Pts',(0.123912220401285,-0.120733877175888,
1.12778787343476));
#17214=CARTESIAN_POINT('Ctrl Pts',(0.168620210916381,0.0387057093103061,
1.13573004155754));
#17215=CARTESIAN_POINT('Ctrl Pts',(0.0588547652196237,0.162686889679659,
1.14367220968032));
#17216=CARTESIAN_POINT('Ctrl Pts',(-0.104827691798069,0.137630165643247,
1.1516143778031));
#17217=CARTESIAN_POINT('Ctrl Pts',(-0.172477213770776,-0.0135099294065116,
1.15955654592588));
#17218=CARTESIAN_POINT('Ctrl Pts',(-0.0821198886720452,-0.152273541192125,
1.16749871404866));
#17219=CARTESIAN_POINT('Ctrl Pts',(0.083467690946984,-0.15153894559049,
1.17544088217144));
#17220=CARTESIAN_POINT('Ctrl Pts',(0.172590290696882,-0.0119791076405788,
1.18338305029422));
#17221=CARTESIAN_POINT('Ctrl Pts',(0.103602453294194,0.13855482356859,1.191325218417));
#17222=CARTESIAN_POINT('Ctrl Pts',(-0.0602958748103966,0.162158302111078,
1.19926738653978));
#17223=CARTESIAN_POINT('Ctrl Pts',(-0.168956987158091,0.0372081167644847,
1.20720955466256));
#17224=CARTESIAN_POINT('Ctrl Pts',(-0.122836141658186,-0.121828526073448,
1.21515172278534));
#17225=CARTESIAN_POINT('Ctrl Pts',(0.0358152290369173,-0.169257723108079,
1.22309389090812));
#17226=CARTESIAN_POINT('Ctrl Pts',(0.161656170495932,-0.0616294572691503,
1.2310360590309));
#17227=CARTESIAN_POINT('Ctrl Pts',(0.13940345221127,0.102457722863032,1.23897822715368));
#17228=CARTESIAN_POINT('Ctrl Pts',(-0.0105571497596809,0.172683102970871,
1.24692039527646));
#17229=CARTESIAN_POINT('Ctrl Pts',(-0.150846317973597,0.0847130203482025,
1.25486256339924));
#17230=CARTESIAN_POINT('Ctrl Pts',(-0.152944761892581,-0.0808628918127005,
1.26280473152202));
#17231=CARTESIAN_POINT('Ctrl Pts',(-0.0149300913057054,-0.172360087712588,
1.2707468996448));
#17232=CARTESIAN_POINT('Ctrl Pts',(0.136762076743997,-0.105957736043287,
1.27868906776758));
#17233=CARTESIAN_POINT('Ctrl Pts',(0.163166132393764,0.0575127872937276,
1.28663123589036));
#17234=CARTESIAN_POINT('Ctrl Pts',(0.0400932480780463,0.168295688956082,
1.29457340401314));
#17235=CARTESIAN_POINT('Ctrl Pts',(-0.119709170414695,0.124902449862528,
1.30251557213592));
#17236=CARTESIAN_POINT('Ctrl Pts',(-0.169845690614082,-0.0329142650230248,
1.3104577402587));
#17237=CARTESIAN_POINT('Ctrl Pts',(-0.0643861093061943,-0.160578131733314,
1.31839990838148));
#17238=CARTESIAN_POINT('Ctrl Pts',(0.100057762773863,-0.141135932963798,
1.32634207650426));
#17239=CARTESIAN_POINT('Ctrl Pts',(0.172838444806952,0.00760127985757451,
1.33428424462704));
#17240=CARTESIAN_POINT('Ctrl Pts',(0.0872813550697656,0.149374939398002,
1.34222641274982));
#17241=CARTESIAN_POINT('Ctrl Pts',(-0.0782344227434143,0.154305808621531,
1.3501685808726));
#17242=CARTESIAN_POINT('Ctrl Pts',(-0.172079431848303,0.0178767046294837,
1.35811074899538));
#17243=CARTESIAN_POINT('Ctrl Pts',(-0.108282003268856,-0.134929297194493,
1.36605291711816));
#17244=CARTESIAN_POINT('Ctrl Pts',(0.0547128650701426,-0.164126201264144,
1.37399508524094));
#17245=CARTESIAN_POINT('Ctrl Pts',(0.167585127127835,-0.0429666431014547,
1.38193725336372));
#17246=CARTESIAN_POINT('Ctrl Pts',(0.126932197981417,0.117554773230619,
1.3898794214865));
#17247=CARTESIAN_POINT('Ctrl Pts',(-0.0300036684000219,0.170383942402052,
1.39782158960928));
#17248=CARTESIAN_POINT('Ctrl Pts',(-0.159453085214751,0.0671239123677834,
1.40576375773206));
#17249=CARTESIAN_POINT('Ctrl Pts',(-0.142827107870127,-0.0976285101620078,
1.41370592585484));
#17250=CARTESIAN_POINT('Ctrl Pts',(0.00464319840846943,-0.172943201171859,
1.42164809397762));
#17251=CARTESIAN_POINT('Ctrl Pts',(0.147859810582222,-0.0898241270588577,
1.4295902621004));
#17252=CARTESIAN_POINT('Ctrl Pts',(0.155621735944117,0.0755830265922534,
1.43753243022318));
#17253=CARTESIAN_POINT('Ctrl Pts',(0.0208179928734729,0.171748455656582,
1.44547459834596));
#17254=CARTESIAN_POINT('Ctrl Pts',(-0.133056846329205,0.11057447892796,
1.45341676646874));
#17255=CARTESIAN_POINT('Ctrl Pts',(-0.165038560097216,-0.0518967460486161,
1.46135893459152));
#17256=CARTESIAN_POINT('Ctrl Pts',(-0.0458268296361176,-0.166825854601292,
1.4693011027143));
#17257=CARTESIAN_POINT('Ctrl Pts',(0.115364766925686,-0.128924136976022,
1.47724327083708));
#17258=CARTESIAN_POINT('Ctrl Pts',(0.170874595884426,0.0270830477535184,
1.48518543895986));
#17259=CARTESIAN_POINT('Ctrl Pts',(0.0698377457337486,0.158283721017069,
1.49312760708264));
#17260=CARTESIAN_POINT('Ctrl Pts',(-0.0951624750893037,0.144471999488883,
1.50106977520542));
#17261=CARTESIAN_POINT('Ctrl Pts',(-0.173012914651864,-0.00167525885548286,
1.5090119433282));
#17262=CARTESIAN_POINT('Ctrl Pts',(-0.092311001583214,-0.14631755460685,
1.51695411145098));
#17263=CARTESIAN_POINT('Ctrl Pts',(0.072853104778531,-0.156861289272697,
1.52489627957376));
#17264=CARTESIAN_POINT('Ctrl Pts',(0.171475934783304,-0.0238129810547936,
1.53283844769654));
#17265=CARTESIAN_POINT('Ctrl Pts',(0.11261423476106,0.131269690464983,1.54078061581932));
#17266=CARTESIAN_POINT('Ctrl Pts',(0.00518264413773371,0.154149172621267,
1.54607539456784));
#17267=CARTESIAN_POINT('Ctrl Pts',(-0.0415060733757155,0.140340900570467,
1.5487227839421));
#17268=CARTESIAN_POINT('Ctrl Pts',(-0.146248097568756,-0.000123763188177425,
1.45893449541571));
#17269=CARTESIAN_POINT('Ctrl Pts',(-0.146367493381718,-0.0150081347743067,
1.45974264180765));
#17270=CARTESIAN_POINT('Ctrl Pts',(-0.144277648885518,-0.0298597803798721,
1.46055078819958));
#17271=CARTESIAN_POINT('Ctrl Pts',(-0.139839652725699,-0.043973059977961,
1.46135893459152));
#17272=CARTESIAN_POINT('Ctrl Pts',(-0.125301316610186,-0.0902064488995044,
1.46400632396578));
#17273=CARTESIAN_POINT('Ctrl Pts',(-0.08556407312315,-0.1285161517504,1.46665371334004));
#17274=CARTESIAN_POINT('Ctrl Pts',(-0.0388301852859989,-0.141354050238301,
1.4693011027143));
#17275=CARTESIAN_POINT('Ctrl Pts',(0.00790370255115092,-0.154191948726202,
1.47194849208856));
#17276=CARTESIAN_POINT('Ctrl Pts',(0.0616342347384179,-0.141558042851112,
1.47459588146282));
#17277=CARTESIAN_POINT('Ctrl Pts',(0.0977511389918415,-0.109239892458645,
1.47724327083708));
#17278=CARTESIAN_POINT('Ctrl Pts',(0.133868043245265,-0.0769217420661769,
1.47989066021134));
#17279=CARTESIAN_POINT('Ctrl Pts',(0.152371319564846,-0.024919347156331,
1.4825380495856));
#17280=CARTESIAN_POINT('Ctrl Pts',(0.144783482699524,0.0229486291758506,
1.48518543895986));
#17281=CARTESIAN_POINT('Ctrl Pts',(0.137195645834202,0.0708166055080336,
1.48783282833412));
#17282=CARTESIAN_POINT('Ctrl Pts',(0.103516695783975,0.114550163262552,
1.49048021770838));
#17283=CARTESIAN_POINT('Ctrl Pts',(0.0591771839550196,0.13411498855178,
1.49312760708264));
#17284=CARTESIAN_POINT('Ctrl Pts',(0.014837672126065,0.153679813841007,
1.4957749964569));
#17285=CARTESIAN_POINT('Ctrl Pts',(-0.0401624014816186,0.149075906664945,
1.49842238583116));
#17286=CARTESIAN_POINT('Ctrl Pts',(-0.0806375115458872,0.122416076686187,
1.50106977520542));
#17287=CARTESIAN_POINT('Ctrl Pts',(-0.0937869288003098,0.113754921033589,
1.50192985013695));
#17288=CARTESIAN_POINT('Ctrl Pts',(-0.105403311347291,0.102765876910903,
1.50278992506847));
#17289=CARTESIAN_POINT('Ctrl Pts',(-0.115078604842433,0.0902138214954038,
1.50365));
#17290=CARTESIAN_POINT('Ctrl Pts',(-0.0686146973663081,-0.0959584553529135,
1.07336015076065E-17));
#17291=CARTESIAN_POINT('Ctrl Pts',(-0.0712979561985307,-0.0944995001033786,
9.02613639135873E-18));
#17292=CARTESIAN_POINT('Ctrl Pts',(-0.0739152333025289,-0.0929325179580126,
1.64107321374712E-17));
#17293=CARTESIAN_POINT('Ctrl Pts',(-0.0764591723283171,-0.0912589988675934,
1.6154612370034E-17));
#17294=CARTESIAN_POINT('Ctrl Pts',(-0.0824897891353913,-0.0872917841461184,
1.52077426268717E-17));
#17295=CARTESIAN_POINT('Ctrl Pts',(-0.0881090519769445,-0.0827275518978924,
1.30971627060498E-17));
#17296=CARTESIAN_POINT('Ctrl Pts',(-0.0932912133381108,-0.0776621329443405,
1.43114686768087E-17));
#17297=CARTESIAN_POINT('Ctrl Pts',(-0.0960634919631888,-0.074952307504085,
1.49610807310118E-17));
#17298=CARTESIAN_POINT('Ctrl Pts',(-0.0987043519497191,-0.0721043812799658,
1.74993329480528E-17));
#17299=CARTESIAN_POINT('Ctrl Pts',(-0.101206237074718,-0.0691378820326018,
9.97465998686664E-18));
#17300=CARTESIAN_POINT('Ctrl Pts',(-0.105823426721714,-0.0636632543305198,
-3.91200561030858E-18));
#17301=CARTESIAN_POINT('Ctrl Pts',(-0.109972666997065,-0.0577811896139199,
2.24798207762934E-18));
#17302=CARTESIAN_POINT('Ctrl Pts',(-0.113625452403263,-0.0515741981665521,
9.54097911787244E-18));
#17303=CARTESIAN_POINT('Ctrl Pts',(-0.115386295340069,-0.0485820878086944,
1.30566037435822E-17));
#17304=CARTESIAN_POINT('Ctrl Pts',(-0.117027309103105,-0.0455212415157476,
-2.79521757168051E-18));
#17305=CARTESIAN_POINT('Ctrl Pts',(-0.118543833519887,-0.0424058589801268,
-3.46944695195361E-18));
#17306=CARTESIAN_POINT('Ctrl Pts',(-0.122700941917732,-0.0338659484069709,
-5.31764971597768E-18));
#17307=CARTESIAN_POINT('Ctrl Pts',(-0.125931492798984,-0.0249085743588085,
-1.15219401683824E-18));
#17308=CARTESIAN_POINT('Ctrl Pts',(-0.128167520083254,-0.0157105262534848,
9.54097911787244E-18));
#17309=CARTESIAN_POINT('Ctrl Pts',(-0.128992166906242,-0.0123182862745252,
1.3484621181291E-17));
#17310=CARTESIAN_POINT('Ctrl Pts',(-0.129681150280034,-0.00889298553317688,
1.10989611676181E-17));
#17311=CARTESIAN_POINT('Ctrl Pts',(-0.130229483957028,-0.00544263935519351,
9.54097911787244E-18));
#17312=CARTESIAN_POINT('Ctrl Pts',(-0.130761899349706,-0.00209245771889707,
8.02822573502553E-18));
#17313=CARTESIAN_POINT('Ctrl Pts',(-0.131160261982709,0.00127366115726457,
1.11791151702242E-17));
#17314=CARTESIAN_POINT('Ctrl Pts',(-0.131420990891747,0.00464012593483382,
8.67361737988404E-18));
#17315=CARTESIAN_POINT('Ctrl Pts',(-0.131728666658755,0.00861275649723166,
5.71697955546795E-18));
#17316=CARTESIAN_POINT('Ctrl Pts',(-0.131845259942619,0.0125891451047215,
-9.26473565962443E-18));
#17317=CARTESIAN_POINT('Ctrl Pts',(-0.131765781147177,0.0165567997877194,
-1.04083408558608E-17));
#17318=CARTESIAN_POINT('Ctrl Pts',(-0.131635692412819,0.0230509492424239,
-1.21888544026837E-17));
#17319=CARTESIAN_POINT('Ctrl Pts',(-0.13098103789945,0.0295216962360144,
-2.67049856555875E-17));
#17320=CARTESIAN_POINT('Ctrl Pts',(-0.129839098367345,0.0359278479980343,
-3.46944695195361E-17));
#17321=CARTESIAN_POINT('Ctrl Pts',(-0.129254890951344,0.0392051855997028,
-3.87818275556788E-17));
#17322=CARTESIAN_POINT('Ctrl Pts',(-0.128542951403208,0.0424656461998481,
-3.10678831811161E-17));
#17323=CARTESIAN_POINT('Ctrl Pts',(-0.1277070993652,0.0457037274559979,
-3.29597460435593E-17));
#17324=CARTESIAN_POINT('Ctrl Pts',(-0.126886363095037,0.0488832504000222,
-3.48173959609792E-17));
#17325=CARTESIAN_POINT('Ctrl Pts',(-0.125948031872817,0.0520333657183593,
-3.53366201082739E-17));
#17326=CARTESIAN_POINT('Ctrl Pts',(-0.124899042599898,0.0551436241923499,
-3.46944695195361E-17));
#17327=CARTESIAN_POINT('Ctrl Pts',(-0.122234979928128,0.0630425834229368,
-3.30636335736642E-17));
#17328=CARTESIAN_POINT('Ctrl Pts',(-0.118856305871375,0.070695441500891,
-2.1366080483524E-17));
#17329=CARTESIAN_POINT('Ctrl Pts',(-0.114834854776346,0.078019637496205,
-1.73472347597681E-17));
#17330=CARTESIAN_POINT('Ctrl Pts',(-0.11215901866562,0.0828930893082948,
-1.46731322388254E-17));
#17331=CARTESIAN_POINT('Ctrl Pts',(-0.109198005187061,0.0876211033078822,
8.28606628989234E-18));
#17332=CARTESIAN_POINT('Ctrl Pts',(-0.105966883726074,0.0921780034666525,
8.67361737988404E-18));
#17333=CARTESIAN_POINT('Ctrl Pts',(-0.104137243112614,0.094758373688769,
8.89307035390601E-18));
#17334=CARTESIAN_POINT('Ctrl Pts',(-0.102221042121924,0.0972831505018574,
-2.31209379389524E-17));
#17335=CARTESIAN_POINT('Ctrl Pts',(-0.100229777791505,0.0997373632832089,
-2.08166817117217E-17));
#17336=CARTESIAN_POINT('Ctrl Pts',(-0.0937202782075859,0.107760254486057,
-1.32840027382311E-17));
#17337=CARTESIAN_POINT('Ctrl Pts',(-0.0863914655699752,0.115060936709644,
5.4842312373535E-18));
#17338=CARTESIAN_POINT('Ctrl Pts',(-0.0783508402622743,0.121487309774744,
1.38777878078145E-17));
#17339=CARTESIAN_POINT('Ctrl Pts',(-0.073610711791116,0.125275800441382,
1.8825977152717E-17));
#17340=CARTESIAN_POINT('Ctrl Pts',(-0.068622257850438,0.128760167547443,
-9.09579695168528E-18));
#17341=CARTESIAN_POINT('Ctrl Pts',(-0.0634007094575209,0.131904027763685,
-6.93889390390723E-18));
#17342=CARTESIAN_POINT('Origin',(0.,0.,0.));
#17343=CARTESIAN_POINT('Origin',(-0.0721687836487033,-0.125,-0.3));
#17344=CARTESIAN_POINT('',(-0.0721687836487033,-0.125,-0.3));
#17345=CARTESIAN_POINT('',(0.0721687836487032,-0.125,-0.3));
#17346=CARTESIAN_POINT('',(-0.0360843918243517,-0.125,-0.3));
#17347=CARTESIAN_POINT('',(-0.0721687836487033,-0.125,-0.15));
#17348=CARTESIAN_POINT('',(-0.0721687836487033,-0.125,-0.3));
#17349=CARTESIAN_POINT('',(0.0721687836487032,-0.125,-0.15));
#17350=CARTESIAN_POINT('',(-0.0721687836487033,-0.125,-0.15));
#17351=CARTESIAN_POINT('',(0.0721687836487032,-0.125,-0.3));
#17352=CARTESIAN_POINT('Origin',(-0.144337567297406,1.76762539787485E-17,
-0.3));
#17353=CARTESIAN_POINT('',(-0.144337567297406,1.76762539787485E-17,-0.3));
#17354=CARTESIAN_POINT('',(-0.126295371385231,-0.03125,-0.3));
#17355=CARTESIAN_POINT('',(-0.144337567297406,2.77555756156289E-17,-0.15));
#17356=CARTESIAN_POINT('',(-0.144337567297406,1.76762539787485E-17,-0.3));
#17357=CARTESIAN_POINT('',(-0.144337567297406,1.76762539787485E-17,-0.15));
#17358=CARTESIAN_POINT('Origin',(-0.0721687836487032,0.125,-0.3));
#17359=CARTESIAN_POINT('',(-0.0721687836487032,0.125,-0.3));
#17360=CARTESIAN_POINT('',(-0.090210979560879,0.09375,-0.3));
#17361=CARTESIAN_POINT('',(-0.0721687836487032,0.125,-0.15));
#17362=CARTESIAN_POINT('',(-0.0721687836487032,0.125,-0.3));
#17363=CARTESIAN_POINT('',(-0.0721687836487032,0.125,-0.15));
#17364=CARTESIAN_POINT('Origin',(0.0721687836487032,0.125,-0.3));
#17365=CARTESIAN_POINT('',(0.0721687836487032,0.125,-0.3));
#17366=CARTESIAN_POINT('',(0.0360843918243516,0.125,-0.3));
#17367=CARTESIAN_POINT('',(0.0721687836487032,0.125,-0.15));
#17368=CARTESIAN_POINT('',(0.0721687836487032,0.125,-0.3));
#17369=CARTESIAN_POINT('',(0.0721687836487032,0.125,-0.15));
#17370=CARTESIAN_POINT('Origin',(0.144337567297406,0.,-0.3));
#17371=CARTESIAN_POINT('',(0.144337567297406,0.,-0.3));
#17372=CARTESIAN_POINT('',(0.126295371385231,0.03125,-0.3));
#17373=CARTESIAN_POINT('',(0.144337567297406,0.,-0.15));
#17374=CARTESIAN_POINT('',(0.144337567297406,0.,-0.3));
#17375=CARTESIAN_POINT('',(0.144337567297406,0.,-0.15));
#17376=CARTESIAN_POINT('Origin',(0.0721687836487032,-0.125,-0.3));
#17377=CARTESIAN_POINT('',(0.0902109795608791,-0.09375,-0.3));
#17378=CARTESIAN_POINT('',(0.0721687836487032,-0.125,-0.15));
#17379=CARTESIAN_POINT('Origin',(0.,0.,-0.15));
#17380=CARTESIAN_POINT('Origin',(0.,0.,0.));
#17381=CARTESIAN_POINT('',(-0.275,-3.36777869765522E-17,0.));
#17382=CARTESIAN_POINT('Origin',(0.,0.,0.));
#17383=CARTESIAN_POINT('Origin',(0.,0.,-0.3));
#17384=CARTESIAN_POINT('',(-0.275,-3.36777869765522E-17,-0.3));
#17385=CARTESIAN_POINT('',(-0.275,-3.36777869765522E-17,-0.3));
#17386=CARTESIAN_POINT('Origin',(0.,0.,-0.3));
#17387=CARTESIAN_POINT('Origin',(0.,0.,-0.3));
#17388=CARTESIAN_POINT('Origin',(0.,0.,1.6));
#18338=UNCERTAINTY_MEASURE_WITH_UNIT(LENGTH_MEASURE(0.001),#18354,
'DISTANCE_ACCURACY_VALUE',
'Maximum model space distance between geometric entities at asserted c
onnectivities');
#18341=UNCERTAINTY_MEASURE_WITH_UNIT(LENGTH_MEASURE(0.001),#18354,
'DISTANCE_ACCURACY_VALUE',
'Maximum model space distance between geometric entities at asserted c
onnectivities');
#18350=(
GEOMETRIC_REPRESENTATION_CONTEXT(3)
GLOBAL_UNCERTAINTY_ASSIGNED_CONTEXT((#18338))
GLOBAL_UNIT_ASSIGNED_CONTEXT((#18354,#18356,#18357))
REPRESENTATION_CONTEXT('','3D')
);
#18353=(
GEOMETRIC_REPRESENTATION_CONTEXT(3)
GLOBAL_UNCERTAINTY_ASSIGNED_CONTEXT((#18341))
GLOBAL_UNIT_ASSIGNED_CONTEXT((#18354,#18356,#18357))
REPRESENTATION_CONTEXT('','3D')
);
#18354=(
LENGTH_UNIT()
NAMED_UNIT(*)
SI_UNIT(.CENTI.,.METRE.)
);
#18356=(
NAMED_UNIT(*)
PLANE_ANGLE_UNIT()
SI_UNIT($,.RADIAN.)
);
#18357=(
NAMED_UNIT(*)
SI_UNIT($,.STERADIAN.)
SOLID_ANGLE_UNIT()
);
#18366=SHAPE_DEFINITION_REPRESENTATION(#18377,#18404);
#18377=PRODUCT_DEFINITION_SHAPE('',$,#18416);
#18404=SHAPE_REPRESENTATION('',(#6949),#18350);
#18407=PRODUCT_DEFINITION_CONTEXT('part definition',#18442,'design');
#18416=PRODUCT_DEFINITION('2026-11-10-01-32-12-367',
'Socket head cap screw M3x16',#18427,#18407);
#18427=PRODUCT_DEFINITION_FORMATION('',$,#18452);
#18442=APPLICATION_CONTEXT(
'Core Data for Automotive Mechanical Design Process');
#18443=PRODUCT_CONTEXT('part definition',#18442,'mechanical');
#18452=PRODUCT('2026-11-10-01-32-12-367','Socket head cap screw M3x16',
$,(#18443));
#18458=PRESENTATION_STYLE_ASSIGNMENT((#18466));
#18466=SURFACE_STYLE_USAGE(.BOTH.,#18474);
#18474=SURFACE_SIDE_STYLE('',(#18482));
#18482=SURFACE_STYLE_FILL_AREA(#18490);
#18490=FILL_AREA_STYLE('Dark gray',(#18498));
#18498=FILL_AREA_STYLE_COLOUR('Dark gray',#18506);
#18506=COLOUR_RGB('Dark gray',0.250980392156863,0.282352941176471,0.32156862745098);
ENDSEC;
END-ISO-10303-21;
